ISO-10303-21;
HEADER;
FILE_DESCRIPTION (('STEP AP214'),
    '1' );
FILE_NAME ('slow gear_ISO - Spur gear 2M 80T 20PA 12FW ---S80A75H50L38.0N.step',
    '2026-09-30T12:41:04',
    ( '' ),
    ( '' ),
    'SwSTEP 2.0',
    'SolidWorks 2026',
    '' );
FILE_SCHEMA (( 'AUTOMOTIVE_DESIGN' ));
ENDSEC;

DATA;
#4=VECTOR ( 'NONE', #40602, 1000.000000000000000 ) ;
#10=DIRECTION ( 'NONE',  ( 1.000000000000000000, 0.000000000000000000, 0.000000000000000000 ) ) ;
#17=DIRECTION ( 'NONE',  ( 0.000000000000000000, 0.000000000000000000, 1.000000000000000000 ) ) ;
#18=VERTEX_POINT ( 'NONE', #22403 ) ;
#19=CARTESIAN_POINT ( 'NONE',  ( 0.000000000000000000, 44.99326035066052043, 68.55367621811159040 ) ) ;
#21=CARTESIAN_POINT ( 'NONE',  ( 11.99999999999999822, 70.53064760720316428, -26.01480285779861035 ) ) ;
#22=ORIENTED_EDGE ( 'NONE', *, *, #45043, .F. ) ;
#26=DIRECTION ( 'NONE',  ( -1.000000000000000000, -0.000000000000000000, -0.000000000000000000 ) ) ;
#31=DIRECTION ( 'NONE',  ( 1.000000000000000000, 0.000000000000000000, -0.000000000000000000 ) ) ;
#36=FACE_OUTER_BOUND ( 'NONE', #8537, .T. ) ;
#39=AXIS2_PLACEMENT_3D ( 'NONE', #46336, #27993, #5460 ) ;
#44=CARTESIAN_POINT ( 'NONE',  ( 0.000000000000000000, 73.44644590900061587, 24.73286445877730699 ) ) ;
#50=DIRECTION ( 'NONE',  ( 0.000000000000000000, -0.4999999999999930611, 0.8660254037844425934 ) ) ;
#54=DIRECTION ( 'NONE',  ( -1.000000000000000000, -0.000000000000000000, -0.000000000000000000 ) ) ;
#57=ORIENTED_EDGE ( 'NONE', *, *, #193, .F. ) ;
#59=VERTEX_POINT ( 'NONE', #33639 ) ;
#62=EDGE_CURVE ( 'NONE', #675, #34767, #3595, .T. ) ;
#68=CIRCLE ( 'NONE', #32916, 31.99999999999998224 ) ;
#70=EDGE_LOOP ( 'NONE', ( #7032, #13998, #28047, #46307 ) ) ;
#71=EDGE_LOOP ( 'NONE', ( #28920, #38356, #28549, #18145 ) ) ;
#73=FACE_OUTER_BOUND ( 'NONE', #11350, .T. ) ;
#76=CARTESIAN_POINT ( 'NONE',  ( 11.99999999999999822, -79.10210256391353312, -21.60688246758669706 ) ) ;
#79=ORIENTED_EDGE ( 'NONE', *, *, #47708, .T. ) ;
#82=LINE ( 'NONE', #3762, #40454 ) ;
#92=DIRECTION ( 'NONE',  ( 0.000000000000000000, 0.000000000000000000, 1.000000000000000000 ) ) ;
#118=CIRCLE ( 'NONE', #32928, 31.99999999999998224 ) ;
#119=CARTESIAN_POINT ( 'NONE',  ( 15.00000000000000000, -22.67460108101782978, -6.353146135317906840 ) ) ;
#121=ADVANCED_FACE ( 'NONE', ( #18943 ), #45382, .T. ) ;
#123=CARTESIAN_POINT ( 'NONE',  ( 5.999999999999999112, 56.15606465354958488, 59.75363087400094741 ) ) ;
#127=VERTEX_POINT ( 'NONE', #19425 ) ;
#131=CIRCLE ( 'NONE', #25925, 31.99999999999998934 ) ;
#133=AXIS2_PLACEMENT_3D ( 'NONE', #22370, #41687, #26758 ) ;
#135=ORIENTED_EDGE ( 'NONE', *, *, #5274, .F. ) ;
#136=CARTESIAN_POINT ( 'NONE',  ( 11.99999999999999822, 0.000000000000000000, 0.000000000000000000 ) ) ;
#138=CIRCLE ( 'NONE', #1733, 82.00000000000000000 ) ;
#139=DIRECTION ( 'NONE',  ( -1.000000000000000000, 0.000000000000000000, 0.000000000000000000 ) ) ;
#140=EDGE_CURVE ( 'NONE', #28665, #44874, #33290, .T. ) ;
#143=CARTESIAN_POINT ( 'NONE',  ( 11.99999999999999822, 0.000000000000000000, 0.000000000000000000 ) ) ;
#144=DIRECTION ( 'NONE',  ( -1.000000000000000000, -0.000000000000000000, -0.000000000000000000 ) ) ;
#147=VECTOR ( 'NONE', #27818, 1000.000000000000000 ) ;
#152=ORIENTED_EDGE ( 'NONE', *, *, #45219, .T. ) ;
#154=ORIENTED_EDGE ( 'NONE', *, *, #22343, .F. ) ;
#155=DIRECTION ( 'NONE',  ( 0.000000000000000000, -0.9876883405951359940, -0.1564344650402420545 ) ) ;
#158=LINE ( 'NONE', #18756, #11859 ) ;
#159=DIRECTION ( 'NONE',  ( 0.000000000000000000, 0.000000000000000000, 1.000000000000000000 ) ) ;
#161=ADVANCED_FACE ( 'NONE', ( #29498 ), #7218, .T. ) ;
#172=ORIENTED_EDGE ( 'NONE', *, *, #6354, .T. ) ;
#174=CIRCLE ( 'NONE', #27550, 82.00000000000000000 ) ;
#177=CARTESIAN_POINT ( 'NONE',  ( 11.99999999999999822, -46.53671651293991118, 59.03961581697383565 ) ) ;
#182=EDGE_LOOP ( 'NONE', ( #38740, #26443, #686, #38124 ) ) ;
#185=ORIENTED_EDGE ( 'NONE', *, *, #40077, .F. ) ;
#188=VERTEX_POINT ( 'NONE', #17657 ) ;
#193=EDGE_CURVE ( 'NONE', #40856, #22912, #44332, .T. ) ;
#194=FACE_OUTER_BOUND ( 'NONE', #46071, .T. ) ;
#198=EDGE_LOOP ( 'NONE', ( #6220, #43941, #13520, #1756 ) ) ;
#200=AXIS2_PLACEMENT_3D ( 'NONE', #41654, #37008, #21837 ) ;
#201=PRESENTATION_STYLE_ASSIGNMENT (( #44758 ) ) ;
#203=ORIENTED_EDGE ( 'NONE', *, *, #19001, .T. ) ;
#215=ADVANCED_FACE ( 'NONE', ( #21326 ), #36975, .T. ) ;
#221=DIRECTION ( 'NONE',  ( -1.000000000000000000, 0.000000000000000000, 0.000000000000000000 ) ) ;
#223=ADVANCED_FACE ( 'NONE', ( #47514 ), #10805, .T. ) ;
#231=CIRCLE ( 'NONE', #23691, 31.99999999999998934 ) ;
#240=CARTESIAN_POINT ( 'NONE',  ( -10.00000000000000000, 0.000000000000000000, 0.000000000000000000 ) ) ;
#241=CIRCLE ( 'NONE', #16690, 77.49900000000000944 ) ;
#242=CARTESIAN_POINT ( 'NONE',  ( 11.99999999999999822, -72.35432306680469594, -20.40083707022958848 ) ) ;
#252=CARTESIAN_POINT ( 'NONE',  ( 15.00000000000000000, -18.13022148937242761, 15.02647892043569122 ) ) ;
#253=CARTESIAN_POINT ( 'NONE',  ( 11.99999999999999822, 0.000000000000000000, 0.000000000000000000 ) ) ;
#257=ORIENTED_EDGE ( 'NONE', *, *, #33177, .T. ) ;
#259=DIRECTION ( 'NONE',  ( -1.000000000000000000, -0.000000000000000000, -0.000000000000000000 ) ) ;
#260=ORIENTED_EDGE ( 'NONE', *, *, #36083, .F. ) ;
#269=EDGE_CURVE ( 'NONE', #2093, #2200, #29638, .T. ) ;
#272=DIRECTION ( 'NONE',  ( -1.000000000000000000, 0.000000000000000000, 0.000000000000000000 ) ) ;
#276=DIRECTION ( 'NONE',  ( 0.000000000000000000, -1.301042606982602560E-15, 1.000000000000000000 ) ) ;
#286=CIRCLE ( 'NONE', #18276, 31.99999999999998934 ) ;
#295=CARTESIAN_POINT ( 'NONE',  ( 12.00000000000000000, -22.67460108101782268, -6.353146135317906840 ) ) ;
#297=ORIENTED_EDGE ( 'NONE', *, *, #34739, .T. ) ;
#302=CIRCLE ( 'NONE', #25312, 77.49899999999999523 ) ;
#304=FACE_OUTER_BOUND ( 'NONE', #9767, .T. ) ;
#307=AXIS2_PLACEMENT_3D ( 'NONE', #36278, #3214, #10821 ) ;
#312=ORIENTED_EDGE ( 'NONE', *, *, #16850, .T. ) ;
#318=EDGE_CURVE ( 'NONE', #41614, #22825, #9882, .T. ) ;
#321=CYLINDRICAL_SURFACE ( 'NONE', #35288, 31.99999999999998579 ) ;
#322=EDGE_CURVE ( 'NONE', #35660, #31329, #38199, .T. ) ;
#323=CARTESIAN_POINT ( 'NONE',  ( 11.99999999999999822, -49.70050353004846500, -59.46389618802017907 ) ) ;
#325=AXIS2_PLACEMENT_3D ( 'NONE', #13479, #5912, #24495 ) ;
#329=ORIENTED_EDGE ( 'NONE', *, *, #30247, .T. ) ;
#330=EDGE_CURVE ( 'NONE', #44007, #20943, #37237, .T. ) ;
#331=AXIS2_PLACEMENT_3D ( 'NONE', #33275, #33743, #3658 ) ;
#333=AXIS2_PLACEMENT_3D ( 'NONE', #25881, #22476, #15130 ) ;
#341=CARTESIAN_POINT ( 'NONE',  ( 11.99999999999999822, 0.000000000000000000, 0.000000000000000000 ) ) ;
#343=CYLINDRICAL_SURFACE ( 'NONE', #30928, 31.99999999999998579 ) ;
#344=DIRECTION ( 'NONE',  ( 0.000000000000000000, -0.1045284632676569680, -0.9945218953682730678 ) ) ;
#345=ADVANCED_FACE ( 'NONE', ( #515 ), #15447, .T. ) ;
#346=DIRECTION ( 'NONE',  ( -1.000000000000000000, -0.000000000000000000, 0.000000000000000000 ) ) ;
#348=DIRECTION ( 'NONE',  ( -1.000000000000000000, 0.000000000000000000, -0.000000000000000000 ) ) ;
#351=EDGE_CURVE ( 'NONE', #24067, #38319, #7847, .T. ) ;
#352=VERTEX_POINT ( 'NONE', #977 ) ;
#362=ADVANCED_FACE ( 'NONE', ( #19342 ), #12497, .T. ) ;
#363=AXIS2_PLACEMENT_3D ( 'NONE', #3070, #22645, #37583 ) ;
#366=AXIS2_PLACEMENT_3D ( 'NONE', #37130, #40340, #3598 ) ;
#369=AXIS2_PLACEMENT_3D ( 'NONE', #26235, #32831, #22557 ) ;
#373=ADVANCED_FACE ( 'NONE', ( #37707 ), #45293, .T. ) ;
#378=DIRECTION ( 'NONE',  ( 0.000000000000000000, -0.8660254037844421493, -0.4999999999999939493 ) ) ;
#382=EDGE_CURVE ( 'NONE', #975, #23651, #30608, .T. ) ;
#384=ORIENTED_EDGE ( 'NONE', *, *, #2359, .F. ) ;
#387=CARTESIAN_POINT ( 'NONE',  ( 12.00000000000000000, 6.762365576493647445, 25.66652317338391498 ) ) ;
#388=CIRCLE ( 'NONE', #33997, 31.99999999999998579 ) ;
#391=ORIENTED_EDGE ( 'NONE', *, *, #18436, .F. ) ;
#396=DIRECTION ( 'NONE',  ( 0.000000000000000000, 0.000000000000000000, 1.000000000000000000 ) ) ;
#400=DIRECTION ( 'NONE',  ( -1.000000000000000000, 0.000000000000000000, -0.000000000000000000 ) ) ;
#401=DIRECTION ( 'NONE',  ( 0.000000000000000000, 0.9945218953682730678, -0.1045284632676570791 ) ) ;
#402=DIRECTION ( 'NONE',  ( -1.000000000000000000, 0.000000000000000000, -0.000000000000000000 ) ) ;
#405=ORIENTED_EDGE ( 'NONE', *, *, #13443, .T. ) ;
#408=AXIS2_PLACEMENT_3D ( 'NONE', #31501, #26915, #8309 ) ;
#410=VERTEX_POINT ( 'NONE', #19816 ) ;
#411=PLANE ( 'NONE',  #16338 ) ;
#416=AXIS2_PLACEMENT_3D ( 'NONE', #18456, #18686, #44643 ) ;
#417=VECTOR ( 'NONE', #47685, 1000.000000000000000 ) ;
#424=CIRCLE ( 'NONE', #33232, 31.99999999999999289 ) ;
#432=CARTESIAN_POINT ( 'NONE',  ( 12.00000000000000000, 18.84667830672579925, -18.68964196561269375 ) ) ;
#437=DIRECTION ( 'NONE',  ( 0.000000000000000000, 0.000000000000000000, 1.000000000000000000 ) ) ;
#438=ORIENTED_EDGE ( 'NONE', *, *, #14400, .T. ) ;
#439=EDGE_LOOP ( 'NONE', ( #31934, #23620, #8333, #8403 ) ) ;
#443=CIRCLE ( 'NONE', #16876, 77.49899999999999523 ) ;
#445=ADVANCED_FACE ( 'NONE', ( #22776 ), #33780, .F. ) ;
#455=CIRCLE ( 'NONE', #41872, 77.49899999999999523 ) ;
#457=CARTESIAN_POINT ( 'NONE',  ( 0.000000000000000000, 0.000000000000000000, 0.000000000000000000 ) ) ;
#458=DIRECTION ( 'NONE',  ( 1.000000000000000000, 0.000000000000000000, 0.000000000000000000 ) ) ;
#461=VERTEX_POINT ( 'NONE', #39664 ) ;
#463=VECTOR ( 'NONE', #18147, 1000.000000000000114 ) ;
#476=DIRECTION ( 'NONE',  ( -1.000000000000000000, 0.000000000000000000, 0.000000000000000000 ) ) ;
#485=FILL_AREA_STYLE ('',( #30352 ) ) ;
#486=AXIS2_PLACEMENT_3D ( 'NONE', #8349, #993, #38213 ) ;
#487=LINE ( 'NONE', #45760, #16267 ) ;
#488=VERTEX_POINT ( 'NONE', #2425 ) ;
#492=ADVANCED_FACE ( 'NONE', ( #9294 ), #21030, .T. ) ;
#496=FACE_OUTER_BOUND ( 'NONE', #5249, .T. ) ;
#501=FACE_OUTER_BOUND ( 'NONE', #22747, .T. ) ;
#503=ORIENTED_EDGE ( 'NONE', *, *, #28074, .T. ) ;
#504=ORIENTED_EDGE ( 'NONE', *, *, #40543, .F. ) ;
#506=EDGE_CURVE ( 'NONE', #11777, #14224, #24669, .T. ) ;
#507=EDGE_CURVE ( 'NONE', #9625, #26682, #29342, .T. ) ;
#511=ORIENTED_EDGE ( 'NONE', *, *, #46423, .T. ) ;
#515=FACE_OUTER_BOUND ( 'NONE', #30757, .T. ) ;
#517=ORIENTED_EDGE ( 'NONE', *, *, #27272, .F. ) ;
#518=CARTESIAN_POINT ( 'NONE',  ( 0.000000000000000000, 0.000000000000000000, 0.000000000000000000 ) ) ;
#520=EDGE_CURVE ( 'NONE', #45830, #43377, #33250, .T. ) ;
#524=AXIS2_PLACEMENT_3D ( 'NONE', #22263, #15169, #37667 ) ;
#526=VERTEX_POINT ( 'NONE', #2197 ) ;
#527=ORIENTED_EDGE ( 'NONE', *, *, #14213, .F. ) ;
#530=CARTESIAN_POINT ( 'NONE',  ( 12.00000000000000000, -19.89357724625003598, -12.59942793731059041 ) ) ;
#532=CARTESIAN_POINT ( 'NONE',  ( 11.99999999999999822, 0.000000000000000000, 0.000000000000000000 ) ) ;
#540=FACE_OUTER_BOUND ( 'NONE', #34689, .T. ) ;
#550=FACE_BOUND ( 'NONE', #1348, .T. ) ;
#554=DIRECTION ( 'NONE',  ( -1.000000000000000000, -0.000000000000000000, -0.000000000000000000 ) ) ;
#558=CARTESIAN_POINT ( 'NONE',  ( 11.99999999999999822, 0.000000000000000000, 0.000000000000000000 ) ) ;
#560=ORIENTED_EDGE ( 'NONE', *, *, #33166, .F. ) ;
#564=DIRECTION ( 'NONE',  ( 1.000000000000000000, 0.000000000000000000, 0.000000000000000000 ) ) ;
#568=ORIENTED_EDGE ( 'NONE', *, *, #2288, .F. ) ;
#573=ADVANCED_FACE ( 'NONE', ( #39161 ), #35489, .T. ) ;
#574=AXIS2_PLACEMENT_3D ( 'NONE', #17954, #2794, #25781 ) ;
#577=ORIENTED_EDGE ( 'NONE', *, *, #21771, .T. ) ;
#578=PLANE ( 'NONE',  #34185 ) ;
#579=ORIENTED_EDGE ( 'NONE', *, *, #16817, .F. ) ;
#581=FACE_OUTER_BOUND ( 'NONE', #182, .T. ) ;
#582=AXIS2_PLACEMENT_3D ( 'NONE', #32036, #28341, #6089 ) ;
#583=DIRECTION ( 'NONE',  ( 0.000000000000000000, -6.938893903907231533E-15, 1.000000000000000000 ) ) ;
#585=DIRECTION ( 'NONE',  ( 1.000000000000000000, -0.000000000000000000, -0.000000000000000000 ) ) ;
#586=ORIENTED_EDGE ( 'NONE', *, *, #36028, .F. ) ;
#589=CARTESIAN_POINT ( 'NONE',  ( 11.99999999999999822, -75.11764819372145041, -2.946379043147127064 ) ) ;
#590=CARTESIAN_POINT ( 'NONE',  ( 11.99999999999999822, 70.52718814184294160, -26.02418014898236720 ) ) ;
#591=DIRECTION ( 'NONE',  ( 0.000000000000000000, 0.000000000000000000, 1.000000000000000000 ) ) ;
#592=VECTOR ( 'NONE', #29908, 1000.000000000000000 ) ;
#593=CARTESIAN_POINT ( 'NONE',  ( 11.99999999999999822, 23.16143007188530589, -73.95703589263951017 ) ) ;
#602=DIRECTION ( 'NONE',  ( 0.000000000000000000, 0.8910065241883655673, 0.4539904997395510233 ) ) ;
#611=ADVANCED_FACE ( 'NONE', ( #47931 ), #25903, .T. ) ;
#617=DIRECTION ( 'NONE',  ( 0.000000000000000000, 0.2334453638558991462, 0.9723699203976781114 ) ) ;
#618=EDGE_CURVE ( 'NONE', #28447, #9412, #30123, .T. ) ;
#619=DIRECTION ( 'NONE',  ( 0.000000000000000000, 0.000000000000000000, 1.000000000000000000 ) ) ;
#621=ORIENTED_EDGE ( 'NONE', *, *, #41797, .T. ) ;
#624=ORIENTED_EDGE ( 'NONE', *, *, #30351, .F. ) ;
#626=LINE ( 'NONE', #4313, #10010 ) ;
#632=ORIENTED_EDGE ( 'NONE', *, *, #24201, .T. ) ;
#636=DIRECTION ( 'NONE',  ( 0.000000000000000000, -0.5877852522924625900, -0.8090169943749551118 ) ) ;
#642=DIRECTION ( 'NONE',  ( -0.000000000000000000, 1.000000000000000000, 0.000000000000000000 ) ) ;
#645=EDGE_CURVE ( 'NONE', #28702, #28196, #9047, .T. ) ;
#647=AXIS2_PLACEMENT_3D ( 'NONE', #9074, #34765, #1982 ) ;
#650=CARTESIAN_POINT ( 'NONE',  ( 11.99999999999999822, 72.35160999960817207, 20.41045688087850607 ) ) ;
#652=CYLINDRICAL_SURFACE ( 'NONE', #35679, 31.99999999999998579 ) ;
#659=DIRECTION ( 'NONE',  ( -1.000000000000000000, 0.000000000000000000, 0.000000000000000000 ) ) ;
#663=CARTESIAN_POINT ( 'NONE',  ( 12.00000000000000000, 23.49999999999999645, -1.500000000000003997 ) ) ;
#664=EDGE_CURVE ( 'NONE', #21593, #23778, #16081, .T. ) ;
#667=EDGE_CURVE ( 'NONE', #33047, #27075, #32761, .T. ) ;
#675=VERTEX_POINT ( 'NONE', #43788 ) ;
#676=ORIENTED_EDGE ( 'NONE', *, *, #28784, .F. ) ;
#677=AXIS2_PLACEMENT_3D ( 'NONE', #21476, #3341, #40339 ) ;
#684=CARTESIAN_POINT ( 'NONE',  ( 11.99999999999999822, 0.000000000000000000, 0.000000000000000000 ) ) ;
#686=ORIENTED_EDGE ( 'NONE', *, *, #40398, .T. ) ;
#688=CARTESIAN_POINT ( 'NONE',  ( 11.99999999999999822, 0.000000000000000000, 0.000000000000000000 ) ) ;
#705=CARTESIAN_POINT ( 'NONE',  ( 0.000000000000000000, 56.15606465354958488, 59.75363087400094741 ) ) ;
#709=ADVANCED_FACE ( 'NONE', ( #21264 ), #44029, .T. ) ;
#712=CYLINDRICAL_SURFACE ( 'NONE', #5093, 82.00000000000000000 ) ;
#719=DIRECTION ( 'NONE',  ( 0.000000000000000000, 0.5000000000000028866, 0.8660254037844369313 ) ) ;
#721=EDGE_CURVE ( 'NONE', #7607, #27429, #23665, .T. ) ;
#728=ORIENTED_EDGE ( 'NONE', *, *, #7555, .T. ) ;
#729=CIRCLE ( 'NONE', #29676, 31.99999999999998579 ) ;
#732=ORIENTED_EDGE ( 'NONE', *, *, #4706, .T. ) ;
#734=ORIENTED_EDGE ( 'NONE', *, *, #13088, .T. ) ;
#735=LINE ( 'NONE', #38434, #18069 ) ;
#738=DIRECTION ( 'NONE',  ( 0.000000000000000000, 0.000000000000000000, 1.000000000000000000 ) ) ;
#745=ADVANCED_FACE ( 'NONE', ( #194 ), #26408, .T. ) ;
#746=CARTESIAN_POINT ( 'NONE',  ( -10.00000000000000000, 0.000000000000000000, 0.000000000000000000 ) ) ;
#749=VECTOR ( 'NONE', #11834, 1000.000000000000000 ) ;
#755=DIRECTION ( 'NONE',  ( 0.000000000000000000, 0.000000000000000000, 1.000000000000000000 ) ) ;
#765=CARTESIAN_POINT ( 'NONE',  ( 11.99999999999999822, 0.000000000000000000, 0.000000000000000000 ) ) ;
#766=LINE ( 'NONE', #19371, #42587 ) ;
#775=CARTESIAN_POINT ( 'NONE',  ( 12.00000000000000000, 20.85821328998756385, 10.92862929874494249 ) ) ;
#782=EDGE_CURVE ( 'NONE', #24639, #37652, #34589, .T. ) ;
#787=LINE ( 'NONE', #33836, #29193 ) ;
#795=DIRECTION ( 'NONE',  ( 1.000000000000000000, 0.000000000000000000, 0.000000000000000000 ) ) ;
#800=EDGE_CURVE ( 'NONE', #47535, #10792, #4146, .T. ) ;
#806=AXIS2_PLACEMENT_3D ( 'NONE', #23101, #7683, #8409 ) ;
#811=CARTESIAN_POINT ( 'NONE',  ( 11.99999999999999822, -71.27951684758045303, 30.41916302227090085 ) ) ;
#813=DIRECTION ( 'NONE',  ( -1.000000000000000000, 0.000000000000000000, 0.000000000000000000 ) ) ;
#814=EDGE_CURVE ( 'NONE', #4586, #33388, #24439, .T. ) ;
#820=LINE ( 'NONE', #30223, #45753 ) ;
#825=EDGE_CURVE ( 'NONE', #38067, #45904, #11958, .T. ) ;
#827=CARTESIAN_POINT ( 'NONE',  ( 12.00000000000000355, 2.571758278209441661E-15, -21.00000000000000000 ) ) ;
#834=ORIENTED_EDGE ( 'NONE', *, *, #44618, .F. ) ;
#836=CIRCLE ( 'NONE', #46174, 82.00000000000000000 ) ;
#839=AXIS2_PLACEMENT_3D ( 'NONE', #13782, #32608, #9855 ) ;
#841=ORIENTED_EDGE ( 'NONE', *, *, #9017, .F. ) ;
#846=AXIS2_PLACEMENT_3D ( 'NONE', #12039, #42367, #4917 ) ;
#848=CIRCLE ( 'NONE', #7885, 31.99999999999998579 ) ;
#853=ORIENTED_EDGE ( 'NONE', *, *, #27879, .T. ) ;
#854=DIRECTION ( 'NONE',  ( 1.000000000000000000, 0.000000000000000000, 0.000000000000000000 ) ) ;
#855=FACE_OUTER_BOUND ( 'NONE', #20424, .T. ) ;
#857=ORIENTED_EDGE ( 'NONE', *, *, #37873, .T. ) ;
#859=ORIENTED_EDGE ( 'NONE', *, *, #34994, .T. ) ;
#860=DIRECTION ( 'NONE',  ( 0.000000000000000000, 0.000000000000000000, 1.000000000000000000 ) ) ;
#861=EDGE_CURVE ( 'NONE', #2920, #21783, #40860, .T. ) ;
#862=DIRECTION ( 'NONE',  ( -1.000000000000000000, 0.000000000000000000, 0.000000000000000000 ) ) ;
#867=ADVANCED_FACE ( 'NONE', ( #3881 ), #46705, .T. ) ;
#872=LINE ( 'NONE', #4802, #26195 ) ;
#874=ORIENTED_EDGE ( 'NONE', *, *, #29513, .T. ) ;
#878=AXIS2_PLACEMENT_3D ( 'NONE', #26880, #35416, #24170 ) ;
#879=LINE ( 'NONE', #34648, #19134 ) ;
#897=VERTEX_POINT ( 'NONE', #42547 ) ;
#903=ORIENTED_EDGE ( 'NONE', *, *, #45602, .F. ) ;
#913=VERTEX_POINT ( 'NONE', #43024 ) ;
#914=ORIENTED_EDGE ( 'NONE', *, *, #29615, .F. ) ;
#916=CARTESIAN_POINT ( 'NONE',  ( 5.999999999999999112, 59.75363087400076267, 56.15606465354979093 ) ) ;
#917=DIRECTION ( 'NONE',  ( 0.000000000000000000, 0.000000000000000000, 1.000000000000000000 ) ) ;
#922=FACE_OUTER_BOUND ( 'NONE', #42259, .T. ) ;
#923=VERTEX_POINT ( 'NONE', #46935 ) ;
#924=EDGE_CURVE ( 'NONE', #15440, #36912, #16644, .T. ) ;
#925=VERTEX_POINT ( 'NONE', #42791 ) ;
#927=EDGE_CURVE ( 'NONE', #44612, #1839, #4897, .T. ) ;
#930=ADVANCED_FACE ( 'NONE', ( #45978 ), #31294, .T. ) ;
#933=ORIENTED_EDGE ( 'NONE', *, *, #27214, .F. ) ;
#938=LINE ( 'NONE', #4404, #46109 ) ;
#942=DIRECTION ( 'NONE',  ( -1.000000000000000000, 0.000000000000000000, 0.000000000000000000 ) ) ;
#945=CARTESIAN_POINT ( 'NONE',  ( 11.99999999999999822, -36.72794159290197769, -65.59268652807249111 ) ) ;
#947=CIRCLE ( 'NONE', #11904, 77.49899999999999523 ) ;
#952=CARTESIAN_POINT ( 'NONE',  ( 11.99999999999999822, -23.16143007188479430, 73.95703589263968070 ) ) ;
#955=EDGE_LOOP ( 'NONE', ( #35156, #19832, #28140, #2313 ) ) ;
#959=CIRCLE ( 'NONE', #40842, 31.99999999999998224 ) ;
#975=VERTEX_POINT ( 'NONE', #29535 ) ;
#976=AXIS2_PLACEMENT_3D ( 'NONE', #12212, #8513, #41339 ) ;
#977=CARTESIAN_POINT ( 'NONE',  ( 11.99999999999999822, 65.64334221924964652, -41.19522573413665611 ) ) ;
#988=CARTESIAN_POINT ( 'NONE',  ( 0.000000000000000000, -40.65526001592564853, -71.21200624218839437 ) ) ;
#989=EDGE_LOOP ( 'NONE', ( #38099, #45863, #32407, #6459 ) ) ;
#990=ORIENTED_EDGE ( 'NONE', *, *, #33029, .T. ) ;
#992=CARTESIAN_POINT ( 'NONE',  ( 12.00000000000000000, -20.55727247249748402, -16.78983467731284307 ) ) ;
#993=DIRECTION ( 'NONE',  ( -1.000000000000000000, 0.000000000000000000, 0.000000000000000000 ) ) ;
#1001=FACE_OUTER_BOUND ( 'NONE', #11697, .T. ) ;
#1007=DIRECTION ( 'NONE',  ( 0.000000000000000000, 0.000000000000000000, -1.000000000000000000 ) ) ;
#1013=VERTEX_POINT ( 'NONE', #43512 ) ;
#1015=ORIENTED_EDGE ( 'NONE', *, *, #23172, .F. ) ;
#1016=CARTESIAN_POINT ( 'NONE',  ( 11.99999999999999822, -30.41916302227164337, 71.27951684758015460 ) ) ;
#1025=EDGE_CURVE ( 'NONE', #38548, #48127, #43741, .T. ) ;
#1028=CIRCLE ( 'NONE', #30787, 82.00000000000000000 ) ;
#1031=CARTESIAN_POINT ( 'NONE',  ( 11.99999999999999822, 75.11725578898472122, -2.956366410619845730 ) ) ;
#1032=ORIENTED_EDGE ( 'NONE', *, *, #24148, .T. ) ;
#1039=CYLINDRICAL_SURFACE ( 'NONE', #12663, 77.49899999999999523 ) ;
#1043=ORIENTED_EDGE ( 'NONE', *, *, #44084, .F. ) ;
#1044=CARTESIAN_POINT ( 'NONE',  ( 11.99999999999999822, 56.15606465355041621, -59.75363087400016582 ) ) ;
#1046=VERTEX_POINT ( 'NONE', #7254 ) ;
#1048=VECTOR ( 'NONE', #20936, 1000.000000000000000 ) ;
#1056=CARTESIAN_POINT ( 'NONE',  ( 0.000000000000000000, -27.74655509720726343, 77.16300072079651784 ) ) ;
#1058=DIRECTION ( 'NONE',  ( -1.000000000000000000, -0.000000000000000000, 0.000000000000000000 ) ) ;
#1059=DIRECTION ( 'NONE',  ( 0.000000000000000000, 0.000000000000000000, 1.000000000000000000 ) ) ;
#1061=CARTESIAN_POINT ( 'NONE',  ( 11.99999999999999822, -36.73666225445845157, -65.58780272294114866 ) ) ;
#1073=ORIENTED_EDGE ( 'NONE', *, *, #12908, .T. ) ;
#1079=DIRECTION ( 'NONE',  ( -1.000000000000000000, 0.000000000000000000, -0.000000000000000000 ) ) ;
#1080=VERTEX_POINT ( 'NONE', #36865 ) ;
#1085=AXIS2_PLACEMENT_3D ( 'NONE', #8224, #22667, #30020 ) ;
#1091=AXIS2_PLACEMENT_3D ( 'NONE', #34675, #1411, #16107 ) ;
#1092=AXIS2_PLACEMENT_3D ( 'NONE', #19598, #38229, #1007 ) ;
#1093=CARTESIAN_POINT ( 'NONE',  ( 11.99999999999999822, -71.91182617369167929, -28.89263327155821059 ) ) ;
#1094=VECTOR ( 'NONE', #31075, 1000.000000000000000 ) ;
#1097=DIRECTION ( 'NONE',  ( 0.000000000000000000, -0.9723699203976741146, -0.2334453638559158550 ) ) ;
#1100=ORIENTED_EDGE ( 'NONE', *, *, #618, .T. ) ;
#1107=DIRECTION ( 'NONE',  ( -1.000000000000000000, -0.000000000000000000, -0.000000000000000000 ) ) ;
#1109=ORIENTED_EDGE ( 'NONE', *, *, #34348, .F. ) ;
#1114=LINE ( 'NONE', #18135, #7231 ) ;
#1115=DIRECTION ( 'NONE',  ( -1.000000000000000000, 0.000000000000000000, 0.000000000000000000 ) ) ;
#1126=ORIENTED_EDGE ( 'NONE', *, *, #27531, .F. ) ;
#1127=ORIENTED_EDGE ( 'NONE', *, *, #25941, .T. ) ;
#1131=CARTESIAN_POINT ( 'NONE',  ( 11.99999999999999822, 8.830959090342393125, 74.65491531819122883 ) ) ;
#1139=DIRECTION ( 'NONE',  ( -0.000000000000000000, -0.3090169943749450088, 0.9510565162951543083 ) ) ;
#1145=CIRCLE ( 'NONE', #23016, 31.99999999999999645 ) ;
#1147=VERTEX_POINT ( 'NONE', #11900 ) ;
#1154=ORIENTED_EDGE ( 'NONE', *, *, #22036, .F. ) ;
#1156=DIRECTION ( 'NONE',  ( -1.000000000000000000, -0.000000000000000000, -0.000000000000000000 ) ) ;
#1158=EDGE_CURVE ( 'NONE', #7124, #22172, #18982, .T. ) ;
#1164=EDGE_CURVE ( 'NONE', #6579, #913, #16687, .T. ) ;
#1168=AXIS2_PLACEMENT_3D ( 'NONE', #16765, #2531, #17466 ) ;
#1171=DIRECTION ( 'NONE',  ( -1.000000000000000000, 0.000000000000000000, 0.000000000000000000 ) ) ;
#1172=ADVANCED_FACE ( 'NONE', ( #11178 ), #37599, .T. ) ;
#1175=FACE_OUTER_BOUND ( 'NONE', #13442, .T. ) ;
#1177=ORIENTED_EDGE ( 'NONE', *, *, #36182, .T. ) ;
#1181=LINE ( 'NONE', #42793, #34588 ) ;
#1184=VECTOR ( 'NONE', #11769, 1000.000000000000000 ) ;
#1185=ORIENTED_EDGE ( 'NONE', *, *, #40362, .F. ) ;
#1194=CARTESIAN_POINT ( 'NONE',  ( 11.99999999999999822, 0.000000000000000000, 0.000000000000000000 ) ) ;
#1196=VECTOR ( 'NONE', #44535, 1000.000000000000000 ) ;
#1198=CARTESIAN_POINT ( 'NONE',  ( 0.000000000000000000, 59.03342792756328095, -46.54456581323744757 ) ) ;
#1200=CARTESIAN_POINT ( 'NONE',  ( 0.000000000000000000, 34.44570377933598593, 69.42325613327452061 ) ) ;
#1202=CIRCLE ( 'NONE', #19188, 31.99999999999998579 ) ;
#1209=ORIENTED_EDGE ( 'NONE', *, *, #5096, .T. ) ;
#1215=EDGE_CURVE ( 'NONE', #19020, #41278, #26852, .T. ) ;
#1216=CIRCLE ( 'NONE', #16076, 82.00000000000000000 ) ;
#1222=ADVANCED_FACE ( 'NONE', ( #19239 ), #15566, .T. ) ;
#1225=EDGE_CURVE ( 'NONE', #39044, #16230, #45604, .T. ) ;
#1227=DIRECTION ( 'NONE',  ( 0.000000000000000000, 0.6691306063588579045, -0.7431448254773945772 ) ) ;
#1233=EDGE_CURVE ( 'NONE', #2023, #43990, #3585, .T. ) ;
#1236=VERTEX_POINT ( 'NONE', #14851 ) ;
#1238=EDGE_CURVE ( 'NONE', #40188, #24194, #34617, .T. ) ;
#1241=DIRECTION ( 'NONE',  ( -1.000000000000000000, 0.000000000000000000, 0.000000000000000000 ) ) ;
#1243=ORIENTED_EDGE ( 'NONE', *, *, #34817, .T. ) ;
#1252=ORIENTED_EDGE ( 'NONE', *, *, #38710, .F. ) ;
#1261=CARTESIAN_POINT ( 'NONE',  ( 0.000000000000000000, 0.000000000000000000, 0.000000000000000000 ) ) ;
#1263=DIRECTION ( 'NONE',  ( 0.000000000000000000, 0.8910065241883656784, 0.4539904997395511344 ) ) ;
#1264=EDGE_CURVE ( 'NONE', #16392, #35973, #42970, .T. ) ;
#1271=DIRECTION ( 'NONE',  ( 0.000000000000000000, -0.3090169943749461745, 0.9510565162951539753 ) ) ;
#1274=AXIS2_PLACEMENT_3D ( 'NONE', #31416, #5223, #23810 ) ;
#1277=VERTEX_POINT ( 'NONE', #16782 ) ;
#1284=CARTESIAN_POINT ( 'NONE',  ( 11.99999999999999822, -44.88180994100329713, -63.18004540533077318 ) ) ;
#1287=EDGE_CURVE ( 'NONE', #4413, #25450, #37700, .T. ) ;
#1288=AXIS2_PLACEMENT_3D ( 'NONE', #684, #1171, #23680 ) ;
#1291=AXIS2_PLACEMENT_3D ( 'NONE', #24020, #34057, #4922 ) ;
#1296=AXIS2_PLACEMENT_3D ( 'NONE', #32032, #29723, #44658 ) ;
#1298=VERTEX_POINT ( 'NONE', #21338 ) ;
#1305=DIRECTION ( 'NONE',  ( 0.000000000000000000, 0.3090169943749480064, -0.9510565162951534202 ) ) ;
#1308=ORIENTED_EDGE ( 'NONE', *, *, #5264, .F. ) ;
#1311=VERTEX_POINT ( 'NONE', #25009 ) ;
#1312=CARTESIAN_POINT ( 'NONE',  ( 0.000000000000000000, 5.256550761633951296, -77.32052557432835727 ) ) ;
#1316=DIRECTION ( 'NONE',  ( -1.000000000000000000, 0.000000000000000000, 0.000000000000000000 ) ) ;
#1320=CARTESIAN_POINT ( 'NONE',  ( -10.00000000000000000, 0.000000000000000000, 0.000000000000000000 ) ) ;
#1322=DIRECTION ( 'NONE',  ( 0.000000000000000000, -0.4539904997395350916, -0.8910065241883738940 ) ) ;
#1323=VECTOR ( 'NONE', #45414, 1000.000000000000000 ) ;
#1324=CARTESIAN_POINT ( 'NONE',  ( 0.000000000000000000, -55.19960302592104284, 51.03279382321070301 ) ) ;
#1327=AXIS2_PLACEMENT_3D ( 'NONE', #22740, #4153, #19068 ) ;
#1331=ORIENTED_EDGE ( 'NONE', *, *, #47345, .T. ) ;
#1334=CIRCLE ( 'NONE', #24007, 31.99999999999998579 ) ;
#1335=ORIENTED_EDGE ( 'NONE', *, *, #38814, .F. ) ;
#1337=EDGE_CURVE ( 'NONE', #36518, #44508, #19728, .T. ) ;
#1340=AXIS2_PLACEMENT_3D ( 'NONE', #28538, #38843, #47128 ) ;
#1347=EDGE_LOOP ( 'NONE', ( #24405, #19869, #14111, #4047 ) ) ;
#1348=EDGE_LOOP ( 'NONE', ( #15991, #38347, #37593, #28798 ) ) ;
#1352=DIRECTION ( 'NONE',  ( -1.000000000000000000, 0.000000000000000000, 0.000000000000000000 ) ) ;
#1358=ORIENTED_EDGE ( 'NONE', *, *, #47675, .T. ) ;
#1365=ORIENTED_EDGE ( 'NONE', *, *, #31617, .T. ) ;
#1367=ORIENTED_EDGE ( 'NONE', *, *, #14530, .T. ) ;
#1369=DIRECTION ( 'NONE',  ( -1.000000000000000000, -0.000000000000000000, 0.000000000000000000 ) ) ;
#1374=CARTESIAN_POINT ( 'NONE',  ( 11.99999999999999822, -55.16347631942997509, -60.67117009219195722 ) ) ;
#1385=DIRECTION ( 'NONE',  ( 0.000000000000000000, 0.000000000000000000, 1.000000000000000000 ) ) ;
#1388=ADVANCED_FACE ( 'NONE', ( #23626 ), #38573, .F. ) ;
#1390=DIRECTION ( 'NONE',  ( 0.000000000000000000, 0.000000000000000000, 1.000000000000000000 ) ) ;
#1393=CARTESIAN_POINT ( 'NONE',  ( 0.000000000000000000, -20.41045688087772092, -72.35160999960838524 ) ) ;
#1397=EDGE_CURVE ( 'NONE', #5571, #4001, #1114, .T. ) ;
#1401=ADVANCED_FACE ( 'NONE', ( #33077 ), #25974, .F. ) ;
#1402=EDGE_CURVE ( 'NONE', #39822, #36554, #3210, .T. ) ;
#1403=ORIENTED_EDGE ( 'NONE', *, *, #15375, .F. ) ;
#1408=ORIENTED_EDGE ( 'NONE', *, *, #3201, .T. ) ;
#1411=DIRECTION ( 'NONE',  ( -1.000000000000000000, 0.000000000000000000, 0.000000000000000000 ) ) ;
#1413=ORIENTED_EDGE ( 'NONE', *, *, #26432, .T. ) ;
#1415=CYLINDRICAL_SURFACE ( 'NONE', #42874, 77.49899999999999523 ) ;
#1418=AXIS2_PLACEMENT_3D ( 'NONE', #30277, #10937, #45196 ) ;
#1419=LINE ( 'NONE', #8503, #29009 ) ;
#1424=DIRECTION ( 'NONE',  ( -1.000000000000000000, 0.000000000000000000, -0.000000000000000000 ) ) ;
#1428=CARTESIAN_POINT ( 'NONE',  ( -10.00000000000000000, 0.000000000000000000, 0.000000000000000000 ) ) ;
#1429=DIRECTION ( 'NONE',  ( -1.000000000000000000, -0.000000000000000000, -0.000000000000000000 ) ) ;
#1434=ADVANCED_FACE ( 'NONE', ( #44580 ), #3461, .T. ) ;
#1435=DIRECTION ( 'NONE',  ( 1.000000000000000000, 0.000000000000000000, -0.000000000000000000 ) ) ;
#1439=DIRECTION ( 'NONE',  ( 1.000000000000000000, 0.000000000000000000, -0.000000000000000000 ) ) ;
#1441=EDGE_CURVE ( 'NONE', #44170, #42578, #43955, .T. ) ;
#1450=DIRECTION ( 'NONE',  ( 0.000000000000000000, 0.7604059656000322631, -0.6494480483301821039 ) ) ;
#1457=ORIENTED_EDGE ( 'NONE', *, *, #5577, .T. ) ;
#1460=AXIS2_PLACEMENT_3D ( 'NONE', #27869, #27135, #4849 ) ;
#1469=VERTEX_POINT ( 'NONE', #21595 ) ;
#1470=VERTEX_POINT ( 'NONE', #33793 ) ;
#1474=VERTEX_POINT ( 'NONE', #33330 ) ;
#1476=CARTESIAN_POINT ( 'NONE',  ( 11.99999999999999822, -46.11716303203233736, 67.80270845531873647 ) ) ;
#1480=CARTESIAN_POINT ( 'NONE',  ( 0.000000000000000000, 75.16055320797030959, 18.89407956138283851 ) ) ;
#1482=FACE_OUTER_BOUND ( 'NONE', #12691, .T. ) ;
#1483=ORIENTED_EDGE ( 'NONE', *, *, #6543, .F. ) ;
#1484=CARTESIAN_POINT ( 'NONE',  ( 11.99999999999999822, 0.000000000000000000, 0.000000000000000000 ) ) ;
#1488=VERTEX_POINT ( 'NONE', #48258 ) ;
#1490=ORIENTED_EDGE ( 'NONE', *, *, #34399, .T. ) ;
#1491=CARTESIAN_POINT ( 'NONE',  ( -10.00000000000000000, 0.000000000000000000, 0.000000000000000000 ) ) ;
#1492=DIRECTION ( 'NONE',  ( -1.000000000000000000, -0.000000000000000000, -0.000000000000000000 ) ) ;
#1501=EDGE_CURVE ( 'NONE', #36444, #36385, #34584, .T. ) ;
#1506=DIRECTION ( 'NONE',  ( -1.000000000000000000, 0.000000000000000000, 0.000000000000000000 ) ) ;
#1508=CARTESIAN_POINT ( 'NONE',  ( 15.00000000000000000, 16.83928648764922542, -16.46020748918050458 ) ) ;
#1515=ORIENTED_EDGE ( 'NONE', *, *, #41664, .F. ) ;
#1516=CARTESIAN_POINT ( 'NONE',  ( -10.00000000000000000, 0.000000000000000000, 0.000000000000000000 ) ) ;
#1523=AXIS2_PLACEMENT_3D ( 'NONE', #5903, #35506, #46780 ) ;
#1524=CIRCLE ( 'NONE', #7768, 77.49899999999999523 ) ;
#1525=DIRECTION ( 'NONE',  ( -1.000000000000000000, 0.000000000000000000, 0.000000000000000000 ) ) ;
#1527=ORIENTED_EDGE ( 'NONE', *, *, #6422, .T. ) ;
#1532=AXIS2_PLACEMENT_3D ( 'NONE', #14785, #17293, #3517 ) ;
#1533=CARTESIAN_POINT ( 'NONE',  ( 11.99999999999999822, -75.54627589209955829, 17.28742895386058009 ) ) ;
#1534=VERTEX_POINT ( 'NONE', #45540 ) ;
#1536=EDGE_LOOP ( 'NONE', ( #37594, #47216, #37658, #17831 ) ) ;
#1539=CARTESIAN_POINT ( 'NONE',  ( 11.99999999999999822, -68.26794271651239399, -31.47745569255214093 ) ) ;
#1543=CARTESIAN_POINT ( 'NONE',  ( 11.99999999999999822, -59.03342792756231461, -46.54456581323868392 ) ) ;
#1548=EDGE_CURVE ( 'NONE', #1534, #18192, #5173, .T. ) ;
#1550=EDGE_LOOP ( 'NONE', ( #26578, #45657, #31473, #2667 ) ) ;
#1553=CARTESIAN_POINT ( 'NONE',  ( 11.99999999999999822, 0.000000000000000000, 0.000000000000000000 ) ) ;
#1556=DIRECTION ( 'NONE',  ( 0.000000000000000000, 0.000000000000000000, 1.000000000000000000 ) ) ;
#1559=DIRECTION ( 'NONE',  ( 1.000000000000000000, 0.000000000000000000, 0.000000000000000000 ) ) ;
#1561=CARTESIAN_POINT ( 'NONE',  ( 11.99999999999999822, 62.50329211542435104, 41.76937507738811917 ) ) ;
#1564=DIRECTION ( 'NONE',  ( -1.000000000000000000, 0.000000000000000000, 0.000000000000000000 ) ) ;
#1565=CARTESIAN_POINT ( 'NONE',  ( 11.99999999999999822, 55.16347631943131091, -60.67117009219074930 ) ) ;
#1566=ADVANCED_FACE ( 'NONE', ( #42125 ), #20087, .T. ) ;
#1568=CIRCLE ( 'NONE', #21072, 31.99999999999999289 ) ;
#1571=ORIENTED_EDGE ( 'NONE', *, *, #40112, .F. ) ;
#1572=ORIENTED_EDGE ( 'NONE', *, *, #1287, .T. ) ;
#1574=AXIS2_PLACEMENT_3D ( 'NONE', #29415, #29645, #40915 ) ;
#1580=CARTESIAN_POINT ( 'NONE',  ( 0.000000000000000000, 0.000000000000000000, 0.000000000000000000 ) ) ;
#1582=VERTEX_POINT ( 'NONE', #19115 ) ;
#1584=ORIENTED_EDGE ( 'NONE', *, *, #39871, .T. ) ;
#1585=AXIS2_PLACEMENT_3D ( 'NONE', #24108, #20417, #5273 ) ;
#1586=PLANE ( 'NONE',  #32321 ) ;
#1598=CARTESIAN_POINT ( 'NONE',  ( 0.000000000000000000, 67.80270845531887858, 46.11716303203210288 ) ) ;
#1606=CARTESIAN_POINT ( 'NONE',  ( 0.000000000000000000, -21.60688246758642705, 79.10210256391358996 ) ) ;
#1612=DIRECTION ( 'NONE',  ( -1.000000000000000000, -0.000000000000000000, -0.000000000000000000 ) ) ;
#1616=DIRECTION ( 'NONE',  ( -1.000000000000000000, 0.000000000000000000, -0.000000000000000000 ) ) ;
#1622=CARTESIAN_POINT ( 'NONE',  ( 11.99999999999999822, 24.73286445877808148, -73.44644590900034586 ) ) ;
#1624=DIRECTION ( 'NONE',  ( 0.000000000000000000, 0.000000000000000000, 1.000000000000000000 ) ) ;
#1625=CIRCLE ( 'NONE', #10207, 31.99999999999998579 ) ;
#1628=VECTOR ( 'NONE', #43967, 1000.000000000000000 ) ;
#1631=AXIS2_PLACEMENT_3D ( 'NONE', #31183, #2047, #31675 ) ;
#1634=CARTESIAN_POINT ( 'NONE',  ( 15.00000000000000000, -26.23277895567245466, 4.042438405570107918 ) ) ;
#1637=CIRCLE ( 'NONE', #28223, 77.49899999999998101 ) ;
#1644=EDGE_CURVE ( 'NONE', #4498, #6663, #15876, .T. ) ;
#1649=CARTESIAN_POINT ( 'NONE',  ( 0.000000000000000000, -62.50884508063453637, 41.76106447765467777 ) ) ;
#1651=VECTOR ( 'NONE', #29901, 1000.000000000000000 ) ;
#1652=FACE_OUTER_BOUND ( 'NONE', #20298, .T. ) ;
#1657=ORIENTED_EDGE ( 'NONE', *, *, #34367, .T. ) ;
#1660=VECTOR ( 'NONE', #41275, 1000.000000000000000 ) ;
#1662=ORIENTED_EDGE ( 'NONE', *, *, #13722, .T. ) ;
#1663=DIRECTION ( 'NONE',  ( 0.000000000000000000, 0.000000000000000000, 1.000000000000000000 ) ) ;
#1666=DIRECTION ( 'NONE',  ( -1.000000000000000000, 0.000000000000000000, 0.000000000000000000 ) ) ;
#1672=CIRCLE ( 'NONE', #25867, 82.00000000000000000 ) ;
#1676=AXIS2_PLACEMENT_3D ( 'NONE', #45673, #4560, #7516 ) ;
#1677=CARTESIAN_POINT ( 'NONE',  ( 0.000000000000000000, 39.78640506895604290, 66.50666863322015843 ) ) ;
#1679=ORIENTED_EDGE ( 'NONE', *, *, #45056, .T. ) ;
#1683=ADVANCED_FACE ( 'NONE', ( #6128 ), #28642, .F. ) ;
#1684=VERTEX_POINT ( 'NONE', #2434 ) ;
#1688=CIRCLE ( 'NONE', #18076, 31.99999999999998934 ) ;
#1693=LINE ( 'NONE', #24202, #22926 ) ;
#1695=ORIENTED_EDGE ( 'NONE', *, *, #7105, .F. ) ;
#1696=VECTOR ( 'NONE', #7755, 1000.000000000000000 ) ;
#1697=AXIS2_PLACEMENT_3D ( 'NONE', #19227, #34623, #41753 ) ;
#1702=AXIS2_PLACEMENT_3D ( 'NONE', #33685, #3339, #4084 ) ;
#1718=DIRECTION ( 'NONE',  ( -1.000000000000000000, 0.000000000000000000, -0.000000000000000000 ) ) ;
#1726=DIRECTION ( 'NONE',  ( -1.000000000000000000, 0.000000000000000000, 0.000000000000000000 ) ) ;
#1732=CARTESIAN_POINT ( 'NONE',  ( 11.99999999999999822, -55.38113227695745167, -54.21277698773732823 ) ) ;
#1733=AXIS2_PLACEMENT_3D ( 'NONE', #14357, #44219, #25602 ) ;
#1736=LINE ( 'NONE', #16663, #47197 ) ;
#1737=CARTESIAN_POINT ( 'NONE',  ( 11.99999999999999822, 0.000000000000000000, 0.000000000000000000 ) ) ;
#1745=DIRECTION ( 'NONE',  ( 0.000000000000000000, -0.8910065241883626808, -0.4539904997395568520 ) ) ;
#1746=VECTOR ( 'NONE', #40375, 1000.000000000000000 ) ;
#1750=CARTESIAN_POINT ( 'NONE',  ( 11.99999999999999822, -76.66974797899844418, 11.30684508768314522 ) ) ;
#1751=VERTEX_POINT ( 'NONE', #31607 ) ;
#1752=ORIENTED_EDGE ( 'NONE', *, *, #5598, .F. ) ;
#1756=ORIENTED_EDGE ( 'NONE', *, *, #43410, .T. ) ;
#1762=ORIENTED_EDGE ( 'NONE', *, *, #41288, .F. ) ;
#1767=EDGE_CURVE ( 'NONE', #29872, #44170, #46774, .T. ) ;
#1769=DIRECTION ( 'NONE',  ( -1.000000000000000000, -0.000000000000000000, -0.000000000000000000 ) ) ;
#1773=VECTOR ( 'NONE', #23912, 1000.000000000000000 ) ;
#1777=CARTESIAN_POINT ( 'NONE',  ( 0.000000000000000000, -65.59268652807237743, 36.72794159290217664 ) ) ;
#1787=CARTESIAN_POINT ( 'NONE',  ( 0.000000000000000000, 80.28980883073781172, -16.65972982744850128 ) ) ;
#1788=AXIS2_PLACEMENT_3D ( 'NONE', #48428, #29831, #36457 ) ;
#1789=CARTESIAN_POINT ( 'NONE',  ( 11.99999999999999822, 74.65374052328660071, -8.840884882374309583 ) ) ;
#1798=DIRECTION ( 'NONE',  ( 0.000000000000000000, 0.000000000000000000, -1.000000000000000000 ) ) ;
#1799=EDGE_CURVE ( 'NONE', #45678, #897, #16417, .T. ) ;
#1800=CARTESIAN_POINT ( 'NONE',  ( 0.000000000000000000, 30.41916302227216562, -71.27951684757994144 ) ) ;
#1808=CARTESIAN_POINT ( 'NONE',  ( 0.000000000000000000, 0.000000000000000000, 0.000000000000000000 ) ) ;
#1810=ORIENTED_EDGE ( 'NONE', *, *, #23986, .F. ) ;
#1813=AXIS2_PLACEMENT_3D ( 'NONE', #37062, #30219, #37788 ) ;
#1816=CARTESIAN_POINT ( 'NONE',  ( 6.000000000000000000, -81.34940948281328588, -10.30890764327469000 ) ) ;
#1817=VERTEX_POINT ( 'NONE', #9078 ) ;
#1819=EDGE_CURVE ( 'NONE', #30895, #38290, #37737, .T. ) ;
#1826=CIRCLE ( 'NONE', #29174, 21.00000000000000000 ) ;
#1830=EDGE_CURVE ( 'NONE', #25492, #2837, #21300, .T. ) ;
#1831=LINE ( 'NONE', #35347, #4699 ) ;
#1833=VECTOR ( 'NONE', #41395, 1000.000000000000000 ) ;
#1836=DIRECTION ( 'NONE',  ( 0.000000000000000000, 0.8660254037844432595, 0.4999999999999919509 ) ) ;
#1837=ORIENTED_EDGE ( 'NONE', *, *, #62, .T. ) ;
#1838=AXIS2_PLACEMENT_3D ( 'NONE', #30287, #25863, #18035 ) ;
#1839=VERTEX_POINT ( 'NONE', #13944 ) ;
#1840=CARTESIAN_POINT ( 'NONE',  ( 15.00000000000000000, -19.89357724624986545, 12.59942793731086219 ) ) ;
#1841=DIRECTION ( 'NONE',  ( -1.000000000000000000, 0.000000000000000000, 0.000000000000000000 ) ) ;
#1843=EDGE_LOOP ( 'NONE', ( #25317, #43109, #16471, #20186 ) ) ;
#1850=AXIS2_PLACEMENT_3D ( 'NONE', #5902, #43341, #47005 ) ;
#1856=CARTESIAN_POINT ( 'NONE',  ( 11.99999999999999822, -21.60688246758531150, -79.10210256391390260 ) ) ;
#1858=LINE ( 'NONE', #35625, #14279 ) ;
#1862=CARTESIAN_POINT ( 'NONE',  ( 11.99999999999999822, 21.60688246758586573, 79.10210256391376049 ) ) ;
#1867=DIRECTION ( 'NONE',  ( -1.000000000000000000, 0.000000000000000000, 0.000000000000000000 ) ) ;
#1869=CARTESIAN_POINT ( 'NONE',  ( 11.99999999999999822, 8.840884882376133902, -74.65374052328640175 ) ) ;
#1873=EDGE_CURVE ( 'NONE', #20499, #29866, #31502, .T. ) ;
#1877=ORIENTED_EDGE ( 'NONE', *, *, #40436, .T. ) ;
#1882=ORIENTED_EDGE ( 'NONE', *, *, #31239, .T. ) ;
#1884=LINE ( 'NONE', #40044, #20526 ) ;
#1890=VECTOR ( 'NONE', #41590, 1000.000000000000000 ) ;
#1891=ADVANCED_FACE ( 'NONE', ( #7074 ), #33502, .T. ) ;
#1895=CARTESIAN_POINT ( 'NONE',  ( 0.000000000000000000, -34.94270380257585629, -74.18225833017926618 ) ) ;
#1896=ADVANCED_FACE ( 'NONE', ( #40607 ), #3651, .T. ) ;
#1902=DIRECTION ( 'NONE',  ( -1.000000000000000000, -0.000000000000000000, -0.000000000000000000 ) ) ;
#1907=ORIENTED_EDGE ( 'NONE', *, *, #20842, .F. ) ;
#1914=VERTEX_POINT ( 'NONE', #44043 ) ;
#1917=DIRECTION ( 'NONE',  ( -1.000000000000000000, 0.000000000000000000, 0.000000000000000000 ) ) ;
#1921=CARTESIAN_POINT ( 'NONE',  ( 0.000000000000000000, -60.67117009219175827, 55.16347631943019536 ) ) ;
#1924=CARTESIAN_POINT ( 'NONE',  ( 5.999999999999999112, -74.74816331893404708, -33.71516098798818462 ) ) ;
#1928=EDGE_LOOP ( 'NONE', ( #23263, #17480, #3567, #17108 ) ) ;
#1929=VECTOR ( 'NONE', #19712, 1000.000000000000000 ) ;
#1934=DIRECTION ( 'NONE',  ( -1.000000000000000000, -0.000000000000000000, 0.000000000000000000 ) ) ;
#1936=LINE ( 'NONE', #5848, #22129 ) ;
#1940=LINE ( 'NONE', #46483, #2114 ) ;
#1944=CARTESIAN_POINT ( 'NONE',  ( 15.00000000000000000, 20.85821328998741109, -10.92862929874522671 ) ) ;
#1953=DIRECTION ( 'NONE',  ( -1.000000000000000000, 0.000000000000000000, 0.000000000000000000 ) ) ;
#1960=DIRECTION ( 'NONE',  ( -1.000000000000000000, 0.000000000000000000, 0.000000000000000000 ) ) ;
#1968=LINE ( 'NONE', #24219, #46948 ) ;
#1969=ORIENTED_EDGE ( 'NONE', *, *, #8697, .F. ) ;
#1970=DIRECTION ( 'NONE',  ( -1.000000000000000000, -0.000000000000000000, -0.000000000000000000 ) ) ;
#1973=EDGE_CURVE ( 'NONE', #39311, #37697, #47850, .T. ) ;
#1974=CARTESIAN_POINT ( 'NONE',  ( 11.99999999999999822, 0.000000000000000000, 0.000000000000000000 ) ) ;
#1977=CARTESIAN_POINT ( 'NONE',  ( 11.99999999999999822, 81.50828551894241514, -8.966570791699814080 ) ) ;
#1978=EDGE_LOOP ( 'NONE', ( #2482, #32004, #25639, #44345 ) ) ;
#1980=VECTOR ( 'NONE', #28472, 1000.000000000000000 ) ;
#1982=DIRECTION ( 'NONE',  ( 0.000000000000000000, 0.000000000000000000, 1.000000000000000000 ) ) ;
#1986=AXIS2_PLACEMENT_3D ( 'NONE', #35367, #35122, #42732 ) ;
#1987=CARTESIAN_POINT ( 'NONE',  ( 5.999999999999999112, -33.71516098798685590, -74.74816331893465815 ) ) ;
#1991=CARTESIAN_POINT ( 'NONE',  ( 11.99999999999999822, 59.46389618802034960, -49.70050353004825894 ) ) ;
#2001=VECTOR ( 'NONE', #38334, 1000.000000000000000 ) ;
#2003=CARTESIAN_POINT ( 'NONE',  ( 11.99999999999999822, -65.58780272294048075, -36.73666225445966660 ) ) ;
#2008=ORIENTED_EDGE ( 'NONE', *, *, #18559, .F. ) ;
#2009=ORIENTED_EDGE ( 'NONE', *, *, #27242, .F. ) ;
#2014=DIRECTION ( 'NONE',  ( 0.000000000000000000, 0.000000000000000000, -1.000000000000000000 ) ) ;
#2018=AXIS2_PLACEMENT_3D ( 'NONE', #12822, #43161, #20387 ) ;
#2019=ORIENTED_EDGE ( 'NONE', *, *, #40436, .F. ) ;
#2022=DIRECTION ( 'NONE',  ( 0.000000000000000000, 0.8526401643540897357, 0.5224985647159527957 ) ) ;
#2023=VERTEX_POINT ( 'NONE', #37663 ) ;
#2024=DIRECTION ( 'NONE',  ( 1.000000000000000000, 0.000000000000000000, 0.000000000000000000 ) ) ;
#2027=CARTESIAN_POINT ( 'NONE',  ( 11.99999999999999822, 0.000000000000000000, 0.000000000000000000 ) ) ;
#2031=VERTEX_POINT ( 'NONE', #30821 ) ;
#2032=ORIENTED_EDGE ( 'NONE', *, *, #9725, .T. ) ;
#2033=AXIS2_PLACEMENT_3D ( 'NONE', #43690, #3045, #14072 ) ;
#2035=AXIS2_PLACEMENT_3D ( 'NONE', #17180, #16719, #6424 ) ;
#2039=ORIENTED_EDGE ( 'NONE', *, *, #21155, .F. ) ;
#2041=DIRECTION ( 'NONE',  ( 0.000000000000000000, -0.7431448254773862505, 0.6691306063588671194 ) ) ;
#2045=AXIS2_PLACEMENT_3D ( 'NONE', #19784, #8532, #23462 ) ;
#2046=FACE_OUTER_BOUND ( 'NONE', #41884, .T. ) ;
#2047=DIRECTION ( 'NONE',  ( -1.000000000000000000, 0.000000000000000000, 0.000000000000000000 ) ) ;
#2050=CIRCLE ( 'NONE', #16130, 82.00000000000000000 ) ;
#2056=CARTESIAN_POINT ( 'NONE',  ( 11.99999999999999822, 77.49459641780886443, 0.8261519478433866359 ) ) ;
#2061=CARTESIAN_POINT ( 'NONE',  ( 6.000000000000000000, 44.99326035066052043, 68.55367621811159040 ) ) ;
#2068=AXIS2_PLACEMENT_3D ( 'NONE', #1561, #16489, #31682 ) ;
#2071=ADVANCED_FACE ( 'NONE', ( #19298 ), #30563, .F. ) ;
#2072=EDGE_CURVE ( 'NONE', #31321, #23779, #959, .T. ) ;
#2073=CYLINDRICAL_SURFACE ( 'NONE', #15126, 77.49899999999999523 ) ;
#2077=ORIENTED_EDGE ( 'NONE', *, *, #40519, .F. ) ;
#2080=CARTESIAN_POINT ( 'NONE',  ( 15.00000000000000000, -14.54903810567644484, 22.19967320028775504 ) ) ;
#2082=VERTEX_POINT ( 'NONE', #28589 ) ;
#2085=LINE ( 'NONE', #35354, #31942 ) ;
#2087=DIRECTION ( 'NONE',  ( 0.000000000000000000, 0.000000000000000000, 1.000000000000000000 ) ) ;
#2091=ORIENTED_EDGE ( 'NONE', *, *, #42948, .T. ) ;
#2093=VERTEX_POINT ( 'NONE', #13411 ) ;
#2097=CARTESIAN_POINT ( 'NONE',  ( 15.00000000000000000, -22.32062822937489344, -14.36278369418800160 ) ) ;
#2098=LINE ( 'NONE', #6019, #1048 ) ;
#2108=LINE ( 'NONE', #34649, #27543 ) ;
#2110=AXIS2_PLACEMENT_3D ( 'NONE', #11919, #4574, #19255 ) ;
#2111=ADVANCED_FACE ( 'NONE', ( #9021 ), #46224, .T. ) ;
#2114=VECTOR ( 'NONE', #9265, 1000.000000000000000 ) ;
#2115=CARTESIAN_POINT ( 'NONE',  ( 0.000000000000000000, -46.53671651293907274, -59.03961581697448935 ) ) ;
#2117=ORIENTED_EDGE ( 'NONE', *, *, #18529, .T. ) ;
#2118=EDGE_CURVE ( 'NONE', #25700, #6361, #23957, .T. ) ;
#2119=CARTESIAN_POINT ( 'NONE',  ( 12.00000000000000000, -0.9646360437375370855, -23.52805723605590060 ) ) ;
#2122=ORIENTED_EDGE ( 'NONE', *, *, #13428, .T. ) ;
#2125=EDGE_CURVE ( 'NONE', #5981, #2920, #28332, .T. ) ;
#2130=DIRECTION ( 'NONE',  ( 0.000000000000000000, 0.9135454576426058626, 0.4067366430757889950 ) ) ;
#2132=ORIENTED_EDGE ( 'NONE', *, *, #6063, .T. ) ;
#2133=EDGE_CURVE ( 'NONE', #2398, #10384, #20991, .T. ) ;
#2134=AXIS2_PLACEMENT_3D ( 'NONE', #6917, #39980, #24801 ) ;
#2138=ORIENTED_EDGE ( 'NONE', *, *, #47345, .F. ) ;
#2139=ORIENTED_EDGE ( 'NONE', *, *, #37424, .T. ) ;
#2142=EDGE_LOOP ( 'NONE', ( #41342, #41173, #35536, #577 ) ) ;
#2143=VECTOR ( 'NONE', #6266, 1000.000000000000000 ) ;
#2145=DIRECTION ( 'NONE',  ( -1.000000000000000000, -0.000000000000000000, -0.000000000000000000 ) ) ;
#2148=DIRECTION ( 'NONE',  ( -1.000000000000000000, 0.000000000000000000, 0.000000000000000000 ) ) ;
#2149=VERTEX_POINT ( 'NONE', #47178 ) ;
#2156=CARTESIAN_POINT ( 'NONE',  ( 11.99999999999999822, 0.000000000000000000, 0.000000000000000000 ) ) ;
#2161=VERTEX_POINT ( 'NONE', #13656 ) ;
#2164=EDGE_CURVE ( 'NONE', #27718, #6779, #24673, .T. ) ;
#2167=CARTESIAN_POINT ( 'NONE',  ( 11.99999999999999822, 0.000000000000000000, 0.000000000000000000 ) ) ;
#2169=DIRECTION ( 'NONE',  ( -0.000000000000000000, -2.312964634635746211E-15, 1.000000000000000000 ) ) ;
#2176=ORIENTED_EDGE ( 'NONE', *, *, #18779, .T. ) ;
#2177=VERTEX_POINT ( 'NONE', #5589 ) ;
#2180=CARTESIAN_POINT ( 'NONE',  ( 0.000000000000000000, -67.80270845531855173, -46.11716303203260736 ) ) ;
#2197=CARTESIAN_POINT ( 'NONE',  ( 11.99999999999999822, -50.23322058963300663, -64.81221759200398935 ) ) ;
#2200=VERTEX_POINT ( 'NONE', #1677 ) ;
#2201=CARTESIAN_POINT ( 'NONE',  ( 11.99999999999999822, -26.01480285779785362, -70.53064760720343429 ) ) ;
#2204=DIRECTION ( 'NONE',  ( 0.000000000000000000, -0.5877852522924689183, 0.8090169943749504489 ) ) ;
#2206=ORIENTED_EDGE ( 'NONE', *, *, #36006, .F. ) ;
#2207=ORIENTED_EDGE ( 'NONE', *, *, #11104, .F. ) ;
#2217=DIRECTION ( 'NONE',  ( -1.000000000000000000, 0.000000000000000000, -0.000000000000000000 ) ) ;
#2226=CARTESIAN_POINT ( 'NONE',  ( 0.000000000000000000, 74.65491531819105830, 8.830959090343693418 ) ) ;
#2230=EDGE_CURVE ( 'NONE', #20992, #23445, #26478, .T. ) ;
#2231=DIRECTION ( 'NONE',  ( -1.000000000000000000, 0.000000000000000000, -0.000000000000000000 ) ) ;
#2238=DIRECTION ( 'NONE',  ( 0.000000000000000000, 1.000000000000000000, 3.491481338843133355E-15 ) ) ;
#2242=EDGE_LOOP ( 'NONE', ( #20469, #42787, #38973, #38945 ) ) ;
#2244=ORIENTED_EDGE ( 'NONE', *, *, #43733, .F. ) ;
#2246=EDGE_LOOP ( 'NONE', ( #47863, #36567, #44691, #17829 ) ) ;
#2248=AXIS2_PLACEMENT_3D ( 'NONE', #29311, #40801, #25137 ) ;
#2250=DIRECTION ( 'NONE',  ( 0.000000000000000000, 0.000000000000000000, 1.000000000000000000 ) ) ;
#2258=ORIENTED_EDGE ( 'NONE', *, *, #39282, .T. ) ;
#2262=DIRECTION ( 'NONE',  ( 0.000000000000000000, 0.000000000000000000, 1.000000000000000000 ) ) ;
#2264=ORIENTED_EDGE ( 'NONE', *, *, #13477, .T. ) ;
#2266=PRODUCT_DEFINITION_SHAPE ( 'NONE', 'NONE',  #10069 ) ;
#2269=ADVANCED_FACE ( 'NONE', ( #6312 ), #43989, .T. ) ;
#2280=DIRECTION ( 'NONE',  ( -0.000000000000000000, -0.3090169943749572767, -0.9510565162951503115 ) ) ;
#2281=DIRECTION ( 'NONE',  ( -1.000000000000000000, 0.000000000000000000, 0.000000000000000000 ) ) ;
#2282=ORIENTED_EDGE ( 'NONE', *, *, #36480, .F. ) ;
#2288=EDGE_CURVE ( 'NONE', #27398, #10618, #27243, .T. ) ;
#2290=VERTEX_POINT ( 'NONE', #36874 ) ;
#2292=DIRECTION ( 'NONE',  ( -1.000000000000000000, 0.000000000000000000, 0.000000000000000000 ) ) ;
#2293=ORIENTED_EDGE ( 'NONE', *, *, #24648, .F. ) ;
#2297=EDGE_CURVE ( 'NONE', #28640, #13942, #29779, .T. ) ;
#2304=VERTEX_POINT ( 'NONE', #14378 ) ;
#2305=DIRECTION ( 'NONE',  ( -1.000000000000000000, -0.000000000000000000, -0.000000000000000000 ) ) ;
#2306=EDGE_CURVE ( 'NONE', #18510, #27706, #10044, .T. ) ;
#2307=EDGE_LOOP ( 'NONE', ( #44490, #15744, #34396, #3995 ) ) ;
#2308=EDGE_LOOP ( 'NONE', ( #5853, #44401, #47795, #2658 ) ) ;
#2309=DIRECTION ( 'NONE',  ( -1.000000000000000000, -0.000000000000000000, -0.000000000000000000 ) ) ;
#2313=ORIENTED_EDGE ( 'NONE', *, *, #46643, .T. ) ;
#2314=CARTESIAN_POINT ( 'NONE',  ( 0.000000000000000000, -51.03279382321048985, -55.19960302592120627 ) ) ;
#2315=ORIENTED_EDGE ( 'NONE', *, *, #38930, .T. ) ;
#2320=DIRECTION ( 'NONE',  ( -1.000000000000000000, 0.000000000000000000, 0.000000000000000000 ) ) ;
#2324=EDGE_CURVE ( 'NONE', #8879, #35187, #37372, .T. ) ;
#2325=CYLINDRICAL_SURFACE ( 'NONE', #3932, 31.99999999999998579 ) ;
#2327=LINE ( 'NONE', #13354, #3287 ) ;
#2330=AXIS2_PLACEMENT_3D ( 'NONE', #6415, #14236, #21331 ) ;
#2331=DIRECTION ( 'NONE',  ( -1.000000000000000000, 0.000000000000000000, -0.000000000000000000 ) ) ;
#2338=CARTESIAN_POINT ( 'NONE',  ( 15.00000000000000000, -13.04903810567646971, 19.60159698893442481 ) ) ;
#2341=ORIENTED_EDGE ( 'NONE', *, *, #2355, .T. ) ;
#2342=FACE_OUTER_BOUND ( 'NONE', #17769, .T. ) ;
#2351=AXIS2_PLACEMENT_3D ( 'NONE', #28384, #6124, #24724 ) ;
#2352=FACE_OUTER_BOUND ( 'NONE', #44491, .T. ) ;
#2355=EDGE_CURVE ( 'NONE', #14655, #4757, #32743, .T. ) ;
#2357=ORIENTED_EDGE ( 'NONE', *, *, #2930, .T. ) ;
#2359=EDGE_CURVE ( 'NONE', #32670, #21593, #17889, .T. ) ;
#2364=ORIENTED_EDGE ( 'NONE', *, *, #18495, .F. ) ;
#2366=EDGE_LOOP ( 'NONE', ( #3065, #34999, #25909, #24829 ) ) ;
#2368=LINE ( 'NONE', #43975, #11627 ) ;
#2370=CARTESIAN_POINT ( 'NONE',  ( 0.000000000000000000, -75.11764819372145041, 29.05362095685286050 ) ) ;
#2371=FACE_OUTER_BOUND ( 'NONE', #22591, .T. ) ;
#2374=DIRECTION ( 'NONE',  ( -1.000000000000000000, 0.000000000000000000, -0.000000000000000000 ) ) ;
#2380=DIRECTION ( 'NONE',  ( -1.000000000000000000, 0.000000000000000000, -0.000000000000000000 ) ) ;
#2381=ORIENTED_EDGE ( 'NONE', *, *, #17686, .T. ) ;
#2386=DIRECTION ( 'NONE',  ( 0.000000000000000000, -1.000000000000000000, -1.040834085586084730E-14 ) ) ;
#2387=ORIENTED_EDGE ( 'NONE', *, *, #14321, .F. ) ;
#2388=DIRECTION ( 'NONE',  ( 0.000000000000000000, -0.8910065241883626808, -0.4539904997395569075 ) ) ;
#2390=EDGE_CURVE ( 'NONE', #40544, #30527, #3829, .T. ) ;
#2398=VERTEX_POINT ( 'NONE', #22677 ) ;
#2399=ORIENTED_EDGE ( 'NONE', *, *, #18220, .T. ) ;
#2407=VECTOR ( 'NONE', #1316, 1000.000000000000000 ) ;
#2410=VERTEX_POINT ( 'NONE', #12172 ) ;
#2412=ORIENTED_EDGE ( 'NONE', *, *, #34145, .F. ) ;
#2413=ADVANCED_FACE ( 'NONE', ( #41775 ), #411, .F. ) ;
#2421=DIRECTION ( 'NONE',  ( 0.000000000000000000, 0.07845909572784530439, -0.9969173337331279638 ) ) ;
#2425=CARTESIAN_POINT ( 'NONE',  ( 0.000000000000000000, -73.44644590900043113, -24.73286445877782924 ) ) ;
#2427=DIRECTION ( 'NONE',  ( 0.000000000000000000, 0.000000000000000000, -1.000000000000000000 ) ) ;
#2428=ORIENTED_EDGE ( 'NONE', *, *, #17993, .F. ) ;
#2434=CARTESIAN_POINT ( 'NONE',  ( 11.99999999999999822, -71.91182617369207719, 28.89263327155721228 ) ) ;
#2439=LINE ( 'NONE', #17138, #19019 ) ;
#2440=VERTEX_POINT ( 'NONE', #38587 ) ;
#2443=DIRECTION ( 'NONE',  ( 0.000000000000000000, -0.8090169943749402348, -0.5877852522924830181 ) ) ;
#2448=DIRECTION ( 'NONE',  ( 0.000000000000000000, 0.7071067811865436870, 0.7071067811865513475 ) ) ;
#2450=AXIS2_PLACEMENT_3D ( 'NONE', #30011, #22429, #7501 ) ;
#2452=DIRECTION ( 'NONE',  ( -1.000000000000000000, 0.000000000000000000, 0.000000000000000000 ) ) ;
#2453=EDGE_CURVE ( 'NONE', #13341, #27075, #29400, .T. ) ;
#2463=DIRECTION ( 'NONE',  ( 0.000000000000000000, -0.9723699203976740035, -0.2334453638559160216 ) ) ;
#2464=ORIENTED_EDGE ( 'NONE', *, *, #25636, .F. ) ;
#2468=ORIENTED_EDGE ( 'NONE', *, *, #48139, .T. ) ;
#2470=ORIENTED_EDGE ( 'NONE', *, *, #12597, .T. ) ;
#2474=ORIENTED_EDGE ( 'NONE', *, *, #22154, .F. ) ;
#2482=ORIENTED_EDGE ( 'NONE', *, *, #21255, .F. ) ;
#2486=DIRECTION ( 'NONE',  ( 0.000000000000000000, -0.5224985647159560154, 0.8526401643540879594 ) ) ;
#2491=ORIENTED_EDGE ( 'NONE', *, *, #25375, .F. ) ;
#2492=CARTESIAN_POINT ( 'NONE',  ( 15.00000000000000000, 0.000000000000000000, 0.000000000000000000 ) ) ;
#2494=ORIENTED_EDGE ( 'NONE', *, *, #6929, .F. ) ;
#2502=DIRECTION ( 'NONE',  ( 0.000000000000000000, 0.000000000000000000, -1.000000000000000000 ) ) ;
#2506=DIRECTION ( 'NONE',  ( 0.000000000000000000, -0.7431448254773878048, 0.6691306063588654540 ) ) ;
#2512=VECTOR ( 'NONE', #14808, 1000.000000000000000 ) ;
#2513=EDGE_LOOP ( 'NONE', ( #8170, #45977, #18123, #18074 ) ) ;
#2519=CIRCLE ( 'NONE', #5680, 77.49900000000000944 ) ;
#2522=DIRECTION ( 'NONE',  ( 1.000000000000000000, 0.000000000000000000, 0.000000000000000000 ) ) ;
#2524=ADVANCED_FACE ( 'NONE', ( #24363 ), #35863, .T. ) ;
#2531=DIRECTION ( 'NONE',  ( -1.000000000000000000, -0.000000000000000000, -0.000000000000000000 ) ) ;
#2533=ORIENTED_EDGE ( 'NONE', *, *, #39317, .F. ) ;
#2535=EDGE_CURVE ( 'NONE', #1277, #21018, #31769, .T. ) ;
#2537=ORIENTED_EDGE ( 'NONE', *, *, #3962, .F. ) ;
#2543=AXIS2_PLACEMENT_3D ( 'NONE', #46396, #34889, #31002 ) ;
#2544=ORIENTED_EDGE ( 'NONE', *, *, #3300, .T. ) ;
#2549=CARTESIAN_POINT ( 'NONE',  ( 11.99999999999999822, -44.99326035066006568, -68.55367621811190304 ) ) ;
#2550=ADVANCED_FACE ( 'NONE', ( #38839 ), #46660, .T. ) ;
#2554=DIRECTION ( 'NONE',  ( 0.000000000000000000, 0.6691306063588670083, 0.7431448254773863615 ) ) ;
#2557=CARTESIAN_POINT ( 'NONE',  ( 11.99999999999999822, 41.76106447765489094, 62.50884508063442269 ) ) ;
#2563=ORIENTED_EDGE ( 'NONE', *, *, #27214, .T. ) ;
#2568=ADVANCED_FACE ( 'NONE', ( #17497 ), #17250, .T. ) ;
#2569=DIRECTION ( 'NONE',  ( -1.000000000000000000, -0.000000000000000000, -0.000000000000000000 ) ) ;
#2572=CARTESIAN_POINT ( 'NONE',  ( 5.999999999999999112, -63.97538442413463855, 51.29473840253199057 ) ) ;
#2577=CARTESIAN_POINT ( 'NONE',  ( 11.99999999999999822, 0.000000000000000000, 0.000000000000000000 ) ) ;
#2585=VERTEX_POINT ( 'NONE', #36819 ) ;
#2592=VERTEX_POINT ( 'NONE', #14572 ) ;
#2597=DIRECTION ( 'NONE',  ( 0.000000000000000000, -0.9510565162951543083, -0.3090169943749448977 ) ) ;
#2598=ORIENTED_EDGE ( 'NONE', *, *, #19428, .F. ) ;
#2599=ORIENTED_EDGE ( 'NONE', *, *, #12044, .F. ) ;
#2600=CARTESIAN_POINT ( 'NONE',  ( 12.00000000000000000, 24.81905959214275370, 9.408202855044498492 ) ) ;
#2609=VERTEX_POINT ( 'NONE', #43469 ) ;
#2610=CARTESIAN_POINT ( 'NONE',  ( 0.000000000000000000, 0.000000000000000000, 0.000000000000000000 ) ) ;
#2614=CARTESIAN_POINT ( 'NONE',  ( 0.000000000000000000, 63.97538442413426907, 51.29473840253246664 ) ) ;
#2615=CYLINDRICAL_SURFACE ( 'NONE', #15241, 31.99999999999998579 ) ;
#2618=CARTESIAN_POINT ( 'NONE',  ( 0.000000000000000000, 2.956366410621684260, -75.11725578898465017 ) ) ;
#2620=ADVANCED_FACE ( 'NONE', ( #28769 ), #6972, .T. ) ;
#2623=DIRECTION ( 'NONE',  ( -1.000000000000000000, -0.000000000000000000, -0.000000000000000000 ) ) ;
#2626=EDGE_LOOP ( 'NONE', ( #1408, #20178, #23614, #17644 ) ) ;
#2627=VECTOR ( 'NONE', #22286, 1000.000000000000000 ) ;
#2628=EDGE_CURVE ( 'NONE', #3559, #40015, #37292, .T. ) ;
#2629=DIRECTION ( 'NONE',  ( -1.000000000000000000, -0.000000000000000000, -0.000000000000000000 ) ) ;
#2635=ORIENTED_EDGE ( 'NONE', *, *, #20793, .T. ) ;
#2640=EDGE_CURVE ( 'NONE', #2161, #12123, #11488, .T. ) ;
#2643=ORIENTED_EDGE ( 'NONE', *, *, #30412, .T. ) ;
#2658=ORIENTED_EDGE ( 'NONE', *, *, #10495, .T. ) ;
#2659=CIRCLE ( 'NONE', #46472, 77.49899999999999523 ) ;
#2660=CARTESIAN_POINT ( 'NONE',  ( 12.00000000000000000, 14.60985201121729737, 18.46759930825687235 ) ) ;
#2661=VECTOR ( 'NONE', #11469, 1000.000000000000000 ) ;
#2664=CIRCLE ( 'NONE', #11287, 31.99999999999998579 ) ;
#2666=DIRECTION ( 'NONE',  ( -1.000000000000000000, 0.000000000000000000, -0.000000000000000000 ) ) ;
#2667=ORIENTED_EDGE ( 'NONE', *, *, #42164, .T. ) ;
#2674=ORIENTED_EDGE ( 'NONE', *, *, #16344, .T. ) ;
#2676=DIRECTION ( 'NONE',  ( -1.000000000000000000, -0.000000000000000000, 0.000000000000000000 ) ) ;
#2677=DIRECTION ( 'NONE',  ( 0.000000000000000000, 0.000000000000000000, 1.000000000000000000 ) ) ;
#2678=DIRECTION ( 'NONE',  ( -1.000000000000000000, -0.000000000000000000, -0.000000000000000000 ) ) ;
#2681=CARTESIAN_POINT ( 'NONE',  ( -10.00000000000000000, 0.000000000000000000, 0.000000000000000000 ) ) ;
#2684=FACE_OUTER_BOUND ( 'NONE', #23919, .T. ) ;
#2689=CARTESIAN_POINT ( 'NONE',  ( 11.99999999999999822, 35.91791733033476675, 68.67312586195008350 ) ) ;
#2690=DIRECTION ( 'NONE',  ( 0.000000000000000000, 0.4539904997395413644, 0.8910065241883706744 ) ) ;
#2692=ADVANCED_FACE ( 'NONE', ( #18931 ), #41241, .T. ) ;
#2698=ADVANCED_FACE ( 'NONE', ( #29722 ), #37553, .F. ) ;
#2699=VECTOR ( 'NONE', #12916, 1000.000000000000000 ) ;
#2704=AXIS2_PLACEMENT_3D ( 'NONE', #14531, #26271, #25277 ) ;
#2706=VECTOR ( 'NONE', #3711, 1000.000000000000227 ) ;
#2708=ORIENTED_EDGE ( 'NONE', *, *, #30296, .T. ) ;
#2709=EDGE_CURVE ( 'NONE', #31959, #4498, #3538, .T. ) ;
#2713=VERTEX_POINT ( 'NONE', #7693 ) ;
#2716=ADVANCED_FACE ( 'NONE', ( #44656 ), #29967, .F. ) ;
#2717=AXIS2_PLACEMENT_3D ( 'NONE', #18469, #44899, #7692 ) ;
#2720=LINE ( 'NONE', #17652, #30522 ) ;
#2721=ORIENTED_EDGE ( 'NONE', *, *, #10550, .T. ) ;
#2724=ORIENTED_EDGE ( 'NONE', *, *, #22985, .F. ) ;
#2728=CARTESIAN_POINT ( 'NONE',  ( 11.99999999999999822, -58.39081064771713869, -50.95692526931392052 ) ) ;
#2732=ORIENTED_EDGE ( 'NONE', *, *, #43881, .T. ) ;
#2734=AXIS2_PLACEMENT_3D ( 'NONE', #20414, #24105, #43441 ) ;
#2735=CIRCLE ( 'NONE', #30113, 31.99999999999998579 ) ;
#2738=VERTEX_POINT ( 'NONE', #14804 ) ;
#2741=DIRECTION ( 'NONE',  ( -0.000000000000000000, -2.312964634635746211E-15, 1.000000000000000000 ) ) ;
#2743=VECTOR ( 'NONE', #20313, 1000.000000000000000 ) ;
#2746=ORIENTED_EDGE ( 'NONE', *, *, #35828, .F. ) ;
#2747=CARTESIAN_POINT ( 'NONE',  ( 0.000000000000000000, 0.000000000000000000, 0.000000000000000000 ) ) ;
#2748=AXIS2_PLACEMENT_3D ( 'NONE', #24349, #21399, #39284 ) ;
#2750=AXIS2_PLACEMENT_3D ( 'NONE', #22542, #30379, #34756 ) ;
#2752=CARTESIAN_POINT ( 'NONE',  ( 15.00000000000000000, -13.04903810567646971, 19.60159698893442481 ) ) ;
#2757=CARTESIAN_POINT ( 'NONE',  ( 11.99999999999999822, 51.03279382321166224, -55.19960302592011914 ) ) ;
#2758=EDGE_CURVE ( 'NONE', #14154, #4001, #11130, .T. ) ;
#2763=CARTESIAN_POINT ( 'NONE',  ( 11.99999999999999822, 0.000000000000000000, 0.000000000000000000 ) ) ;
#2766=AXIS2_PLACEMENT_3D ( 'NONE', #19416, #8645, #344 ) ;
#2774=AXIS2_PLACEMENT_3D ( 'NONE', #43907, #28745, #36792 ) ;
#2775=DIRECTION ( 'NONE',  ( -1.000000000000000000, 0.000000000000000000, 0.000000000000000000 ) ) ;
#2778=VECTOR ( 'NONE', #46587, 1000.000000000000000 ) ;
#2787=CIRCLE ( 'NONE', #9054, 31.99999999999999289 ) ;
#2788=ORIENTED_EDGE ( 'NONE', *, *, #1819, .T. ) ;
#2794=DIRECTION ( 'NONE',  ( 1.000000000000000000, 0.000000000000000000, 0.000000000000000000 ) ) ;
#2797=CARTESIAN_POINT ( 'NONE',  ( 11.99999999999999822, 0.000000000000000000, 0.000000000000000000 ) ) ;
#2799=CARTESIAN_POINT ( 'NONE',  ( 11.99999999999999822, -41.19522573413689059, -65.64334221924951862 ) ) ;
#2801=ORIENTED_EDGE ( 'NONE', *, *, #34348, .T. ) ;
#2812=DIRECTION ( 'NONE',  ( -1.000000000000000000, 0.000000000000000000, 0.000000000000000000 ) ) ;
#2817=EDGE_CURVE ( 'NONE', #8980, #19503, #8737, .T. ) ;
#2820=LINE ( 'NONE', #6033, #2143 ) ;
#2825=DIRECTION ( 'NONE',  ( 0.000000000000000000, 0.000000000000000000, 1.000000000000000000 ) ) ;
#2828=VECTOR ( 'NONE', #10809, 1000.000000000000114 ) ;
#2829=DIRECTION ( 'NONE',  ( 1.000000000000000000, 0.000000000000000000, 0.000000000000000000 ) ) ;
#2831=ORIENTED_EDGE ( 'NONE', *, *, #14332, .F. ) ;
#2835=CARTESIAN_POINT ( 'NONE',  ( 0.000000000000000000, -75.11764819372149304, 2.946379043146075905 ) ) ;
#2836=ORIENTED_EDGE ( 'NONE', *, *, #30067, .F. ) ;
#2837=VERTEX_POINT ( 'NONE', #1565 ) ;
#2841=CARTESIAN_POINT ( 'NONE',  ( 15.00000000000000000, 22.07842321921492612, 8.187992925817123790 ) ) ;
#2857=DIRECTION ( 'NONE',  ( 0.000000000000000000, -0.5224985647159380298, -0.8526401643540988395 ) ) ;
#2861=VERTEX_POINT ( 'NONE', #16260 ) ;
#2863=PLANE ( 'NONE',  #8071 ) ;
#2867=AXIS2_PLACEMENT_3D ( 'NONE', #5065, #19980, #20708 ) ;
#2879=LINE ( 'NONE', #32510, #33367 ) ;
#2881=VECTOR ( 'NONE', #36860, 1000.000000000000000 ) ;
#2882=LINE ( 'NONE', #17807, #32572 ) ;
#2887=ORIENTED_EDGE ( 'NONE', *, *, #8363, .F. ) ;
#2891=CARTESIAN_POINT ( 'NONE',  ( 5.999999999999999112, -67.80270845531855173, -46.11716303203260736 ) ) ;
#2896=CARTESIAN_POINT ( 'NONE',  ( 5.999999999999999112, 55.16347631943042984, 60.67117009219155932 ) ) ;
#2900=AXIS2_PLACEMENT_3D ( 'NONE', #17973, #43693, #32208 ) ;
#2904=ORIENTED_EDGE ( 'NONE', *, *, #42276, .F. ) ;
#2908=DIRECTION ( 'NONE',  ( 0.000000000000000000, 0.000000000000000000, 1.000000000000000000 ) ) ;
#2909=EDGE_CURVE ( 'NONE', #15376, #46446, #40794, .T. ) ;
#2911=CARTESIAN_POINT ( 'NONE',  ( 0.000000000000000000, 0.000000000000000000, 0.000000000000000000 ) ) ;
#2914=ORIENTED_EDGE ( 'NONE', *, *, #21131, .F. ) ;
#2915=DIRECTION ( 'NONE',  ( -1.000000000000000000, -0.000000000000000000, -0.000000000000000000 ) ) ;
#2920=VERTEX_POINT ( 'NONE', #9375 ) ;
#2924=VERTEX_POINT ( 'NONE', #13303 ) ;
#2926=DIRECTION ( 'NONE',  ( -1.000000000000000000, 0.000000000000000000, 0.000000000000000000 ) ) ;
#2929=CARTESIAN_POINT ( 'NONE',  ( 0.000000000000000000, 68.27212725128275395, -31.46837873495001503 ) ) ;
#2930=EDGE_CURVE ( 'NONE', #14333, #29462, #24313, .T. ) ;
#2935=DIRECTION ( 'NONE',  ( -1.000000000000000000, -0.000000000000000000, 0.000000000000000000 ) ) ;
#2937=CYLINDRICAL_SURFACE ( 'NONE', #33848, 82.00000000000000000 ) ;
#2941=EDGE_CURVE ( 'NONE', #20052, #22205, #21108, .T. ) ;
#2944=CARTESIAN_POINT ( 'NONE',  ( 0.000000000000000000, -64.81221759200379040, 50.23322058963324110 ) ) ;
#2945=VECTOR ( 'NONE', #16433, 1000.000000000000000 ) ;
#2946=CARTESIAN_POINT ( 'NONE',  ( 0.000000000000000000, -63.97538442413390669, -51.29473840253292138 ) ) ;
#2954=AXIS2_PLACEMENT_3D ( 'NONE', #33914, #37841, #19954 ) ;
#2963=CARTESIAN_POINT ( 'NONE',  ( 11.99999999999999822, 46.21855187248630870, 62.20884554314035597 ) ) ;
#2974=EDGE_LOOP ( 'NONE', ( #17846, #34037, #15084, #12770 ) ) ;
#2978=LINE ( 'NONE', #33331, #8973 ) ;
#2979=CIRCLE ( 'NONE', #13919, 77.49899999999999523 ) ;
#2983=ORIENTED_EDGE ( 'NONE', *, *, #35523, .F. ) ;
#2985=DIRECTION ( 'NONE',  ( -1.000000000000000000, -0.000000000000000000, -0.000000000000000000 ) ) ;
#2986=DIRECTION ( 'NONE',  ( 0.000000000000000000, 0.9781476007338065770, 0.2079116908177544853 ) ) ;
#2988=DIRECTION ( 'NONE',  ( 0.000000000000000000, 0.000000000000000000, -1.000000000000000000 ) ) ;
#3001=CIRCLE ( 'NONE', #34259, 82.00000000000000000 ) ;
#3003=EDGE_LOOP ( 'NONE', ( #13930, #10435, #14734, #19264 ) ) ;
#3004=CYLINDRICAL_SURFACE ( 'NONE', #35549, 31.99999999999998579 ) ;
#3008=CARTESIAN_POINT ( 'NONE',  ( 11.99999999999999822, 41.76937507738788469, 62.50329211542452157 ) ) ;
#3012=VECTOR ( 'NONE', #6818, 1000.000000000000114 ) ;
#3015=CARTESIAN_POINT ( 'NONE',  ( 0.000000000000000000, 29.01471420065673712, -76.69515212745984911 ) ) ;
#3016=EDGE_LOOP ( 'NONE', ( #32904, #12032, #47094, #6880 ) ) ;
#3017=ADVANCED_FACE ( 'NONE', ( #36293 ), #29177, .T. ) ;
#3019=CYLINDRICAL_SURFACE ( 'NONE', #43389, 31.99999999999998579 ) ;
#3020=VERTEX_POINT ( 'NONE', #36529 ) ;
#3022=FACE_OUTER_BOUND ( 'NONE', #36010, .T. ) ;
#3032=CARTESIAN_POINT ( 'NONE',  ( 11.99999999999999822, -6.903761155838323837, 77.19088730480521576 ) ) ;
#3034=EDGE_LOOP ( 'NONE', ( #20211, #4846, #8905, #4012 ) ) ;
#3040=ORIENTED_EDGE ( 'NONE', *, *, #46065, .F. ) ;
#3042=CARTESIAN_POINT ( 'NONE',  ( 11.99999999999999822, -17.28742895386137945, 75.54627589209938776 ) ) ;
#3045=DIRECTION ( 'NONE',  ( -1.000000000000000000, 0.000000000000000000, -0.000000000000000000 ) ) ;
#3046=ORIENTED_EDGE ( 'NONE', *, *, #12341, .T. ) ;
#3051=CARTESIAN_POINT ( 'NONE',  ( 11.99999999999999822, 0.000000000000000000, 0.000000000000000000 ) ) ;
#3053=DIRECTION ( 'NONE',  ( -1.000000000000000000, 0.000000000000000000, -0.000000000000000000 ) ) ;
#3062=EDGE_CURVE ( 'NONE', #20359, #39585, #4350, .T. ) ;
#3063=DIRECTION ( 'NONE',  ( -1.000000000000000000, 0.000000000000000000, 0.000000000000000000 ) ) ;
#3065=ORIENTED_EDGE ( 'NONE', *, *, #44702, .T. ) ;
#3067=VECTOR ( 'NONE', #23921, 1000.000000000000000 ) ;
#3068=EDGE_CURVE ( 'NONE', #18838, #35058, #37944, .T. ) ;
#3070=CARTESIAN_POINT ( 'NONE',  ( 11.99999999999999822, 0.000000000000000000, 0.000000000000000000 ) ) ;
#3075=EDGE_CURVE ( 'NONE', #6056, #33596, #32405, .T. ) ;
#3076=EDGE_LOOP ( 'NONE', ( #34244, #18823, #6534, #26464 ) ) ;
#3078=DIRECTION ( 'NONE',  ( 0.000000000000000000, 0.000000000000000000, 1.000000000000000000 ) ) ;
#3080=ORIENTED_EDGE ( 'NONE', *, *, #26244, .F. ) ;
#3086=ORIENTED_EDGE ( 'NONE', *, *, #22996, .F. ) ;
#3092=ORIENTED_EDGE ( 'NONE', *, *, #35353, .F. ) ;
#3093=CARTESIAN_POINT ( 'NONE',  ( 15.00000000000000000, 6.762365576493647445, 25.66652317338391498 ) ) ;
#3096=CARTESIAN_POINT ( 'NONE',  ( 5.999999999999999112, 67.80270845531887858, 46.11716303203210288 ) ) ;
#3097=DIRECTION ( 'NONE',  ( 0.000000000000000000, 0.000000000000000000, 1.000000000000000000 ) ) ;
#3099=DIRECTION ( 'NONE',  ( -1.000000000000000000, 0.000000000000000000, 0.000000000000000000 ) ) ;
#3100=ORIENTED_EDGE ( 'NONE', *, *, #43406, .F. ) ;
#3102=CARTESIAN_POINT ( 'NONE',  ( 5.999999999999999112, 46.11716303203186840, 67.80270845531904911 ) ) ;
#3103=DIRECTION ( 'NONE',  ( -1.000000000000000000, -0.000000000000000000, -0.000000000000000000 ) ) ;
#3105=CARTESIAN_POINT ( 'NONE',  ( 11.99999999999999822, 33.71516098798849015, -74.74816331893393340 ) ) ;
#3114=AXIS2_PLACEMENT_3D ( 'NONE', #42240, #42015, #12629 ) ;
#3123=CARTESIAN_POINT ( 'NONE',  ( 0.000000000000000000, 0.000000000000000000, 0.000000000000000000 ) ) ;
#3124=ORIENTED_EDGE ( 'NONE', *, *, #14091, .T. ) ;
#3132=ORIENTED_EDGE ( 'NONE', *, *, #17169, .T. ) ;
#3137=DIRECTION ( 'NONE',  ( -1.000000000000000000, 0.000000000000000000, 0.000000000000000000 ) ) ;
#3138=AXIS2_PLACEMENT_3D ( 'NONE', #35853, #2320, #31004 ) ;
#3148=CARTESIAN_POINT ( 'NONE',  ( 11.99999999999999822, 80.55351364060611274, -15.33399622253397609 ) ) ;
#3151=VERTEX_POINT ( 'NONE', #1200 ) ;
#3153=LINE ( 'NONE', #10517, #5910 ) ;
#3161=CARTESIAN_POINT ( 'NONE',  ( 11.99999999999999822, 73.95703589264006439, -23.16143007188350822 ) ) ;
#3168=ORIENTED_EDGE ( 'NONE', *, *, #43733, .T. ) ;
#3176=AXIS2_PLACEMENT_3D ( 'NONE', #33251, #26633, #29813 ) ;
#3178=DIRECTION ( 'NONE',  ( -1.000000000000000000, 0.000000000000000000, 0.000000000000000000 ) ) ;
#3184=CARTESIAN_POINT ( 'NONE',  ( 11.99999999999999822, 33.71516098798741012, 74.74816331893441657 ) ) ;
#3185=ORIENTED_EDGE ( 'NONE', *, *, #11289, .F. ) ;
#3189=CARTESIAN_POINT ( 'NONE',  ( 11.99999999999999822, -8.830959090341869100, -74.65491531819127147 ) ) ;
#3190=EDGE_CURVE ( 'NONE', #27256, #1470, #1688, .T. ) ;
#3200=DIRECTION ( 'NONE',  ( 0.000000000000000000, -0.9510565162951507556, 0.3090169943749561110 ) ) ;
#3201=EDGE_CURVE ( 'NONE', #18192, #45952, #40683, .T. ) ;
#3206=AXIS2_PLACEMENT_3D ( 'NONE', #5029, #31468, #16289 ) ;
#3210=LINE ( 'NONE', #41174, #42431 ) ;
#3211=DIRECTION ( 'NONE',  ( 0.000000000000000000, 0.000000000000000000, 1.000000000000000000 ) ) ;
#3212=AXIS2_PLACEMENT_3D ( 'NONE', #24002, #5393, #8567 ) ;
#3214=DIRECTION ( 'NONE',  ( -1.000000000000000000, -0.000000000000000000, 0.000000000000000000 ) ) ;
#3219=AXIS2_PLACEMENT_3D ( 'NONE', #18576, #12690, #23217 ) ;
#3221=AXIS2_PLACEMENT_3D ( 'NONE', #40861, #11251, #36926 ) ;
#3223=ORIENTED_EDGE ( 'NONE', *, *, #47675, .F. ) ;
#3224=CARTESIAN_POINT ( 'NONE',  ( 15.00000000000000000, -3.948201729842032215, 23.21447184625297666 ) ) ;
#3230=DIRECTION ( 'NONE',  ( 1.000000000000000000, 0.000000000000000000, 0.000000000000000000 ) ) ;
#3232=DIRECTION ( 'NONE',  ( -1.000000000000000000, 0.000000000000000000, 0.000000000000000000 ) ) ;
#3233=LINE ( 'NONE', #47780, #27268 ) ;
#3236=CARTESIAN_POINT ( 'NONE',  ( 11.99999999999999822, -59.46389618801999433, 49.70050353004867816 ) ) ;
#3243=ORIENTED_EDGE ( 'NONE', *, *, #36006, .T. ) ;
#3248=CARTESIAN_POINT ( 'NONE',  ( 0.000000000000000000, 54.21277698773675979, 55.38113227695801299 ) ) ;
#3260=CARTESIAN_POINT ( 'NONE',  ( 0.000000000000000000, -28.89263327155693517, -71.91182617369219088 ) ) ;
#3264=CARTESIAN_POINT ( 'NONE',  ( 11.99999999999999822, -60.67117009219176538, 55.16347631943021668 ) ) ;
#3265=EDGE_CURVE ( 'NONE', #27284, #36359, #7753, .T. ) ;
#3267=ORIENTED_EDGE ( 'NONE', *, *, #14213, .T. ) ;
#3271=DIRECTION ( 'NONE',  ( 0.000000000000000000, -0.9238795325112906243, 0.3826834323650805669 ) ) ;
#3274=DIRECTION ( 'NONE',  ( -1.000000000000000000, -0.000000000000000000, 0.000000000000000000 ) ) ;
#3278=DIRECTION ( 'NONE',  ( 0.000000000000000000, 0.000000000000000000, 1.000000000000000000 ) ) ;
#3280=DIRECTION ( 'NONE',  ( -1.000000000000000000, -0.000000000000000000, 0.000000000000000000 ) ) ;
#3281=ORIENTED_EDGE ( 'NONE', *, *, #17632, .T. ) ;
#3283=DIRECTION ( 'NONE',  ( 0.000000000000000000, -0.7071067811865389130, -0.7071067811865561215 ) ) ;
#3286=CARTESIAN_POINT ( 'NONE',  ( 6.000000000000000000, 34.94270380257639630, 74.18225833017899618 ) ) ;
#3287=VECTOR ( 'NONE', #39059, 1000.000000000000000 ) ;
#3295=ADVANCED_FACE ( 'NONE', ( #28340 ), #31558, .T. ) ;
#3298=EDGE_LOOP ( 'NONE', ( #12279, #35398, #34194, #8022 ) ) ;
#3300=EDGE_CURVE ( 'NONE', #20106, #31210, #39264, .T. ) ;
#3305=ORIENTED_EDGE ( 'NONE', *, *, #41146, .T. ) ;
#3309=ORIENTED_EDGE ( 'NONE', *, *, #44430, .F. ) ;
#3311=DIRECTION ( 'NONE',  ( -1.000000000000000000, -0.000000000000000000, 0.000000000000000000 ) ) ;
#3320=VERTEX_POINT ( 'NONE', #47896 ) ;
#3328=CYLINDRICAL_SURFACE ( 'NONE', #25545, 82.00000000000000000 ) ;
#3329=ORIENTED_EDGE ( 'NONE', *, *, #7204, .T. ) ;
#3330=CARTESIAN_POINT ( 'NONE',  ( 11.99999999999999822, -58.39081064771786345, 50.95692526931308919 ) ) ;
#3331=AXIS2_PLACEMENT_3D ( 'NONE', #46850, #28486, #24812 ) ;
#3334=DIRECTION ( 'NONE',  ( -1.000000000000000000, 0.000000000000000000, 0.000000000000000000 ) ) ;
#3339=DIRECTION ( 'NONE',  ( -1.000000000000000000, 0.000000000000000000, 0.000000000000000000 ) ) ;
#3340=VERTEX_POINT ( 'NONE', #40344 ) ;
#3341=DIRECTION ( 'NONE',  ( -1.000000000000000000, 0.000000000000000000, 0.000000000000000000 ) ) ;
#3343=DIRECTION ( 'NONE',  ( 0.000000000000000000, -0.07845909572783055230, -0.9969173337331290741 ) ) ;
#3345=VECTOR ( 'NONE', #54, 1000.000000000000000 ) ;
#3352=DIRECTION ( 'NONE',  ( -1.000000000000000000, -0.000000000000000000, 0.000000000000000000 ) ) ;
#3359=CARTESIAN_POINT ( 'NONE',  ( 0.000000000000000000, 41.19522573413826194, -65.64334221924865176 ) ) ;
#3363=CIRCLE ( 'NONE', #44009, 31.99999999999998934 ) ;
#3364=EDGE_CURVE ( 'NONE', #14436, #25362, #18535, .T. ) ;
#3366=DIRECTION ( 'NONE',  ( -0.000000000000000000, 0.4067366430757998752, 0.9135454576426010886 ) ) ;
#3380=AXIS2_PLACEMENT_3D ( 'NONE', #18742, #22187, #15091 ) ;
#3388=AXIS2_PLACEMENT_3D ( 'NONE', #25148, #6094, #28345 ) ;
#3391=ORIENTED_EDGE ( 'NONE', *, *, #3068, .T. ) ;
#3395=EDGE_LOOP ( 'NONE', ( #47926, #405, #25717, #36183 ) ) ;
#3396=CIRCLE ( 'NONE', #16739, 31.99999999999998224 ) ;
#3401=DIRECTION ( 'NONE',  ( 1.000000000000000000, 0.000000000000000000, 0.000000000000000000 ) ) ;
#3402=AXIS2_PLACEMENT_3D ( 'NONE', #24334, #39266, #17215 ) ;
#3403=CYLINDRICAL_SURFACE ( 'NONE', #16972, 82.00000000000000000 ) ;
#3408=EDGE_CURVE ( 'NONE', #23027, #26795, #38842, .T. ) ;
#3409=DIRECTION ( 'NONE',  ( -1.000000000000000000, 0.000000000000000000, -0.000000000000000000 ) ) ;
#3415=ORIENTED_EDGE ( 'NONE', *, *, #42497, .F. ) ;
#3416=CIRCLE ( 'NONE', #47209, 77.49899999999999523 ) ;
#3417=ORIENTED_EDGE ( 'NONE', *, *, #269, .T. ) ;
#3419=LINE ( 'NONE', #11019, #36189 ) ;
#3422=AXIS2_PLACEMENT_3D ( 'NONE', #6786, #21212, #13890 ) ;
#3424=EDGE_CURVE ( 'NONE', #39585, #16941, #37380, .T. ) ;
#3425=CARTESIAN_POINT ( 'NONE',  ( 6.000000000000000000, 81.50828551894227303, 8.966570791700986476 ) ) ;
#3427=AXIS2_PLACEMENT_3D ( 'NONE', #44484, #6807, #29555 ) ;
#3428=CIRCLE ( 'NONE', #23782, 31.99999999999999289 ) ;
#3430=DIRECTION ( 'NONE',  ( -1.000000000000000000, 0.000000000000000000, 0.000000000000000000 ) ) ;
#3435=EDGE_CURVE ( 'NONE', #15783, #22095, #2879, .T. ) ;
#3437=EDGE_LOOP ( 'NONE', ( #15915, #27323, #27063, #33416 ) ) ;
#3438=ORIENTED_EDGE ( 'NONE', *, *, #41015, .F. ) ;
#3447=CARTESIAN_POINT ( 'NONE',  ( 15.00000000000000000, -22.67460108101774452, 6.353146135318220367 ) ) ;
#3450=DIRECTION ( 'NONE',  ( 0.000000000000000000, 0.9723699203976756689, 0.2334453638559094157 ) ) ;
#3453=CARTESIAN_POINT ( 'NONE',  ( 11.99999999999999822, -51.29473840253269401, 63.97538442413408433 ) ) ;
#3459=VERTEX_POINT ( 'NONE', #14636 ) ;
#3460=ORIENTED_EDGE ( 'NONE', *, *, #12945, .T. ) ;
#3461=CYLINDRICAL_SURFACE ( 'NONE', #4107, 82.00000000000000000 ) ;
#3463=VERTEX_POINT ( 'NONE', #29551 ) ;
#3466=CARTESIAN_POINT ( 'NONE',  ( 11.99999999999999822, 67.80270845531889279, 46.11716303203210288 ) ) ;
#3470=AXIS2_PLACEMENT_3D ( 'NONE', #41447, #7905, #22839 ) ;
#3475=CARTESIAN_POINT ( 'NONE',  ( 6.000000000000000000, 81.90746397400387480, 3.894527615418180044 ) ) ;
#3476=ORIENTED_EDGE ( 'NONE', *, *, #20730, .F. ) ;
#3478=CIRCLE ( 'NONE', #21434, 31.99999999999998579 ) ;
#3482=DIRECTION ( 'NONE',  ( 0.000000000000000000, 0.9238795325112877377, -0.3826834323650873948 ) ) ;
#3484=AXIS2_PLACEMENT_3D ( 'NONE', #30533, #45453, #7545 ) ;
#3491=EDGE_CURVE ( 'NONE', #40723, #15200, #25530, .T. ) ;
#3503=DIRECTION ( 'NONE',  ( 0.000000000000000000, 0.000000000000000000, 1.000000000000000000 ) ) ;
#3506=CARTESIAN_POINT ( 'NONE',  ( 11.99999999999999822, -65.59268652807183742, -36.72794159290312166 ) ) ;
#3508=DIRECTION ( 'NONE',  ( -1.000000000000000000, -0.000000000000000000, 0.000000000000000000 ) ) ;
#3510=CYLINDRICAL_SURFACE ( 'NONE', #21544, 31.99999999999998579 ) ;
#3516=DIRECTION ( 'NONE',  ( 0.000000000000000000, -0.8910065241883723397, 0.4539904997395382003 ) ) ;
#3517=DIRECTION ( 'NONE',  ( 0.000000000000000000, 0.8090169943749486725, -0.5877852522924714718 ) ) ;
#3520=CARTESIAN_POINT ( 'NONE',  ( 0.000000000000000000, -2.946379043146863719, 75.11764819372146462 ) ) ;
#3525=CYLINDRICAL_SURFACE ( 'NONE', #30880, 31.99999999999998579 ) ;
#3528=DIRECTION ( 'NONE',  ( 1.000000000000000000, -0.000000000000000000, -0.000000000000000000 ) ) ;
#3530=DIRECTION ( 'NONE',  ( -1.000000000000000000, 0.000000000000000000, 0.000000000000000000 ) ) ;
#3536=CARTESIAN_POINT ( 'NONE',  ( 0.000000000000000000, -72.35160999960801576, -20.41045688087902121 ) ) ;
#3538=LINE ( 'NONE', #45617, #37266 ) ;
#3550=DIRECTION ( 'NONE',  ( -1.000000000000000000, 0.000000000000000000, 0.000000000000000000 ) ) ;
#3552=CARTESIAN_POINT ( 'NONE',  ( 0.000000000000000000, 34.94270380257639630, 74.18225833017899618 ) ) ;
#3555=EDGE_LOOP ( 'NONE', ( #34376, #7559, #10795, #28368 ) ) ;
#3557=EDGE_CURVE ( 'NONE', #22223, #24540, #34130, .T. ) ;
#3559=VERTEX_POINT ( 'NONE', #30516 ) ;
#3562=ORIENTED_EDGE ( 'NONE', *, *, #2909, .T. ) ;
#3563=AXIS2_PLACEMENT_3D ( 'NONE', #13013, #28164, #5414 ) ;
#3565=DIRECTION ( 'NONE',  ( 0.000000000000000000, 0.2079116908177555123, -0.9781476007338064660 ) ) ;
#3567=ORIENTED_EDGE ( 'NONE', *, *, #16872, .F. ) ;
#3569=ORIENTED_EDGE ( 'NONE', *, *, #43344, .F. ) ;
#3575=CARTESIAN_POINT ( 'NONE',  ( 15.00000000000000000, 8.688484142254226938, 21.88630264137359305 ) ) ;
#3576=AXIS2_PLACEMENT_3D ( 'NONE', #28628, #1970, #17343 ) ;
#3585=LINE ( 'NONE', #18517, #30731 ) ;
#3586=CYLINDRICAL_SURFACE ( 'NONE', #8117, 31.99999999999998579 ) ;
#3587=CARTESIAN_POINT ( 'NONE',  ( 0.000000000000000000, 8.966570791700705811, 81.50828551894228724 ) ) ;
#3589=DIRECTION ( 'NONE',  ( -1.000000000000000000, 0.000000000000000000, 0.000000000000000000 ) ) ;
#3591=LINE ( 'NONE', #30278, #34716 ) ;
#3592=EDGE_LOOP ( 'NONE', ( #31845, #9182, #38858, #40891 ) ) ;
#3593=DIRECTION ( 'NONE',  ( 1.000000000000000000, 0.000000000000000000, -0.000000000000000000 ) ) ;
#3595=CIRCLE ( 'NONE', #30973, 82.00000000000000000 ) ;
#3596=EDGE_CURVE ( 'NONE', #23277, #27199, #20948, .T. ) ;
#3598=DIRECTION ( 'NONE',  ( 0.000000000000000000, 0.07845909572784530439, -0.9969173337331279638 ) ) ;
#3599=CIRCLE ( 'NONE', #26281, 31.99999999999998934 ) ;
#3600=CARTESIAN_POINT ( 'NONE',  ( 6.000000000000000000, -22.90783923731575200, -78.73519480814978522 ) ) ;
#3607=CYLINDRICAL_SURFACE ( 'NONE', #23983, 31.99999999999998579 ) ;
#3615=ORIENTED_EDGE ( 'NONE', *, *, #15695, .F. ) ;
#3620=CARTESIAN_POINT ( 'NONE',  ( 11.99999999999999822, -31.47745569255092235, -68.26794271651296242 ) ) ;
#3622=ORIENTED_EDGE ( 'NONE', *, *, #13594, .T. ) ;
#3625=CARTESIAN_POINT ( 'NONE',  ( 11.99999999999999822, 81.96053171279901051, -2.543863470248673764 ) ) ;
#3626=EDGE_LOOP ( 'NONE', ( #38255, #27177, #18126, #3562 ) ) ;
#3629=EDGE_LOOP ( 'NONE', ( #26626, #11407, #29031, #16703 ) ) ;
#3631=VECTOR ( 'NONE', #35927, 1000.000000000000000 ) ;
#3634=CYLINDRICAL_SURFACE ( 'NONE', #46567, 82.00000000000000000 ) ;
#3636=ORIENTED_EDGE ( 'NONE', *, *, #8442, .F. ) ;
#3638=LINE ( 'NONE', #916, #37687 ) ;
#3639=ADVANCED_FACE ( 'NONE', ( #16800 ), #9204, .F. ) ;
#3642=ORIENTED_EDGE ( 'NONE', *, *, #4528, .T. ) ;
#3648=VERTEX_POINT ( 'NONE', #46896 ) ;
#3650=ADVANCED_FACE ( 'NONE', ( #31751 ), #12645, .T. ) ;
#3651=CYLINDRICAL_SURFACE ( 'NONE', #1788, 77.49899999999999523 ) ;
#3653=ORIENTED_EDGE ( 'NONE', *, *, #11617, .F. ) ;
#3656=AXIS2_PLACEMENT_3D ( 'NONE', #38223, #11790, #46055 ) ;
#3657=DIRECTION ( 'NONE',  ( 0.000000000000000000, -0.2079116908177664758, -0.9781476007338042455 ) ) ;
#3658=DIRECTION ( 'NONE',  ( 0.000000000000000000, -0.9969173337331271867, -0.07845909572785571273 ) ) ;
#3663=CYLINDRICAL_SURFACE ( 'NONE', #38025, 77.49899999999999523 ) ;
#3665=DIRECTION ( 'NONE',  ( 0.000000000000000000, 0.7071067811865486830, -0.7071067811865464625 ) ) ;
#3667=DIRECTION ( 'NONE',  ( 1.000000000000000000, 0.000000000000000000, 0.000000000000000000 ) ) ;
#3691=ORIENTED_EDGE ( 'NONE', *, *, #34310, .F. ) ;
#3703=ORIENTED_EDGE ( 'NONE', *, *, #17024, .F. ) ;
#3708=ORIENTED_EDGE ( 'NONE', *, *, #18499, .T. ) ;
#3711=DIRECTION ( 'NONE',  ( 0.000000000000000000, 0.3090169943749560555, 0.9510565162951506446 ) ) ;
#3714=LINE ( 'NONE', #33799, #20345 ) ;
#3741=EDGE_CURVE ( 'NONE', #36132, #28640, #30276, .T. ) ;
#3747=CARTESIAN_POINT ( 'NONE',  ( 11.99999999999999822, 77.19088730480532945, -6.903761155836932062 ) ) ;
#3748=CARTESIAN_POINT ( 'NONE',  ( 0.000000000000000000, 75.16055320797057959, -18.89407956138179046 ) ) ;
#3749=VERTEX_POINT ( 'NONE', #40515 ) ;
#3761=ORIENTED_EDGE ( 'NONE', *, *, #19163, .T. ) ;
#3762=CARTESIAN_POINT ( 'NONE',  ( 11.99999999999999822, 77.32052557432849937, -5.256550761632002633 ) ) ;
#3770=ORIENTED_EDGE ( 'NONE', *, *, #22635, .T. ) ;
#3777=CARTESIAN_POINT ( 'NONE',  ( 0.000000000000000000, 41.76937507738788469, 62.50329211542452157 ) ) ;
#3781=CARTESIAN_POINT ( 'NONE',  ( 11.99999999999999822, -59.03961581697432592, 46.53671651293927880 ) ) ;
#3787=CARTESIAN_POINT ( 'NONE',  ( 11.99999999999999822, 0.000000000000000000, 0.000000000000000000 ) ) ;
#3794=ORIENTED_EDGE ( 'NONE', *, *, #25279, .T. ) ;
#3795=EDGE_CURVE ( 'NONE', #9001, #40828, #14322, .T. ) ;
#3797=ORIENTED_EDGE ( 'NONE', *, *, #14332, .T. ) ;
#3798=EDGE_CURVE ( 'NONE', #15671, #8125, #28623, .T. ) ;
#3801=CARTESIAN_POINT ( 'NONE',  ( 11.99999999999999822, 46.21855187248719687, -62.20884554313968806 ) ) ;
#3809=EDGE_LOOP ( 'NONE', ( #4105, #5843, #7603, #4696 ) ) ;
#3822=VERTEX_POINT ( 'NONE', #40036 ) ;
#3823=CIRCLE ( 'NONE', #20278, 31.99999999999999289 ) ;
#3827=VECTOR ( 'NONE', #36429, 999.9999999999998863 ) ;
#3829=CIRCLE ( 'NONE', #37441, 31.99999999999998934 ) ;
#3830=CARTESIAN_POINT ( 'NONE',  ( 11.99999999999999822, 62.50884508063427347, 41.76106447765511831 ) ) ;
#3841=DIRECTION ( 'NONE',  ( -1.000000000000000000, -0.000000000000000000, -0.000000000000000000 ) ) ;
#3847=DIRECTION ( 'NONE',  ( -1.000000000000000000, 0.000000000000000000, -0.000000000000000000 ) ) ;
#3857=ORIENTED_EDGE ( 'NONE', *, *, #34399, .F. ) ;
#3859=ORIENTED_EDGE ( 'NONE', *, *, #18405, .T. ) ;
#3860=AXIS2_PLACEMENT_3D ( 'NONE', #2835, #3063, #17991 ) ;
#3861=EDGE_CURVE ( 'NONE', #43300, #25765, #2050, .T. ) ;
#3862=ORIENTED_EDGE ( 'NONE', *, *, #28651, .T. ) ;
#3863=DIRECTION ( 'NONE',  ( 0.000000000000000000, 0.000000000000000000, 1.000000000000000000 ) ) ;
#3867=DIRECTION ( 'NONE',  ( -1.000000000000000000, 0.000000000000000000, -0.000000000000000000 ) ) ;
#3868=ORIENTED_EDGE ( 'NONE', *, *, #9825, .T. ) ;
#3877=ADVANCED_FACE ( 'NONE', ( #23116 ), #22866, .T. ) ;
#3878=ORIENTED_EDGE ( 'NONE', *, *, #9783, .T. ) ;
#3881=FACE_OUTER_BOUND ( 'NONE', #989, .T. ) ;
#3882=LINE ( 'NONE', #33729, #10385 ) ;
#3884=ORIENTED_EDGE ( 'NONE', *, *, #39018, .F. ) ;
#3886=EDGE_CURVE ( 'NONE', #7287, #40723, #26311, .T. ) ;
#3888=CARTESIAN_POINT ( 'NONE',  ( 0.000000000000000000, 0.000000000000000000, 21.00000000000000000 ) ) ;
#3909=SURFACE_SIDE_STYLE ('',( #22516 ) ) ;
#3912=EDGE_CURVE ( 'NONE', #41773, #29157, #48151, .T. ) ;
#3913=DIRECTION ( 'NONE',  ( -1.000000000000000000, 0.000000000000000000, 0.000000000000000000 ) ) ;
#3921=VECTOR ( 'NONE', #22423, 1000.000000000000000 ) ;
#3923=VECTOR ( 'NONE', #10626, 1000.000000000000000 ) ;
#3928=ORIENTED_EDGE ( 'NONE', *, *, #24030, .T. ) ;
#3932=AXIS2_PLACEMENT_3D ( 'NONE', #28271, #9919, #17243 ) ;
#3937=EDGE_CURVE ( 'NONE', #32083, #37092, #22366, .T. ) ;
#3938=EDGE_LOOP ( 'NONE', ( #18113, #44434, #30257, #31538 ) ) ;
#3947=ORIENTED_EDGE ( 'NONE', *, *, #42333, .F. ) ;
#3949=VERTEX_POINT ( 'NONE', #827 ) ;
#3954=ORIENTED_EDGE ( 'NONE', *, *, #12430, .T. ) ;
#3959=DIRECTION ( 'NONE',  ( 0.000000000000000000, 0.000000000000000000, 1.000000000000000000 ) ) ;
#3961=DIRECTION ( 'NONE',  ( -1.000000000000000000, 0.000000000000000000, 0.000000000000000000 ) ) ;
#3962=EDGE_CURVE ( 'NONE', #29157, #24923, #4287, .T. ) ;
#3964=CARTESIAN_POINT ( 'NONE',  ( 11.99999999999999822, -14.66109333815513160, 73.73191006444567108 ) ) ;
#3966=AXIS2_PLACEMENT_3D ( 'NONE', #31220, #17223, #46376 ) ;
#3967=EDGE_CURVE ( 'NONE', #18691, #35660, #2787, .T. ) ;
#3968=VECTOR ( 'NONE', #23800, 1000.000000000000000 ) ;
#3970=CARTESIAN_POINT ( 'NONE',  ( 11.99999999999999822, 36.72794159290241822, 65.59268652807223532 ) ) ;
#3975=DIRECTION ( 'NONE',  ( 0.000000000000000000, 0.000000000000000000, 1.000000000000000000 ) ) ;
#3983=FACE_BOUND ( 'NONE', #33500, .T. ) ;
#3985=ORIENTED_EDGE ( 'NONE', *, *, #24756, .T. ) ;
#3986=EDGE_CURVE ( 'NONE', #45638, #30137, #36412, .T. ) ;
#3991=ORIENTED_EDGE ( 'NONE', *, *, #41015, .T. ) ;
#3995=ORIENTED_EDGE ( 'NONE', *, *, #3967, .T. ) ;
#4001=VERTEX_POINT ( 'NONE', #27012 ) ;
#4002=AXIS2_PLACEMENT_3D ( 'NONE', #19461, #144, #4795 ) ;
#4008=VECTOR ( 'NONE', #23758, 1000.000000000000000 ) ;
#4012=ORIENTED_EDGE ( 'NONE', *, *, #15003, .T. ) ;
#4021=VERTEX_POINT ( 'NONE', #27735 ) ;
#4030=CARTESIAN_POINT ( 'NONE',  ( 11.99999999999999822, 55.19960302592141232, -51.03279382321027668 ) ) ;
#4037=CIRCLE ( 'NONE', #8702, 82.00000000000000000 ) ;
#4041=EDGE_CURVE ( 'NONE', #1914, #36873, #42904, .T. ) ;
#4042=CARTESIAN_POINT ( 'NONE',  ( 5.999999999999999112, 77.16300072079660310, 27.74655509720697211 ) ) ;
#4043=VECTOR ( 'NONE', #38835, 1000.000000000000000 ) ;
#4045=ADVANCED_FACE ( 'NONE', ( #38497 ), #34562, .F. ) ;
#4047=ORIENTED_EDGE ( 'NONE', *, *, #34315, .T. ) ;
#4048=VECTOR ( 'NONE', #18848, 1000.000000000000000 ) ;
#4049=EDGE_CURVE ( 'NONE', #4021, #14753, #9123, .T. ) ;
#4051=EDGE_LOOP ( 'NONE', ( #874, #14968, #39484, #9962 ) ) ;
#4054=CARTESIAN_POINT ( 'NONE',  ( 12.00000000000000000, -14.54903810567644484, 22.19967320028775504 ) ) ;
#4057=CARTESIAN_POINT ( 'NONE',  ( 0.000000000000000000, 0.000000000000000000, 0.000000000000000000 ) ) ;
#4063=AXIS2_PLACEMENT_3D ( 'NONE', #46411, #8960, #38840 ) ;
#4064=CARTESIAN_POINT ( 'NONE',  ( 5.999999999999999112, 64.81221759200342092, 50.23322058963371006 ) ) ;
#4071=DIRECTION ( 'NONE',  ( 0.000000000000000000, 0.000000000000000000, 1.000000000000000000 ) ) ;
#4084=DIRECTION ( 'NONE',  ( 0.000000000000000000, -0.6494480483301903195, 0.7604059656000251577 ) ) ;
#4086=ORIENTED_EDGE ( 'NONE', *, *, #10061, .T. ) ;
#4088=CARTESIAN_POINT ( 'NONE',  ( 11.99999999999999822, 0.000000000000000000, 0.000000000000000000 ) ) ;
#4089=VECTOR ( 'NONE', #36909, 1000.000000000000000 ) ;
#4100=EDGE_CURVE ( 'NONE', #14333, #38548, #12556, .T. ) ;
#4102=FACE_OUTER_BOUND ( 'NONE', #23591, .T. ) ;
#4103=EDGE_CURVE ( 'NONE', #23663, #31053, #22405, .T. ) ;
#4105=ORIENTED_EDGE ( 'NONE', *, *, #17498, .F. ) ;
#4107=AXIS2_PLACEMENT_3D ( 'NONE', #18634, #14495, #25725 ) ;
#4108=ORIENTED_EDGE ( 'NONE', *, *, #2133, .F. ) ;
#4110=VERTEX_POINT ( 'NONE', #5949 ) ;
#4112=DIRECTION ( 'NONE',  ( 0.000000000000000000, 0.9238795325112878487, -0.3826834323650874503 ) ) ;
#4113=EDGE_LOOP ( 'NONE', ( #5825, #4828, #38494, #2708 ) ) ;
#4127=CARTESIAN_POINT ( 'NONE',  ( 11.99999999999999822, -5.256550761633395297, 77.32052557432841411 ) ) ;
#4129=VECTOR ( 'NONE', #7416, 1000.000000000000000 ) ;
#4133=AXIS2_PLACEMENT_3D ( 'NONE', #765, #46293, #42635 ) ;
#4134=SURFACE_STYLE_FILL_AREA ( #48422 ) ;
#4146=CIRCLE ( 'NONE', #36925, 77.49900000000000944 ) ;
#4148=CARTESIAN_POINT ( 'NONE',  ( 11.99999999999999822, 44.88180994100466847, -63.18004540532978552 ) ) ;
#4149=CARTESIAN_POINT ( 'NONE',  ( 11.99999999999999822, 27.74655509720779989, -77.16300072079630468 ) ) ;
#4150=DIRECTION ( 'NONE',  ( 0.000000000000000000, -0.9945218953682740670, -0.1045284632676459352 ) ) ;
#4152=AXIS2_PLACEMENT_3D ( 'NONE', #11253, #26178, #41119 ) ;
#4153=DIRECTION ( 'NONE',  ( 1.000000000000000000, 0.000000000000000000, 0.000000000000000000 ) ) ;
#4154=DIRECTION ( 'NONE',  ( -0.000000000000000000, 0.9781476007338067991, 0.2079116908177533474 ) ) ;
#4157=AXIS2_PLACEMENT_3D ( 'NONE', #27776, #16748, #31698 ) ;
#4160=CARTESIAN_POINT ( 'NONE',  ( 11.99999999999999822, 75.11764819372142199, 2.946379043147685728 ) ) ;
#4161=EDGE_CURVE ( 'NONE', #2738, #31325, #39476, .T. ) ;
#4165=CYLINDRICAL_SURFACE ( 'NONE', #13621, 82.00000000000000000 ) ;
#4166=CARTESIAN_POINT ( 'NONE',  ( 11.99999999999999822, -46.21855187248585395, -62.20884554314068993 ) ) ;
#4168=DIRECTION ( 'NONE',  ( -1.000000000000000000, -0.000000000000000000, -0.000000000000000000 ) ) ;
#4176=ORIENTED_EDGE ( 'NONE', *, *, #46618, .F. ) ;
#4178=VERTEX_POINT ( 'NONE', #47519 ) ;
#4180=ORIENTED_EDGE ( 'NONE', *, *, #45631, .F. ) ;
#4189=VECTOR ( 'NONE', #2231, 1000.000000000000000 ) ;
#4191=CARTESIAN_POINT ( 'NONE',  ( 11.99999999999999822, 0.000000000000000000, 0.000000000000000000 ) ) ;
#4194=CARTESIAN_POINT ( 'NONE',  ( 15.00000000000000000, 8.688484142254226938, 21.88630264137359305 ) ) ;
#4195=ORIENTED_EDGE ( 'NONE', *, *, #32752, .F. ) ;
#4196=CARTESIAN_POINT ( 'NONE',  ( 11.99999999999999822, -62.20884554314051229, 46.21855187248609553 ) ) ;
#4197=CARTESIAN_POINT ( 'NONE',  ( 11.99999999999999822, 73.72996012237460661, -14.67089635893632504 ) ) ;
#4198=VERTEX_POINT ( 'NONE', #25000 ) ;
#4207=DIRECTION ( 'NONE',  ( -1.000000000000000000, -0.000000000000000000, 0.000000000000000000 ) ) ;
#4209=CARTESIAN_POINT ( 'NONE',  ( 0.000000000000000000, 78.73519480814985627, -22.90783923731548199 ) ) ;
#4214=ORIENTED_EDGE ( 'NONE', *, *, #21143, .T. ) ;
#4220=AXIS2_PLACEMENT_3D ( 'NONE', #13110, #35124, #9190 ) ;
#4222=CARTESIAN_POINT ( 'NONE',  ( 11.99999999999999822, 14.66109333815460225, 73.73191006444577056 ) ) ;
#4224=DIRECTION ( 'NONE',  ( 0.000000000000000000, 0.000000000000000000, 1.000000000000000000 ) ) ;
#4225=DIRECTION ( 'NONE',  ( -1.000000000000000000, -0.000000000000000000, -0.000000000000000000 ) ) ;
#4228=ORIENTED_EDGE ( 'NONE', *, *, #22524, .T. ) ;
#4229=FACE_BOUND ( 'NONE', #36849, .T. ) ;
#4230=VECTOR ( 'NONE', #33815, 1000.000000000000000 ) ;
#4231=ORIENTED_EDGE ( 'NONE', *, *, #33058, .T. ) ;
#4232=EDGE_CURVE ( 'NONE', #35871, #37888, #8318, .T. ) ;
#4233=AXIS2_PLACEMENT_3D ( 'NONE', #41356, #11731, #8044 ) ;
#4235=AXIS2_PLACEMENT_3D ( 'NONE', #36482, #21788, #7100 ) ;
#4244=AXIS2_PLACEMENT_3D ( 'NONE', #1789, #27503, #43151 ) ;
#4245=DIRECTION ( 'NONE',  ( 0.000000000000000000, -0.4067366430757887730, 0.9135454576426059736 ) ) ;
#4247=CIRCLE ( 'NONE', #24542, 82.00000000000000000 ) ;
#4253=ORIENTED_EDGE ( 'NONE', *, *, #26981, .T. ) ;
#4256=DIRECTION ( 'NONE',  ( -1.000000000000000000, 0.000000000000000000, -0.000000000000000000 ) ) ;
#4259=CIRCLE ( 'NONE', #40216, 31.99999999999998934 ) ;
#4264=ORIENTED_EDGE ( 'NONE', *, *, #22224, .T. ) ;
#4273=ORIENTED_EDGE ( 'NONE', *, *, #24861, .F. ) ;
#4277=ADVANCED_FACE ( 'NONE', ( #30382 ), #40659, .F. ) ;
#4278=FACE_OUTER_BOUND ( 'NONE', #32052, .T. ) ;
#4280=CARTESIAN_POINT ( 'NONE',  ( 11.99999999999999822, 55.20638768913760686, 51.02545421589343988 ) ) ;
#4283=ADVANCED_FACE ( 'NONE', ( #14962 ), #14484, .T. ) ;
#4284=CARTESIAN_POINT ( 'NONE',  ( 0.000000000000000000, -23.16143007188479075, 73.95703589263966649 ) ) ;
#4287=LINE ( 'NONE', #27041, #25458 ) ;
#4288=ORIENTED_EDGE ( 'NONE', *, *, #38592, .F. ) ;
#4290=CARTESIAN_POINT ( 'NONE',  ( 0.000000000000000000, -39.78640506895651185, 66.50666863321987421 ) ) ;
#4300=CIRCLE ( 'NONE', #21475, 31.99999999999998934 ) ;
#4301=VERTEX_POINT ( 'NONE', #25964 ) ;
#4302=AXIS2_PLACEMENT_3D ( 'NONE', #39760, #2522, #21371 ) ;
#4306=DIRECTION ( 'NONE',  ( 0.000000000000000000, 0.000000000000000000, 1.000000000000000000 ) ) ;
#4309=DIRECTION ( 'NONE',  ( 0.000000000000000000, 0.000000000000000000, 1.000000000000000000 ) ) ;
#4313=CARTESIAN_POINT ( 'NONE',  ( 5.999999999999999112, -63.97538442413390669, -51.29473840253292138 ) ) ;
#4316=CARTESIAN_POINT ( 'NONE',  ( -10.00000000000000000, 0.000000000000000000, 0.000000000000000000 ) ) ;
#4324=DIRECTION ( 'NONE',  ( -1.000000000000000000, 0.000000000000000000, 0.000000000000000000 ) ) ;
#4327=LINE ( 'NONE', #4794, #22962 ) ;
#4328=DIRECTION ( 'NONE',  ( -1.000000000000000000, -0.000000000000000000, -0.000000000000000000 ) ) ;
#4330=CARTESIAN_POINT ( 'NONE',  ( 15.00000000000000000, -0.9646360437375368635, -23.52805723605589705 ) ) ;
#4332=ORIENTED_EDGE ( 'NONE', *, *, #43443, .T. ) ;
#4335=ORIENTED_EDGE ( 'NONE', *, *, #26981, .F. ) ;
#4342=EDGE_CURVE ( 'NONE', #4790, #23277, #44336, .T. ) ;
#4344=EDGE_CURVE ( 'NONE', #13122, #5353, #29414, .T. ) ;
#4346=CARTESIAN_POINT ( 'NONE',  ( 15.00000000000000000, 14.60985201121729737, 18.46759930825687235 ) ) ;
#4350=CIRCLE ( 'NONE', #31712, 77.49899999999999523 ) ;
#4351=DIRECTION ( 'NONE',  ( -1.000000000000000000, -0.000000000000000000, 0.000000000000000000 ) ) ;
#4352=DIRECTION ( 'NONE',  ( 1.000000000000000000, 0.000000000000000000, 0.000000000000000000 ) ) ;
#4356=CARTESIAN_POINT ( 'NONE',  ( 11.99999999999999822, 0.000000000000000000, 0.000000000000000000 ) ) ;
#4357=VERTEX_POINT ( 'NONE', #18854 ) ;
#4359=AXIS2_PLACEMENT_3D ( 'NONE', #1324, #38781, #15297 ) ;
#4362=LINE ( 'NONE', #8003, #23384 ) ;
#4364=ORIENTED_EDGE ( 'NONE', *, *, #14528, .T. ) ;
#4365=EDGE_CURVE ( 'NONE', #14824, #1839, #41140, .T. ) ;
#4371=EDGE_LOOP ( 'NONE', ( #257, #24392, #30476, #11036 ) ) ;
#4373=CIRCLE ( 'NONE', #46577, 31.99999999999998579 ) ;
#4381=EDGE_LOOP ( 'NONE', ( #10742, #4714, #16922, #3391 ) ) ;
#4396=ORIENTED_EDGE ( 'NONE', *, *, #5654, .T. ) ;
#4404=CARTESIAN_POINT ( 'NONE',  ( 15.00000000000000000, -4.261787119644963262, 26.19803753235780164 ) ) ;
#4405=PLANE ( 'NONE',  #23225 ) ;
#4410=DIRECTION ( 'NONE',  ( 1.000000000000000000, 0.000000000000000000, -0.000000000000000000 ) ) ;
#4413=VERTEX_POINT ( 'NONE', #18387 ) ;
#4414=CARTESIAN_POINT ( 'NONE',  ( 15.00000000000000000, 18.84667830672605859, 18.68964196561243796 ) ) ;
#4422=ORIENTED_EDGE ( 'NONE', *, *, #45697, .T. ) ;
#4423=ADVANCED_FACE ( 'NONE', ( #33069 ), #29884, .T. ) ;
#4426=EDGE_CURVE ( 'NONE', #43334, #35253, #35004, .T. ) ;
#4429=EDGE_CURVE ( 'NONE', #30390, #39278, #16156, .T. ) ;
#4430=AXIS2_PLACEMENT_3D ( 'NONE', #38567, #11895, #5033 ) ;
#4436=VECTOR ( 'NONE', #39181, 1000.000000000000000 ) ;
#4445=EDGE_LOOP ( 'NONE', ( #36165, #32617, #903, #8797 ) ) ;
#4446=CARTESIAN_POINT ( 'NONE',  ( 11.99999999999999822, -6.903761155837269570, -77.19088730480530103 ) ) ;
#4447=ORIENTED_EDGE ( 'NONE', *, *, #10374, .T. ) ;
#4449=ORIENTED_EDGE ( 'NONE', *, *, #15213, .T. ) ;
#4452=CARTESIAN_POINT ( 'NONE',  ( 0.000000000000000000, 55.16347631943131802, -60.67117009219074930 ) ) ;
#4455=FACE_OUTER_BOUND ( 'NONE', #42145, .T. ) ;
#4456=DIRECTION ( 'NONE',  ( 0.000000000000000000, -6.982962677686266711E-15, 1.000000000000000000 ) ) ;
#4457=DIRECTION ( 'NONE',  ( -1.000000000000000000, -0.000000000000000000, 0.000000000000000000 ) ) ;
#4460=DIRECTION ( 'NONE',  ( 0.000000000000000000, 0.000000000000000000, 1.000000000000000000 ) ) ;
#4462=CARTESIAN_POINT ( 'NONE',  ( 11.99999999999999822, 76.69515212746016175, 29.01471420065590578 ) ) ;
#4467=CARTESIAN_POINT ( 'NONE',  ( 11.99999999999999822, 0.000000000000000000, 0.000000000000000000 ) ) ;
#4468=ORIENTED_EDGE ( 'NONE', *, *, #33039, .F. ) ;
#4472=VERTEX_POINT ( 'NONE', #41885 ) ;
#4473=DIRECTION ( 'NONE',  ( -1.000000000000000000, -0.000000000000000000, -0.000000000000000000 ) ) ;
#4474=PRODUCT_CONTEXT ( 'NONE', #12581, 'mechanical' ) ;
#4485=ADVANCED_FACE ( 'NONE', ( #1482 ), #27192, .F. ) ;
#4486=CARTESIAN_POINT ( 'NONE',  ( 11.99999999999999822, 0.000000000000000000, 0.000000000000000000 ) ) ;
#4488=ORIENTED_EDGE ( 'NONE', *, *, #33025, .F. ) ;
#4490=CARTESIAN_POINT ( 'NONE',  ( 11.99999999999999822, 65.58780272294076497, 36.73666225445916211 ) ) ;
#4492=PLANE ( 'NONE',  #25926 ) ;
#4493=VECTOR ( 'NONE', #13344, 1000.000000000000000 ) ;
#4495=EDGE_LOOP ( 'NONE', ( #10672, #36609, #47612, #9646 ) ) ;
#4498=VERTEX_POINT ( 'NONE', #19821 ) ;
#4500=CYLINDRICAL_SURFACE ( 'NONE', #23123, 31.99999999999998579 ) ;
#4506=CARTESIAN_POINT ( 'NONE',  ( 15.00000000000000000, 24.81905959214260804, -9.408202855044828894 ) ) ;
#4507=DIRECTION ( 'NONE',  ( -1.000000000000000000, -0.000000000000000000, 0.000000000000000000 ) ) ;
#4508=CARTESIAN_POINT ( 'NONE',  ( 11.99999999999999822, -31.47745569255092235, -68.26794271651296242 ) ) ;
#4512=CIRCLE ( 'NONE', #11530, 31.99999999999998934 ) ;
#4514=CARTESIAN_POINT ( 'NONE',  ( 15.00000000000000000, 0.000000000000000000, 0.000000000000000000 ) ) ;
#4515=DIRECTION ( 'NONE',  ( 0.000000000000000000, -0.9238795325112822976, -0.3826834323651006620 ) ) ;
#4522=DIRECTION ( 'NONE',  ( 0.000000000000000000, 0.000000000000000000, 1.000000000000000000 ) ) ;
#4527=CIRCLE ( 'NONE', #18562, 82.00000000000000000 ) ;
#4528=EDGE_CURVE ( 'NONE', #10250, #42048, #11823, .T. ) ;
#4530=AXIS2_PLACEMENT_3D ( 'NONE', #11569, #37741, #4224 ) ;
#4537=EDGE_CURVE ( 'NONE', #5207, #33303, #12502, .T. ) ;
#4539=CARTESIAN_POINT ( 'NONE',  ( 11.99999999999999822, 59.46389618802034960, -49.70050353004825894 ) ) ;
#4550=ORIENTED_EDGE ( 'NONE', *, *, #20098, .F. ) ;
#4554=CYLINDRICAL_SURFACE ( 'NONE', #36581, 31.99999999999997868 ) ;
#4556=DIRECTION ( 'NONE',  ( -1.000000000000000000, 0.000000000000000000, -0.000000000000000000 ) ) ;
#4557=CARTESIAN_POINT ( 'NONE',  ( 11.99999999999999822, 0.000000000000000000, 0.000000000000000000 ) ) ;
#4560=DIRECTION ( 'NONE',  ( -1.000000000000000000, -0.000000000000000000, 0.000000000000000000 ) ) ;
#4562=DIRECTION ( 'NONE',  ( 1.000000000000000000, 0.000000000000000000, 0.000000000000000000 ) ) ;
#4564=DIRECTION ( 'NONE',  ( 0.000000000000000000, 0.000000000000000000, 1.000000000000000000 ) ) ;
#4565=VERTEX_POINT ( 'NONE', #17839 ) ;
#4566=VERTEX_POINT ( 'NONE', #1977 ) ;
#4568=CIRCLE ( 'NONE', #18637, 31.99999999999998579 ) ;
#4574=DIRECTION ( 'NONE',  ( -1.000000000000000000, -0.000000000000000000, 0.000000000000000000 ) ) ;
#4575=CYLINDRICAL_SURFACE ( 'NONE', #29508, 31.99999999999998579 ) ;
#4585=EDGE_CURVE ( 'NONE', #2093, #11149, #29008, .T. ) ;
#4586=VERTEX_POINT ( 'NONE', #47233 ) ;
#4589=LINE ( 'NONE', #22944, #2661 ) ;
#4591=ADVANCED_FACE ( 'NONE', ( #13459 ), #43792, .T. ) ;
#4592=CARTESIAN_POINT ( 'NONE',  ( 11.99999999999999822, 18.89407956138257205, 75.16055320797038064 ) ) ;
#4597=CIRCLE ( 'NONE', #7743, 31.99999999999998579 ) ;
#4605=ORIENTED_EDGE ( 'NONE', *, *, #45502, .F. ) ;
#4607=CARTESIAN_POINT ( 'NONE',  ( 11.99999999999999822, 0.000000000000000000, 0.000000000000000000 ) ) ;
#4610=CARTESIAN_POINT ( 'NONE',  ( 11.99999999999999822, -75.16055320797043748, 18.89407956138231270 ) ) ;
#4613=EDGE_CURVE ( 'NONE', #25392, #38067, #43330, .T. ) ;
#4621=DIRECTION ( 'NONE',  ( -1.000000000000000000, 0.000000000000000000, -0.000000000000000000 ) ) ;
#4626=CARTESIAN_POINT ( 'NONE',  ( 15.00000000000000000, -22.67460108101782978, -6.353146135317906840 ) ) ;
#4628=CARTESIAN_POINT ( 'NONE',  ( 11.99999999999999822, 58.39081064771751528, 50.95692526931350841 ) ) ;
#4633=FACE_OUTER_BOUND ( 'NONE', #25604, .T. ) ;
#4635=DIRECTION ( 'NONE',  ( -1.000000000000000000, 0.000000000000000000, -0.000000000000000000 ) ) ;
#4636=ORIENTED_EDGE ( 'NONE', *, *, #2628, .F. ) ;
#4640=DIRECTION ( 'NONE',  ( 0.000000000000000000, 0.000000000000000000, 1.000000000000000000 ) ) ;
#4641=EDGE_CURVE ( 'NONE', #34700, #41319, #6342, .T. ) ;
#4642=DIRECTION ( 'NONE',  ( 0.000000000000000000, 0.000000000000000000, 1.000000000000000000 ) ) ;
#4645=EDGE_CURVE ( 'NONE', #41493, #45717, #46764, .T. ) ;
#4648=ORIENTED_EDGE ( 'NONE', *, *, #12597, .F. ) ;
#4649=ORIENTED_EDGE ( 'NONE', *, *, #17498, .T. ) ;
#4656=ORIENTED_EDGE ( 'NONE', *, *, #26930, .F. ) ;
#4663=DIRECTION ( 'NONE',  ( 0.000000000000000000, 0.000000000000000000, 1.000000000000000000 ) ) ;
#4666=DIRECTION ( 'NONE',  ( -1.000000000000000000, 0.000000000000000000, 0.000000000000000000 ) ) ;
#4667=EDGE_LOOP ( 'NONE', ( #12438, #5813, #8662, #5432 ) ) ;
#4677=CYLINDRICAL_SURFACE ( 'NONE', #38793, 31.99999999999998579 ) ;
#4682=DIRECTION ( 'NONE',  ( 1.000000000000000000, 0.000000000000000000, 0.000000000000000000 ) ) ;
#4685=EDGE_CURVE ( 'NONE', #15795, #17381, #8704, .T. ) ;
#4688=DIRECTION ( 'NONE',  ( -1.000000000000000000, 0.000000000000000000, 0.000000000000000000 ) ) ;
#4689=ORIENTED_EDGE ( 'NONE', *, *, #21256, .F. ) ;
#4691=DIRECTION ( 'NONE',  ( 0.000000000000000000, 0.6691306063588570163, -0.7431448254773953543 ) ) ;
#4696=ORIENTED_EDGE ( 'NONE', *, *, #42211, .F. ) ;
#4697=AXIS2_PLACEMENT_3D ( 'NONE', #24961, #3401, #21541 ) ;
#4699=VECTOR ( 'NONE', #46136, 1000.000000000000000 ) ;
#4702=VECTOR ( 'NONE', #22291, 1000.000000000000000 ) ;
#4704=DIRECTION ( 'NONE',  ( -1.000000000000000000, -0.000000000000000000, 0.000000000000000000 ) ) ;
#4706=EDGE_CURVE ( 'NONE', #45468, #37953, #36830, .T. ) ;
#4708=CIRCLE ( 'NONE', #4741, 77.49899999999999523 ) ;
#4710=DIRECTION ( 'NONE',  ( 0.000000000000000000, -0.8660254037844427044, -0.4999999999999931166 ) ) ;
#4711=ORIENTED_EDGE ( 'NONE', *, *, #17097, .T. ) ;
#4713=CARTESIAN_POINT ( 'NONE',  ( 11.99999999999999822, 15.33399622253600647, -80.55351364060571484 ) ) ;
#4714=ORIENTED_EDGE ( 'NONE', *, *, #35231, .F. ) ;
#4716=FACE_OUTER_BOUND ( 'NONE', #20484, .T. ) ;
#4719=DIRECTION ( 'NONE',  ( 0.000000000000000000, 0.000000000000000000, 1.000000000000000000 ) ) ;
#4723=DIRECTION ( 'NONE',  ( 1.000000000000000000, 0.000000000000000000, 0.000000000000000000 ) ) ;
#4728=EDGE_LOOP ( 'NONE', ( #19114, #31430, #37216, #40262 ) ) ;
#4730=CIRCLE ( 'NONE', #3138, 77.49899999999999523 ) ;
#4731=ORIENTED_EDGE ( 'NONE', *, *, #33585, .F. ) ;
#4734=CARTESIAN_POINT ( 'NONE',  ( 11.99999999999999822, -71.91182617369207719, 28.89263327155721228 ) ) ;
#4738=CYLINDRICAL_SURFACE ( 'NONE', #13548, 77.49899999999999523 ) ;
#4741=AXIS2_PLACEMENT_3D ( 'NONE', #24072, #34572, #31428 ) ;
#4749=EDGE_CURVE ( 'NONE', #27075, #18133, #68, .T. ) ;
#4757=VERTEX_POINT ( 'NONE', #22908 ) ;
#4762=EDGE_CURVE ( 'NONE', #28804, #42832, #16063, .T. ) ;
#4763=EDGE_CURVE ( 'NONE', #18839, #42776, #31380, .T. ) ;
#4768=AXIS2_PLACEMENT_3D ( 'NONE', #20539, #16171, #24457 ) ;
#4774=AXIS2_PLACEMENT_3D ( 'NONE', #19582, #42859, #23284 ) ;
#4778=CARTESIAN_POINT ( 'NONE',  ( 0.000000000000000000, -75.11764819372145041, -2.946379043147127064 ) ) ;
#4790=VERTEX_POINT ( 'NONE', #44952 ) ;
#4791=DIRECTION ( 'NONE',  ( -1.000000000000000000, 0.000000000000000000, 0.000000000000000000 ) ) ;
#4793=DIRECTION ( 'NONE',  ( 0.000000000000000000, -0.2079116908177664480, -0.9781476007338041345 ) ) ;
#4794=CARTESIAN_POINT ( 'NONE',  ( 15.00000000000000000, -4.261787119644963262, 26.19803753235780164 ) ) ;
#4795=DIRECTION ( 'NONE',  ( 0.000000000000000000, 0.000000000000000000, 1.000000000000000000 ) ) ;
#4798=LINE ( 'NONE', #35129, #48438 ) ;
#4801=CARTESIAN_POINT ( 'NONE',  ( 11.99999999999999822, -73.44644590900043113, -24.73286445877782924 ) ) ;
#4802=CARTESIAN_POINT ( 'NONE',  ( 6.000000000000000000, -76.69515212746036070, 29.01471420065536932 ) ) ;
#4809=EDGE_CURVE ( 'NONE', #21783, #19662, #42010, .T. ) ;
#4811=VECTOR ( 'NONE', #20026, 1000.000000000000000 ) ;
#4812=CARTESIAN_POINT ( 'NONE',  ( 11.99999999999999822, 34.94270380257639630, 74.18225833017902460 ) ) ;
#4813=ADVANCED_FACE ( 'NONE', ( #7512 ), #26351, .T. ) ;
#4816=ORIENTED_EDGE ( 'NONE', *, *, #37750, .F. ) ;
#4817=ADVANCED_FACE ( 'NONE', ( #45194 ), #11661, .T. ) ;
#4818=AXIS2_PLACEMENT_3D ( 'NONE', #29478, #14063, #6482 ) ;
#4825=EDGE_CURVE ( 'NONE', #42048, #34678, #20935, .T. ) ;
#4826=ORIENTED_EDGE ( 'NONE', *, *, #37000, .F. ) ;
#4828=ORIENTED_EDGE ( 'NONE', *, *, #32231, .F. ) ;
#4829=ORIENTED_EDGE ( 'NONE', *, *, #1819, .F. ) ;
#4833=DIRECTION ( 'NONE',  ( 0.000000000000000000, 0.000000000000000000, 1.000000000000000000 ) ) ;
#4835=ORIENTED_EDGE ( 'NONE', *, *, #32063, .T. ) ;
#4840=EDGE_LOOP ( 'NONE', ( #13629, #18206, #12768, #27217 ) ) ;
#4845=DIRECTION ( 'NONE',  ( 0.000000000000000000, 0.9135454576426005335, -0.4067366430758009299 ) ) ;
#4846=ORIENTED_EDGE ( 'NONE', *, *, #3596, .F. ) ;
#4849=DIRECTION ( 'NONE',  ( 0.000000000000000000, -0.3090169943749350168, -0.9510565162951576390 ) ) ;
#4850=VECTOR ( 'NONE', #8509, 1000.000000000000000 ) ;
#4851=VERTEX_POINT ( 'NONE', #27555 ) ;
#4854=CYLINDRICAL_SURFACE ( 'NONE', #28348, 77.49899999999999523 ) ;
#4855=VERTEX_POINT ( 'NONE', #23628 ) ;
#4856=VERTEX_POINT ( 'NONE', #42483 ) ;
#4857=( LENGTH_UNIT ( ) NAMED_UNIT ( * ) SI_UNIT ( .MILLI., .METRE. ) );
#4859=ORIENTED_EDGE ( 'NONE', *, *, #7422, .T. ) ;
#4860=ADVANCED_FACE ( 'NONE', ( #38575 ), #20433, .F. ) ;
#4862=ORIENTED_EDGE ( 'NONE', *, *, #48360, .T. ) ;
#4867=CARTESIAN_POINT ( 'NONE',  ( 6.000000000000000000, 16.65972982745045528, -80.28980883073738539 ) ) ;
#4879=DIRECTION ( 'NONE',  ( 1.000000000000000000, 0.000000000000000000, 0.000000000000000000 ) ) ;
#4884=VERTEX_POINT ( 'NONE', #1856 ) ;
#4897=CIRCLE ( 'NONE', #33829, 31.99999999999998579 ) ;
#4898=CARTESIAN_POINT ( 'NONE',  ( 0.000000000000000000, 0.000000000000000000, 0.000000000000000000 ) ) ;
#4900=AXIS2_PLACEMENT_3D ( 'NONE', #5240, #42686, #13531 ) ;
#4903=ORIENTED_EDGE ( 'NONE', *, *, #35294, .T. ) ;
#4905=EDGE_CURVE ( 'NONE', #3151, #13690, #7938, .T. ) ;
#4907=VERTEX_POINT ( 'NONE', #2097 ) ;
#4909=DIRECTION ( 'NONE',  ( -1.000000000000000000, 0.000000000000000000, 0.000000000000000000 ) ) ;
#4912=EDGE_CURVE ( 'NONE', #38297, #11714, #46398, .T. ) ;
#4917=DIRECTION ( 'NONE',  ( 0.000000000000000000, 0.4539904997395413644, 0.8910065241883706744 ) ) ;
#4919=EDGE_CURVE ( 'NONE', #46849, #14154, #12625, .T. ) ;
#4922=DIRECTION ( 'NONE',  ( 0.000000000000000000, 0.8526401643540897357, 0.5224985647159527957 ) ) ;
#4923=EDGE_LOOP ( 'NONE', ( #21009, #44884, #9654, #329 ) ) ;
#4925=DIRECTION ( 'NONE',  ( 0.000000000000000000, -0.9510565162951510887, 0.3090169943749551673 ) ) ;
#4934=ORIENTED_EDGE ( 'NONE', *, *, #36530, .T. ) ;
#4935=AXIS2_PLACEMENT_3D ( 'NONE', #1508, #16671, #4691 ) ;
#4944=DIRECTION ( 'NONE',  ( 0.000000000000000000, 0.000000000000000000, 1.000000000000000000 ) ) ;
#4948=EDGE_LOOP ( 'NONE', ( #7569, #6269, #20759, #8147 ) ) ;
#4950=ORIENTED_EDGE ( 'NONE', *, *, #36234, .T. ) ;
#4951=CARTESIAN_POINT ( 'NONE',  ( 0.000000000000000000, 0.000000000000000000, 0.000000000000000000 ) ) ;
#4953=EDGE_CURVE ( 'NONE', #28743, #27429, #29743, .T. ) ;
#4954=DIRECTION ( 'NONE',  ( -1.000000000000000000, -0.000000000000000000, -0.000000000000000000 ) ) ;
#4955=CARTESIAN_POINT ( 'NONE',  ( 0.000000000000000000, -30.41916302227164337, 71.27951684758015460 ) ) ;
#4957=DIRECTION ( 'NONE',  ( 0.000000000000000000, 0.000000000000000000, 1.000000000000000000 ) ) ;
#4958=EDGE_CURVE ( 'NONE', #16116, #11391, #4730, .T. ) ;
#4960=EDGE_CURVE ( 'NONE', #5392, #47811, #45923, .T. ) ;
#4965=CARTESIAN_POINT ( 'NONE',  ( 12.00000000000000000, -20.55727247249748757, -16.78983467731284662 ) ) ;
#4969=EDGE_LOOP ( 'NONE', ( #15786, #10000, #21340, #1882 ) ) ;
#4972=DIRECTION ( 'NONE',  ( -1.000000000000000000, 0.000000000000000000, 0.000000000000000000 ) ) ;
#4976=DIRECTION ( 'NONE',  ( -1.000000000000000000, 0.000000000000000000, -0.000000000000000000 ) ) ;
#4985=CARTESIAN_POINT ( 'NONE',  ( 15.00000000000000000, -26.23277895567245466, 4.042438405570107918 ) ) ;
#4988=CIRCLE ( 'NONE', #10425, 31.99999999999998224 ) ;
#4996=AXIS2_PLACEMENT_3D ( 'NONE', #20125, #20857, #27970 ) ;
#5000=ORIENTED_EDGE ( 'NONE', *, *, #269, .F. ) ;
#5001=VERTEX_POINT ( 'NONE', #14563 ) ;
#5003=CARTESIAN_POINT ( 'NONE',  ( 11.99999999999999822, 81.90746397400394585, -3.894527615416972566 ) ) ;
#5004=VERTEX_POINT ( 'NONE', #21653 ) ;
#5009=CIRCLE ( 'NONE', #23001, 77.49899999999999523 ) ;
#5018=CIRCLE ( 'NONE', #38656, 77.49899999999999523 ) ;
#5027=DIRECTION ( 'NONE',  ( 0.000000000000000000, -0.07845909572785224328, 0.9969173337331274087 ) ) ;
#5029=CARTESIAN_POINT ( 'NONE',  ( 15.00000000000000000, 14.60985201121729737, 18.46759930825687235 ) ) ;
#5033=DIRECTION ( 'NONE',  ( 0.000000000000000000, 0.2334453638558990629, 0.9723699203976782224 ) ) ;
#5034=ORIENTED_EDGE ( 'NONE', *, *, #44437, .F. ) ;
#5037=CARTESIAN_POINT ( 'NONE',  ( 11.99999999999999822, -51.02545421589363883, 55.20638768913742922 ) ) ;
#5044=EDGE_LOOP ( 'NONE', ( #40600, #40480, #20302, #10736 ) ) ;
#5055=DIRECTION ( 'NONE',  ( 0.000000000000000000, 0.000000000000000000, 1.000000000000000000 ) ) ;
#5056=CIRCLE ( 'NONE', #19080, 77.49900000000000944 ) ;
#5058=DIRECTION ( 'NONE',  ( -0.000000000000000000, -0.6691306063588670083, -0.7431448254773863615 ) ) ;
#5060=FACE_OUTER_BOUND ( 'NONE', #35917, .T. ) ;
#5065=CARTESIAN_POINT ( 'NONE',  ( 11.99999999999999822, -20.41045688087876897, 72.35160999960810102 ) ) ;
#5066=CYLINDRICAL_SURFACE ( 'NONE', #16258, 82.00000000000000000 ) ;
#5084=ORIENTED_EDGE ( 'NONE', *, *, #34515, .F. ) ;
#5086=ADVANCED_FACE ( 'NONE', ( #44169 ), #10877, .T. ) ;
#5088=CYLINDRICAL_SURFACE ( 'NONE', #21177, 77.49899999999999523 ) ;
#5089=ORIENTED_EDGE ( 'NONE', *, *, #19989, .F. ) ;
#5090=CARTESIAN_POINT ( 'NONE',  ( 11.99999999999999822, -72.35160999960801576, -20.41045688087902121 ) ) ;
#5093=AXIS2_PLACEMENT_3D ( 'NONE', #9210, #24144, #11261 ) ;
#5094=ORIENTED_EDGE ( 'NONE', *, *, #9017, .T. ) ;
#5096=EDGE_CURVE ( 'NONE', #39585, #4021, #47796, .T. ) ;
#5099=DIRECTION ( 'NONE',  ( 0.000000000000000000, 0.5877852522924743583, -0.8090169943749465631 ) ) ;
#5106=CIRCLE ( 'NONE', #27784, 77.49899999999999523 ) ;
#5108=VECTOR ( 'NONE', #41159, 1000.000000000000000 ) ;
#5110=EDGE_CURVE ( 'NONE', #4856, #36554, #18098, .T. ) ;
#5115=DIRECTION ( 'NONE',  ( 0.000000000000000000, 0.000000000000000000, 1.000000000000000000 ) ) ;
#5119=CARTESIAN_POINT ( 'NONE',  ( 11.99999999999999822, -76.41127070299280888, 12.93880638057290788 ) ) ;
#5120=VECTOR ( 'NONE', #33028, 1000.000000000000000 ) ;
#5124=EDGE_CURVE ( 'NONE', #33807, #33795, #30630, .T. ) ;
#5128=VERTEX_POINT ( 'NONE', #43460 ) ;
#5138=AXIS2_PLACEMENT_3D ( 'NONE', #13287, #35563, #28209 ) ;
#5140=VECTOR ( 'NONE', #37958, 1000.000000000000000 ) ;
#5149=CIRCLE ( 'NONE', #5926, 77.49900000000000944 ) ;
#5151=AXIS2_PLACEMENT_3D ( 'NONE', #26782, #15770, #34352 ) ;
#5160=CARTESIAN_POINT ( 'NONE',  ( 11.99999999999999822, 0.000000000000000000, 0.000000000000000000 ) ) ;
#5162=DIRECTION ( 'NONE',  ( -1.000000000000000000, 0.000000000000000000, -0.000000000000000000 ) ) ;
#5167=DIRECTION ( 'NONE',  ( 0.000000000000000000, 0.000000000000000000, 1.000000000000000000 ) ) ;
#5170=CARTESIAN_POINT ( 'NONE',  ( 0.000000000000000000, -49.70050353004846500, -59.46389618802017907 ) ) ;
#5171=ORIENTED_EDGE ( 'NONE', *, *, #41777, .T. ) ;
#5172=VERTEX_POINT ( 'NONE', #811 ) ;
#5173=LINE ( 'NONE', #992, #32266 ) ;
#5174=CARTESIAN_POINT ( 'NONE',  ( 11.99999999999999822, -63.18004540533059554, 44.88180994100355292 ) ) ;
#5175=CARTESIAN_POINT ( 'NONE',  ( -10.00000000000000000, 0.000000000000000000, 0.000000000000000000 ) ) ;
#5177=DIRECTION ( 'NONE',  ( -1.000000000000000000, -0.000000000000000000, 0.000000000000000000 ) ) ;
#5180=CARTESIAN_POINT ( 'NONE',  ( 11.99999999999999822, 2.946379043147425492, -75.11764819372145041 ) ) ;
#5188=CARTESIAN_POINT ( 'NONE',  ( 15.00000000000000000, -14.54903810567644484, 22.19967320028775504 ) ) ;
#5189=CARTESIAN_POINT ( 'NONE',  ( 11.99999999999999822, 0.000000000000000000, 0.000000000000000000 ) ) ;
#5190=ADVANCED_FACE ( 'NONE', ( #22851 ), #15035, .T. ) ;
#5194=EDGE_LOOP ( 'NONE', ( #9194, #1877, #34528, #25970 ) ) ;
#5206=AXIS2_PLACEMENT_3D ( 'NONE', #8585, #34777, #1263 ) ;
#5207=VERTEX_POINT ( 'NONE', #15514 ) ;
#5210=ORIENTED_EDGE ( 'NONE', *, *, #29303, .T. ) ;
#5211=CARTESIAN_POINT ( 'NONE',  ( 11.99999999999999822, 30.41916302227216562, -71.27951684757994144 ) ) ;
#5220=EDGE_CURVE ( 'NONE', #43680, #34540, #34108, .T. ) ;
#5222=CARTESIAN_POINT ( 'NONE',  ( 11.99999999999999822, 0.000000000000000000, 0.000000000000000000 ) ) ;
#5223=DIRECTION ( 'NONE',  ( -1.000000000000000000, 0.000000000000000000, 0.000000000000000000 ) ) ;
#5224=DIRECTION ( 'NONE',  ( -1.000000000000000000, -0.000000000000000000, 0.000000000000000000 ) ) ;
#5235=DIRECTION ( 'NONE',  ( 0.000000000000000000, 0.000000000000000000, 1.000000000000000000 ) ) ;
#5240=CARTESIAN_POINT ( 'NONE',  ( 11.99999999999999822, 0.000000000000000000, 0.000000000000000000 ) ) ;
#5242=VECTOR ( 'NONE', #44693, 1000.000000000000000 ) ;
#5243=DIRECTION ( 'NONE',  ( -1.000000000000000000, -0.000000000000000000, 0.000000000000000000 ) ) ;
#5249=EDGE_LOOP ( 'NONE', ( #19968, #48396, #21594, #26137 ) ) ;
#5255=EDGE_CURVE ( 'NONE', #18838, #21898, #45606, .T. ) ;
#5257=EDGE_CURVE ( 'NONE', #6838, #20356, #12101, .T. ) ;
#5260=CIRCLE ( 'NONE', #25568, 31.99999999999998224 ) ;
#5264=EDGE_CURVE ( 'NONE', #21229, #27047, #11797, .T. ) ;
#5272=AXIS2_PLACEMENT_3D ( 'NONE', #36646, #21726, #40570 ) ;
#5273=DIRECTION ( 'NONE',  ( 0.000000000000000000, 0.000000000000000000, 1.000000000000000000 ) ) ;
#5274=EDGE_CURVE ( 'NONE', #20737, #29586, #26041, .T. ) ;
#5276=DIRECTION ( 'NONE',  ( -1.000000000000000000, 0.000000000000000000, 0.000000000000000000 ) ) ;
#5282=DIRECTION ( 'NONE',  ( 0.000000000000000000, 0.000000000000000000, -1.000000000000000000 ) ) ;
#5289=CARTESIAN_POINT ( 'NONE',  ( 0.000000000000000000, 0.000000000000000000, 0.000000000000000000 ) ) ;
#5295=DIRECTION ( 'NONE',  ( 0.000000000000000000, -0.5877852522924624790, -0.8090169943749551118 ) ) ;
#5299=CARTESIAN_POINT ( 'NONE',  ( 0.000000000000000000, 8.830959090342393125, 74.65491531819122883 ) ) ;
#5301=EDGE_CURVE ( 'NONE', #4198, #20488, #42423, .T. ) ;
#5309=VERTEX_POINT ( 'NONE', #1056 ) ;
#5311=AXIS2_PLACEMENT_3D ( 'NONE', #44127, #24372, #46667 ) ;
#5312=ORIENTED_EDGE ( 'NONE', *, *, #28749, .T. ) ;
#5317=ORIENTED_EDGE ( 'NONE', *, *, #45644, .F. ) ;
#5322=ADVANCED_FACE ( 'NONE', ( #28214 ), #35074, .T. ) ;
#5323=CIRCLE ( 'NONE', #14716, 31.99999999999998579 ) ;
#5325=CYLINDRICAL_SURFACE ( 'NONE', #46073, 31.99999999999998579 ) ;
#5329=LINE ( 'NONE', #17053, #46751 ) ;
#5334=DIRECTION ( 'NONE',  ( 0.000000000000000000, 0.000000000000000000, 1.000000000000000000 ) ) ;
#5340=DIRECTION ( 'NONE',  ( 0.000000000000000000, -0.8660254037844363761, 0.5000000000000039968 ) ) ;
#5341=VERTEX_POINT ( 'NONE', #42678 ) ;
#5345=DIRECTION ( 'NONE',  ( 0.000000000000000000, -0.6691306063588586817, 0.7431448254773939111 ) ) ;
#5348=FACE_OUTER_BOUND ( 'NONE', #44783, .T. ) ;
#5350=ORIENTED_EDGE ( 'NONE', *, *, #28932, .T. ) ;
#5353=VERTEX_POINT ( 'NONE', #23826 ) ;
#5355=DIRECTION ( 'NONE',  ( 0.000000000000000000, -0.2334453638558922350, -0.9723699203976797767 ) ) ;
#5360=EDGE_CURVE ( 'NONE', #4198, #6843, #25858, .T. ) ;
#5368=CARTESIAN_POINT ( 'NONE',  ( 15.00000000000000000, -13.04903810567675393, -19.60159698893424718 ) ) ;
#5371=AXIS2_PLACEMENT_3D ( 'NONE', #2610, #10712, #48146 ) ;
#5372=CARTESIAN_POINT ( 'NONE',  ( 11.99999999999999822, -17.28742895386031719, -75.54627589209962935 ) ) ;
#5375=ORIENTED_EDGE ( 'NONE', *, *, #44430, .T. ) ;
#5381=ORIENTED_EDGE ( 'NONE', *, *, #46551, .F. ) ;
#5382=ORIENTED_EDGE ( 'NONE', *, *, #3068, .F. ) ;
#5388=ORIENTED_EDGE ( 'NONE', *, *, #33571, .T. ) ;
#5392=VERTEX_POINT ( 'NONE', #34573 ) ;
#5393=DIRECTION ( 'NONE',  ( 0.000000000000000000, -0.9781476007338070211, -0.2079116908177532363 ) ) ;
#5395=CARTESIAN_POINT ( 'NONE',  ( 0.000000000000000000, 0.000000000000000000, 0.000000000000000000 ) ) ;
#5401=CARTESIAN_POINT ( 'NONE',  ( 11.99999999999999822, 8.830959090343430518, -74.65491531819107252 ) ) ;
#5402=LINE ( 'NONE', #1987, #2743 ) ;
#5404=AXIS2_PLACEMENT_3D ( 'NONE', #8982, #45955, #2130 ) ;
#5405=DIRECTION ( 'NONE',  ( 0.000000000000000000, 0.000000000000000000, 1.000000000000000000 ) ) ;
#5414=DIRECTION ( 'NONE',  ( 0.000000000000000000, 0.000000000000000000, 1.000000000000000000 ) ) ;
#5417=ADVANCED_FACE ( 'NONE', ( #27262 ), #30945, .T. ) ;
#5418=DIRECTION ( 'NONE',  ( -0.000000000000000000, 0.9510565162951539753, 0.3090169943749461745 ) ) ;
#5420=CARTESIAN_POINT ( 'NONE',  ( -10.00000000000000000, 0.000000000000000000, 0.000000000000000000 ) ) ;
#5421=ADVANCED_FACE ( 'NONE', ( #20148 ), #16480, .T. ) ;
#5426=EDGE_CURVE ( 'NONE', #25415, #16364, #23523, .T. ) ;
#5427=CYLINDRICAL_SURFACE ( 'NONE', #33096, 82.00000000000000000 ) ;
#5429=EDGE_CURVE ( 'NONE', #40000, #30381, #8663, .T. ) ;
#5430=CARTESIAN_POINT ( 'NONE',  ( 6.000000000000000000, 21.60688246758586928, 79.10210256391376049 ) ) ;
#5431=DIRECTION ( 'NONE',  ( 0.000000000000000000, 0.000000000000000000, 1.000000000000000000 ) ) ;
#5432=ORIENTED_EDGE ( 'NONE', *, *, #4912, .F. ) ;
#5439=DIRECTION ( 'NONE',  ( -1.000000000000000000, -0.000000000000000000, 0.000000000000000000 ) ) ;
#5442=AXIS2_PLACEMENT_3D ( 'NONE', #26286, #39836, #33385 ) ;
#5455=EDGE_LOOP ( 'NONE', ( #22838, #41930, #17871, #13620 ) ) ;
#5460=DIRECTION ( 'NONE',  ( 0.000000000000000000, 0.000000000000000000, 1.000000000000000000 ) ) ;
#5462=CARTESIAN_POINT ( 'NONE',  ( 11.99999999999999822, -55.38113227695820484, 54.21277698773656084 ) ) ;
#5463=LINE ( 'NONE', #46832, #39327 ) ;
#5470=DIRECTION ( 'NONE',  ( 0.000000000000000000, 0.000000000000000000, -1.000000000000000000 ) ) ;
#5472=DIRECTION ( 'NONE',  ( 0.000000000000000000, 0.000000000000000000, 1.000000000000000000 ) ) ;
#5474=VECTOR ( 'NONE', #9340, 1000.000000000000000 ) ;
#5484=ORIENTED_EDGE ( 'NONE', *, *, #22872, .T. ) ;
#5489=ORIENTED_EDGE ( 'NONE', *, *, #47854, .F. ) ;
#5492=VERTEX_POINT ( 'NONE', #47061 ) ;
#5496=AXIS2_PLACEMENT_3D ( 'NONE', #13507, #47735, #9578 ) ;
#5498=LINE ( 'NONE', #43185, #34779 ) ;
#5504=ORIENTED_EDGE ( 'NONE', *, *, #23270, .T. ) ;
#5507=CARTESIAN_POINT ( 'NONE',  ( 0.000000000000000000, 0.000000000000000000, 0.000000000000000000 ) ) ;
#5508=AXIS2_PLACEMENT_3D ( 'NONE', #17676, #47759, #29165 ) ;
#5510=EDGE_LOOP ( 'NONE', ( #14075, #42291, #38865, #6032 ) ) ;
#5514=ORIENTED_EDGE ( 'NONE', *, *, #36182, .F. ) ;
#5520=DIRECTION ( 'NONE',  ( 0.000000000000000000, 0.5877852522924742473, -0.8090169943749466741 ) ) ;
#5523=DIRECTION ( 'NONE',  ( -1.000000000000000000, -0.000000000000000000, 0.000000000000000000 ) ) ;
#5525=CARTESIAN_POINT ( 'NONE',  ( 6.000000000000000000, 40.65526001592611749, 71.21200624218811015 ) ) ;
#5533=DIRECTION ( 'NONE',  ( -1.000000000000000000, 0.000000000000000000, -0.000000000000000000 ) ) ;
#5537=DIRECTION ( 'NONE',  ( 1.000000000000000000, 0.000000000000000000, -0.000000000000000000 ) ) ;
#5538=EDGE_LOOP ( 'NONE', ( #39001, #32288, #10362, #8761 ) ) ;
#5544=ORIENTED_EDGE ( 'NONE', *, *, #9725, .F. ) ;
#5546=DIRECTION ( 'NONE',  ( -1.000000000000000000, 0.000000000000000000, -0.000000000000000000 ) ) ;
#5547=AXIS2_PLACEMENT_3D ( 'NONE', #7132, #44341, #14487 ) ;
#5556=CARTESIAN_POINT ( 'NONE',  ( 11.99999999999999822, -34.44570377933549565, -69.42325613327476219 ) ) ;
#5558=ORIENTED_EDGE ( 'NONE', *, *, #10129, .T. ) ;
#5560=ORIENTED_EDGE ( 'NONE', *, *, #35855, .F. ) ;
#5562=LINE ( 'NONE', #6061, #13365 ) ;
#5565=DIRECTION ( 'NONE',  ( 0.000000000000000000, -0.6494480483301904306, 0.7604059656000252687 ) ) ;
#5567=AXIS2_PLACEMENT_3D ( 'NONE', #15335, #45182, #41039 ) ;
#5570=CARTESIAN_POINT ( 'NONE',  ( 11.99999999999999822, 8.830959090343430518, -74.65491531819107252 ) ) ;
#5571=VERTEX_POINT ( 'NONE', #40926 ) ;
#5572=ORIENTED_EDGE ( 'NONE', *, *, #20834, .T. ) ;
#5573=CARTESIAN_POINT ( 'NONE',  ( -10.00000000000000000, 0.000000000000000000, 0.000000000000000000 ) ) ;
#5574=VECTOR ( 'NONE', #4666, 1000.000000000000000 ) ;
#5576=DIRECTION ( 'NONE',  ( 0.000000000000000000, 0.000000000000000000, 1.000000000000000000 ) ) ;
#5577=EDGE_CURVE ( 'NONE', #12155, #4884, #28427, .T. ) ;
#5582=ADVANCED_FACE ( 'NONE', ( #22329 ), #18869, .T. ) ;
#5583=VERTEX_POINT ( 'NONE', #41410 ) ;
#5584=AXIS2_PLACEMENT_3D ( 'NONE', #29099, #24476, #40136 ) ;
#5585=VERTEX_POINT ( 'NONE', #30398 ) ;
#5589=CARTESIAN_POINT ( 'NONE',  ( 0.000000000000000000, 10.30890764327501152, -81.34940948281325745 ) ) ;
#5591=CIRCLE ( 'NONE', #14995, 31.99999999999998934 ) ;
#5594=DIRECTION ( 'NONE',  ( -1.000000000000000000, 0.000000000000000000, 0.000000000000000000 ) ) ;
#5598=EDGE_CURVE ( 'NONE', #4110, #38297, #25980, .T. ) ;
#5601=CARTESIAN_POINT ( 'NONE',  ( 0.000000000000000000, 0.000000000000000000, 0.000000000000000000 ) ) ;
#5604=CARTESIAN_POINT ( 'NONE',  ( 0.000000000000000000, 55.38113227695783536, 54.21277698773694453 ) ) ;
#5614=AXIS2_PLACEMENT_3D ( 'NONE', #43684, #21882, #25789 ) ;
#5620=VECTOR ( 'NONE', #34691, 1000.000000000000000 ) ;
#5623=VERTEX_POINT ( 'NONE', #11555 ) ;
#5625=ADVANCED_FACE ( 'NONE', ( #4455 ), #34284, .T. ) ;
#5627=CARTESIAN_POINT ( 'NONE',  ( 11.99999999999999822, 0.000000000000000000, 0.000000000000000000 ) ) ;
#5643=ORIENTED_EDGE ( 'NONE', *, *, #37797, .F. ) ;
#5646=ORIENTED_EDGE ( 'NONE', *, *, #8069, .F. ) ;
#5647=CYLINDRICAL_SURFACE ( 'NONE', #19109, 31.99999999999998579 ) ;
#5650=CARTESIAN_POINT ( 'NONE',  ( 11.99999999999999822, 0.000000000000000000, 0.000000000000000000 ) ) ;
#5651=VECTOR ( 'NONE', #41237, 1000.000000000000000 ) ;
#5654=EDGE_CURVE ( 'NONE', #19037, #14039, #22563, .T. ) ;
#5658=CARTESIAN_POINT ( 'NONE',  ( 0.000000000000000000, -55.20638768913724448, -51.02545421589383068 ) ) ;
#5660=CARTESIAN_POINT ( 'NONE',  ( 11.99999999999999822, -77.49459641780886443, 0.8261519478428549501 ) ) ;
#5668=CARTESIAN_POINT ( 'NONE',  ( 15.00000000000000000, -23.29833615347104470, 3.418703333116808629 ) ) ;
#5670=CARTESIAN_POINT ( 'NONE',  ( 11.99999999999999822, 31.47745569255140552, 68.26794271651274926 ) ) ;
#5677=LINE ( 'NONE', #9342, #39374 ) ;
#5678=ORIENTED_EDGE ( 'NONE', *, *, #29615, .T. ) ;
#5680=AXIS2_PLACEMENT_3D ( 'NONE', #31190, #45142, #45874 ) ;
#5682=AXIS2_PLACEMENT_3D ( 'NONE', #37117, #3589, #41054 ) ;
#5687=EDGE_CURVE ( 'NONE', #17817, #26988, #23739, .T. ) ;
#5690=EDGE_CURVE ( 'NONE', #13195, #2592, #45812, .T. ) ;
#5691=CARTESIAN_POINT ( 'NONE',  ( 0.000000000000000000, -74.74816331893404708, -33.71516098798818462 ) ) ;
#5692=DIRECTION ( 'NONE',  ( 0.000000000000000000, -0.9510565162951503115, 0.3090169943749573878 ) ) ;
#5697=ORIENTED_EDGE ( 'NONE', *, *, #36367, .T. ) ;
#5699=DIRECTION ( 'NONE',  ( -1.000000000000000000, -0.000000000000000000, -0.000000000000000000 ) ) ;
#5700=VERTEX_POINT ( 'NONE', #46048 ) ;
#5706=AXIS2_PLACEMENT_3D ( 'NONE', #39512, #10353, #25270 ) ;
#5707=FACE_OUTER_BOUND ( 'NONE', #9682, .T. ) ;
#5715=EDGE_CURVE ( 'NONE', #18510, #39232, #16421, .T. ) ;
#5716=DIRECTION ( 'NONE',  ( 0.000000000000000000, 0.000000000000000000, -1.000000000000000000 ) ) ;
#5726=CARTESIAN_POINT ( 'NONE',  ( 15.00000000000000000, -14.54903810567644484, 22.19967320028775504 ) ) ;
#5727=EDGE_LOOP ( 'NONE', ( #17634, #31035, #39140, #28125 ) ) ;
#5731=ORIENTED_EDGE ( 'NONE', *, *, #46316, .T. ) ;
#5732=EDGE_CURVE ( 'NONE', #25011, #5981, #26859, .T. ) ;
#5734=FACE_OUTER_BOUND ( 'NONE', #32633, .T. ) ;
#5736=AXIS2_PLACEMENT_3D ( 'NONE', #9816, #44064, #10544 ) ;
#5737=EDGE_LOOP ( 'NONE', ( #9581, #5000, #46264, #37084 ) ) ;
#5739=VECTOR ( 'NONE', #36939, 1000.000000000000000 ) ;
#5740=CARTESIAN_POINT ( 'NONE',  ( 15.00000000000000000, 18.84667830672605859, 18.68964196561243796 ) ) ;
#5741=ADVANCED_FACE ( 'NONE', ( #20092 ), #15944, .T. ) ;
#5743=AXIS2_PLACEMENT_3D ( 'NONE', #11044, #44335, #33320 ) ;
#5752=ADVANCED_FACE ( 'NONE', ( #16908 ), #34774, .T. ) ;
#5753=DIRECTION ( 'NONE',  ( -1.000000000000000000, 0.000000000000000000, 0.000000000000000000 ) ) ;
#5760=DIRECTION ( 'NONE',  ( -1.000000000000000000, -0.000000000000000000, -0.000000000000000000 ) ) ;
#5761=ORIENTED_EDGE ( 'NONE', *, *, #40237, .F. ) ;
#5763=VECTOR ( 'NONE', #5177, 1000.000000000000000 ) ;
#5765=VECTOR ( 'NONE', #4704, 1000.000000000000000 ) ;
#5768=DIRECTION ( 'NONE',  ( -1.000000000000000000, -0.000000000000000000, 0.000000000000000000 ) ) ;
#5770=AXIS2_PLACEMENT_3D ( 'NONE', #14939, #30840, #7824 ) ;
#5775=DIRECTION ( 'NONE',  ( -1.000000000000000000, -0.000000000000000000, -0.000000000000000000 ) ) ;
#5777=VERTEX_POINT ( 'NONE', #39177 ) ;
#5793=VERTEX_POINT ( 'NONE', #1991 ) ;
#5796=CARTESIAN_POINT ( 'NONE',  ( 0.000000000000000000, 16.65972982745045528, -80.28980883073738539 ) ) ;
#5798=ORIENTED_EDGE ( 'NONE', *, *, #3741, .F. ) ;
#5799=ORIENTED_EDGE ( 'NONE', *, *, #29284, .F. ) ;
#5802=CIRCLE ( 'NONE', #12064, 31.99999999999998579 ) ;
#5804=AXIS2_PLACEMENT_3D ( 'NONE', #8544, #26441, #11273 ) ;
#5806=ORIENTED_EDGE ( 'NONE', *, *, #16234, .T. ) ;
#5807=AXIS2_PLACEMENT_3D ( 'NONE', #41210, #37517, #34085 ) ;
#5811=DIRECTION ( 'NONE',  ( 0.000000000000000000, -0.9135454576426055295, -0.4067366430757899942 ) ) ;
#5812=ORIENTED_EDGE ( 'NONE', *, *, #11873, .F. ) ;
#5813=ORIENTED_EDGE ( 'NONE', *, *, #31030, .F. ) ;
#5819=AXIS2_PLACEMENT_3D ( 'NONE', #18337, #28869, #24958 ) ;
#5823=ORIENTED_EDGE ( 'NONE', *, *, #1501, .T. ) ;
#5824=CARTESIAN_POINT ( 'NONE',  ( -10.00000000000000000, 0.000000000000000000, 0.000000000000000000 ) ) ;
#5825=ORIENTED_EDGE ( 'NONE', *, *, #23074, .T. ) ;
#5829=DIRECTION ( 'NONE',  ( 0.000000000000000000, 0.000000000000000000, 1.000000000000000000 ) ) ;
#5835=CARTESIAN_POINT ( 'NONE',  ( 11.99999999999999822, 81.34940948281349904, -10.30890764327296161 ) ) ;
#5840=ORIENTED_EDGE ( 'NONE', *, *, #33575, .T. ) ;
#5841=CIRCLE ( 'NONE', #39449, 31.99999999999998934 ) ;
#5842=CARTESIAN_POINT ( 'NONE',  ( 6.000000000000000000, 3.894527615419050903, -81.90746397400384637 ) ) ;
#5843=ORIENTED_EDGE ( 'NONE', *, *, #27190, .T. ) ;
#5845=CARTESIAN_POINT ( 'NONE',  ( 11.99999999999999822, 77.19088730480524418, 6.903761155838049390 ) ) ;
#5848=CARTESIAN_POINT ( 'NONE',  ( 5.999999999999999112, 63.97538442413498672, -51.29473840253155004 ) ) ;
#5849=AXIS2_PLACEMENT_3D ( 'NONE', #31087, #23718, #9040 ) ;
#5850=EDGE_CURVE ( 'NONE', #29983, #25935, #1736, .T. ) ;
#5853=ORIENTED_EDGE ( 'NONE', *, *, #22758, .T. ) ;
#5859=ORIENTED_EDGE ( 'NONE', *, *, #4960, .T. ) ;
#5863=VECTOR ( 'NONE', #12303, 1000.000000000000000 ) ;
#5864=ADVANCED_FACE ( 'NONE', ( #29110 ), #21047, .T. ) ;
#5867=EDGE_CURVE ( 'NONE', #43255, #34359, #2439, .T. ) ;
#5868=ORIENTED_EDGE ( 'NONE', *, *, #20704, .F. ) ;
#5873=ORIENTED_EDGE ( 'NONE', *, *, #2453, .T. ) ;
#5879=CARTESIAN_POINT ( 'NONE',  ( 11.99999999999999822, -12.93880638057369659, 76.41127070299266677 ) ) ;
#5889=DIRECTION ( 'NONE',  ( -1.000000000000000000, -0.000000000000000000, -0.000000000000000000 ) ) ;
#5891=CARTESIAN_POINT ( 'NONE',  ( 11.99999999999999822, -63.18004540532995605, -44.88180994100445531 ) ) ;
#5893=DIRECTION ( 'NONE',  ( 0.000000000000000000, 0.000000000000000000, -1.000000000000000000 ) ) ;
#5894=DIRECTION ( 'NONE',  ( -1.000000000000000000, 0.000000000000000000, 0.000000000000000000 ) ) ;
#5895=ORIENTED_EDGE ( 'NONE', *, *, #43508, .T. ) ;
#5900=DIRECTION ( 'NONE',  ( -1.000000000000000000, 0.000000000000000000, 0.000000000000000000 ) ) ;
#5902=CARTESIAN_POINT ( 'NONE',  ( 11.99999999999999822, -65.59268652807237743, 36.72794159290217664 ) ) ;
#5903=CARTESIAN_POINT ( 'NONE',  ( 11.99999999999999822, -20.40083707022935400, 72.35432306680478121 ) ) ;
#5904=CYLINDRICAL_SURFACE ( 'NONE', #24764, 82.00000000000000000 ) ;
#5910=VECTOR ( 'NONE', #14434, 1000.000000000000000 ) ;
#5912=DIRECTION ( 'NONE',  ( -1.000000000000000000, -0.000000000000000000, -0.000000000000000000 ) ) ;
#5914=LINE ( 'NONE', #39194, #20232 ) ;
#5918=VERTEX_POINT ( 'NONE', #13720 ) ;
#5920=VERTEX_POINT ( 'NONE', #17616 ) ;
#5921=ADVANCED_FACE ( 'NONE', ( #39679 ), #28649, .T. ) ;
#5925=VERTEX_POINT ( 'NONE', #25191 ) ;
#5926=AXIS2_PLACEMENT_3D ( 'NONE', #6560, #21491, #47195 ) ;
#5927=DIRECTION ( 'NONE',  ( 0.000000000000000000, 0.1564344650402242909, 0.9876883405951387696 ) ) ;
#5929=ORIENTED_EDGE ( 'NONE', *, *, #19813, .F. ) ;
#5931=CARTESIAN_POINT ( 'NONE',  ( 11.99999999999999822, -68.27212725128298132, 31.46837873494953541 ) ) ;
#5937=EDGE_CURVE ( 'NONE', #44520, #26821, #25304, .T. ) ;
#5939=DIRECTION ( 'NONE',  ( -1.000000000000000000, -0.000000000000000000, 0.000000000000000000 ) ) ;
#5945=CIRCLE ( 'NONE', #33282, 31.99999999999998579 ) ;
#5946=CARTESIAN_POINT ( 'NONE',  ( 11.99999999999999822, 66.50666863322055633, -39.78640506895536078 ) ) ;
#5948=LINE ( 'NONE', #21329, #18310 ) ;
#5949=CARTESIAN_POINT ( 'NONE',  ( 15.00000000000000000, 23.59884966291521380, -12.14883922797262805 ) ) ;
#5950=EDGE_CURVE ( 'NONE', #15783, #22304, #35485, .T. ) ;
#5951=FACE_OUTER_BOUND ( 'NONE', #23753, .T. ) ;
#5954=ORIENTED_EDGE ( 'NONE', *, *, #8328, .F. ) ;
#5968=DIRECTION ( 'NONE',  ( -1.000000000000000000, -0.000000000000000000, 0.000000000000000000 ) ) ;
#5969=AXIS2_PLACEMENT_3D ( 'NONE', #27634, #35701, #1450 ) ;
#5974=CARTESIAN_POINT ( 'NONE',  ( -10.00000000000000000, 0.000000000000000000, 0.000000000000000000 ) ) ;
#5978=CARTESIAN_POINT ( 'NONE',  ( 11.99999999999999822, 0.000000000000000000, 0.000000000000000000 ) ) ;
#5981=VERTEX_POINT ( 'NONE', #40862 ) ;
#5991=CARTESIAN_POINT ( 'NONE',  ( 11.99999999999999822, -70.53064760720297954, -26.01480285779911839 ) ) ;
#5992=AXIS2_PLACEMENT_3D ( 'NONE', #9320, #35511, #12524 ) ;
#5994=AXIS2_PLACEMENT_3D ( 'NONE', #16409, #23502, #38937 ) ;
#5996=EDGE_CURVE ( 'NONE', #4855, #40825, #37668, .T. ) ;
#5999=DIRECTION ( 'NONE',  ( -0.000000000000000000, 0.7431448254773945772, 0.6691306063588579045 ) ) ;
#6004=VERTEX_POINT ( 'NONE', #37919 ) ;
#6010=EDGE_CURVE ( 'NONE', #14267, #6565, #40615, .T. ) ;
#6012=ORIENTED_EDGE ( 'NONE', *, *, #9922, .T. ) ;
#6014=EDGE_LOOP ( 'NONE', ( #45785, #28980, #21540, #44916 ) ) ;
#6019=CARTESIAN_POINT ( 'NONE',  ( 6.000000000000000000, -21.60688246758530795, -79.10210256391388839 ) ) ;
#6020=DIRECTION ( 'NONE',  ( -1.000000000000000000, 0.000000000000000000, -0.000000000000000000 ) ) ;
#6025=ORIENTED_EDGE ( 'NONE', *, *, #42098, .F. ) ;
#6030=AXIS2_PLACEMENT_3D ( 'NONE', #42499, #31495, #35140 ) ;
#6032=ORIENTED_EDGE ( 'NONE', *, *, #27106, .T. ) ;
#6033=CARTESIAN_POINT ( 'NONE',  ( 5.999999999999999112, -44.99326035066101781, 68.55367621811126355 ) ) ;
#6036=EDGE_CURVE ( 'NONE', #33795, #34978, #29837, .T. ) ;
#6037=LINE ( 'NONE', #21179, #37896 ) ;
#6038=ADVANCED_FACE ( 'NONE', ( #22506 ), #22982, .T. ) ;
#6041=EDGE_CURVE ( 'NONE', #32445, #37684, #2659, .T. ) ;
#6042=ORIENTED_EDGE ( 'NONE', *, *, #18779, .F. ) ;
#6046=EDGE_CURVE ( 'NONE', #32651, #10384, #8132, .T. ) ;
#6052=ORIENTED_EDGE ( 'NONE', *, *, #35081, .T. ) ;
#6054=DIRECTION ( 'NONE',  ( -1.000000000000000000, 0.000000000000000000, 0.000000000000000000 ) ) ;
#6056=VERTEX_POINT ( 'NONE', #7080 ) ;
#6058=ORIENTED_EDGE ( 'NONE', *, *, #42374, .T. ) ;
#6061=CARTESIAN_POINT ( 'NONE',  ( 15.00000000000000000, 16.83928648764922542, -16.46020748918050458 ) ) ;
#6063=EDGE_CURVE ( 'NONE', #2200, #37092, #5802, .T. ) ;
#6066=ORIENTED_EDGE ( 'NONE', *, *, #42432, .F. ) ;
#6067=ORIENTED_EDGE ( 'NONE', *, *, #31711, .T. ) ;
#6070=DIRECTION ( 'NONE',  ( 0.000000000000000000, 0.000000000000000000, 1.000000000000000000 ) ) ;
#6078=DIRECTION ( 'NONE',  ( 0.000000000000000000, 0.000000000000000000, 1.000000000000000000 ) ) ;
#6079=VECTOR ( 'NONE', #31666, 1000.000000000000000 ) ;
#6086=ORIENTED_EDGE ( 'NONE', *, *, #41245, .T. ) ;
#6087=CYLINDRICAL_SURFACE ( 'NONE', #44772, 77.49899999999999523 ) ;
#6089=DIRECTION ( 'NONE',  ( 0.000000000000000000, 0.000000000000000000, 1.000000000000000000 ) ) ;
#6090=ADVANCED_FACE ( 'NONE', ( #11003 ), #25920, .T. ) ;
#6091=VERTEX_POINT ( 'NONE', #12228 ) ;
#6092=CIRCLE ( 'NONE', #18547, 82.00000000000000000 ) ;
#6094=DIRECTION ( 'NONE',  ( -1.000000000000000000, 0.000000000000000000, 0.000000000000000000 ) ) ;
#6096=EDGE_CURVE ( 'NONE', #29406, #45717, #38159, .T. ) ;
#6101=CIRCLE ( 'NONE', #20940, 31.99999999999998579 ) ;
#6103=ORIENTED_EDGE ( 'NONE', *, *, #3986, .T. ) ;
#6106=VERTEX_POINT ( 'NONE', #20271 ) ;
#6112=ORIENTED_EDGE ( 'NONE', *, *, #10790, .F. ) ;
#6119=DIRECTION ( 'NONE',  ( 0.000000000000000000, 0.000000000000000000, -1.000000000000000000 ) ) ;
#6120=VERTEX_POINT ( 'NONE', #5119 ) ;
#6122=ORIENTED_EDGE ( 'NONE', *, *, #30960, .F. ) ;
#6124=DIRECTION ( 'NONE',  ( -1.000000000000000000, -0.000000000000000000, -0.000000000000000000 ) ) ;
#6128=FACE_OUTER_BOUND ( 'NONE', #45641, .T. ) ;
#6129=CARTESIAN_POINT ( 'NONE',  ( 11.99999999999999822, 39.78640506895698792, -66.50666863321958999 ) ) ;
#6144=DIRECTION ( 'NONE',  ( 0.000000000000000000, 0.8910065241883690090, -0.4539904997395446395 ) ) ;
#6150=ADVANCED_FACE ( 'NONE', ( #42076 ), #27152, .T. ) ;
#6158=EDGE_LOOP ( 'NONE', ( #13545, #11494, #1073, #17586 ) ) ;
#6162=DIRECTION ( 'NONE',  ( -1.000000000000000000, 0.000000000000000000, 0.000000000000000000 ) ) ;
#6167=DIRECTION ( 'NONE',  ( 1.000000000000000000, 0.000000000000000000, 0.000000000000000000 ) ) ;
#6169=AXIS2_PLACEMENT_3D ( 'NONE', #40637, #3430, #16324 ) ;
#6173=ORIENTED_EDGE ( 'NONE', *, *, #10395, .F. ) ;
#6176=AXIS2_PLACEMENT_3D ( 'NONE', #42050, #15389, #12199 ) ;
#6180=DIRECTION ( 'NONE',  ( 0.000000000000000000, -0.8910065241883723397, 0.4539904997395382003 ) ) ;
#6186=CARTESIAN_POINT ( 'NONE',  ( 0.000000000000000000, 6.903761155838878061, -77.19088730480517313 ) ) ;
#6188=EDGE_CURVE ( 'NONE', #41290, #25709, #31555, .T. ) ;
#6200=CARTESIAN_POINT ( 'NONE',  ( 0.000000000000000000, 74.65491531819118620, -8.830959090342659579 ) ) ;
#6202=VERTEX_POINT ( 'NONE', #26906 ) ;
#6203=CARTESIAN_POINT ( 'NONE',  ( 0.000000000000000000, -74.65491531819111515, -8.830959090343204920 ) ) ;
#6208=DIRECTION ( 'NONE',  ( -1.000000000000000000, 0.000000000000000000, 0.000000000000000000 ) ) ;
#6210=ORIENTED_EDGE ( 'NONE', *, *, #19225, .T. ) ;
#6212=ORIENTED_EDGE ( 'NONE', *, *, #37907, .T. ) ;
#6215=AXIS2_PLACEMENT_3D ( 'NONE', #40111, #6575, #41807 ) ;
#6216=ORIENTED_EDGE ( 'NONE', *, *, #40316, .F. ) ;
#6218=VECTOR ( 'NONE', #37393, 1000.000000000000000 ) ;
#6220=ORIENTED_EDGE ( 'NONE', *, *, #23365, .T. ) ;
#6228=ORIENTED_EDGE ( 'NONE', *, *, #3364, .F. ) ;
#6231=ORIENTED_EDGE ( 'NONE', *, *, #27827, .F. ) ;
#6232=LINE ( 'NONE', #46630, #42284 ) ;
#6237=DIRECTION ( 'NONE',  ( 0.000000000000000000, -0.4539904997395350361, -0.8910065241883738940 ) ) ;
#6238=VECTOR ( 'NONE', #12518, 999.9999999999998863 ) ;
#6248=DIRECTION ( 'NONE',  ( 0.000000000000000000, 0.000000000000000000, 1.000000000000000000 ) ) ;
#6252=CARTESIAN_POINT ( 'NONE',  ( 0.000000000000000000, 78.73519480814955784, 22.90783923731656557 ) ) ;
#6253=CIRCLE ( 'NONE', #26574, 31.99999999999999289 ) ;
#6259=CIRCLE ( 'NONE', #15645, 31.99999999999998579 ) ;
#6260=DIRECTION ( 'NONE',  ( 0.000000000000000000, 0.000000000000000000, 1.000000000000000000 ) ) ;
#6263=ADVANCED_FACE ( 'NONE', ( #16857 ), #2615, .T. ) ;
#6266=DIRECTION ( 'NONE',  ( 1.000000000000000000, -0.000000000000000000, -0.000000000000000000 ) ) ;
#6269=ORIENTED_EDGE ( 'NONE', *, *, #32753, .F. ) ;
#6270=DIRECTION ( 'NONE',  ( -1.000000000000000000, 0.000000000000000000, 0.000000000000000000 ) ) ;
#6277=CIRCLE ( 'NONE', #42998, 31.99999999999998579 ) ;
#6280=CARTESIAN_POINT ( 'NONE',  ( 11.99999999999999822, -41.19522573413780009, 65.64334221924896440 ) ) ;
#6287=CARTESIAN_POINT ( 'NONE',  ( 11.99999999999999822, -50.95692526931372157, 58.39081064771733054 ) ) ;
#6289=VERTEX_POINT ( 'NONE', #35444 ) ;
#6295=ORIENTED_EDGE ( 'NONE', *, *, #33489, .T. ) ;
#6306=EDGE_CURVE ( 'NONE', #24194, #44863, #22247, .T. ) ;
#6312=FACE_OUTER_BOUND ( 'NONE', #45710, .T. ) ;
#6314=AXIS2_PLACEMENT_3D ( 'NONE', #17423, #20880, #32381 ) ;
#6318=DIRECTION ( 'NONE',  ( 0.000000000000000000, -0.8526401643540860720, -0.5224985647159589019 ) ) ;
#6319=CARTESIAN_POINT ( 'NONE',  ( 12.00000000000000000, 16.61724383029361718, -20.69703378468927113 ) ) ;
#6325=AXIS2_PLACEMENT_3D ( 'NONE', #8758, #16132, #31064 ) ;
#6327=FACE_OUTER_BOUND ( 'NONE', #18303, .T. ) ;
#6330=ORIENTED_EDGE ( 'NONE', *, *, #43881, .F. ) ;
#6335=DIRECTION ( 'NONE',  ( 0.000000000000000000, -0.9135454576426010886, 0.4067366430757998752 ) ) ;
#6342=CIRCLE ( 'NONE', #14163, 31.99999999999998579 ) ;
#6343=VECTOR ( 'NONE', #43779, 1000.000000000000000 ) ;
#6346=VERTEX_POINT ( 'NONE', #22204 ) ;
#6347=VECTOR ( 'NONE', #47236, 1000.000000000000000 ) ;
#6351=ORIENTED_EDGE ( 'NONE', *, *, #19007, .T. ) ;
#6354=EDGE_CURVE ( 'NONE', #28804, #23663, #4300, .T. ) ;
#6355=CARTESIAN_POINT ( 'NONE',  ( 15.00000000000000000, -18.13022148937242761, 15.02647892043569122 ) ) ;
#6359=EDGE_CURVE ( 'NONE', #27340, #24200, #32419, .T. ) ;
#6361=VERTEX_POINT ( 'NONE', #21718 ) ;
#6363=CARTESIAN_POINT ( 'NONE',  ( 0.000000000000000000, -24.73286445877654671, -73.44644590900084324 ) ) ;
#6364=CARTESIAN_POINT ( 'NONE',  ( 12.00000000000000355, 0.000000000000000000, 0.000000000000000000 ) ) ;
#6367=EDGE_CURVE ( 'NONE', #26225, #24099, #44920, .T. ) ;
#6376=DIRECTION ( 'NONE',  ( -1.000000000000000000, -0.000000000000000000, 0.000000000000000000 ) ) ;
#6386=DIRECTION ( 'NONE',  ( 0.000000000000000000, 0.000000000000000000, 1.000000000000000000 ) ) ;
#6388=VECTOR ( 'NONE', #11119, 1000.000000000000000 ) ;
#6390=AXIS2_PLACEMENT_3D ( 'NONE', #5160, #31352, #12733 ) ;
#6396=ORIENTED_EDGE ( 'NONE', *, *, #4953, .F. ) ;
#6400=EDGE_LOOP ( 'NONE', ( #26030, #10190, #21142, #41324 ) ) ;
#6401=DIRECTION ( 'NONE',  ( 0.000000000000000000, 0.9945218953682731788, -0.1045284632676558162 ) ) ;
#6407=AXIS2_PLACEMENT_3D ( 'NONE', #39221, #20607, #39473 ) ;
#6409=ORIENTED_EDGE ( 'NONE', *, *, #27106, .F. ) ;
#6415=CARTESIAN_POINT ( 'NONE',  ( -10.00000000000000000, 0.000000000000000000, 0.000000000000000000 ) ) ;
#6420=ORIENTED_EDGE ( 'NONE', *, *, #19768, .T. ) ;
#6422=EDGE_CURVE ( 'NONE', #36912, #41773, #8164, .T. ) ;
#6424=DIRECTION ( 'NONE',  ( 0.000000000000000000, 0.000000000000000000, 1.000000000000000000 ) ) ;
#6427=EDGE_CURVE ( 'NONE', #38433, #37023, #38682, .T. ) ;
#6428=DIRECTION ( 'NONE',  ( 0.000000000000000000, 0.000000000000000000, 1.000000000000000000 ) ) ;
#6432=DIRECTION ( 'NONE',  ( -1.000000000000000000, -0.000000000000000000, -0.000000000000000000 ) ) ;
#6442=DIRECTION ( 'NONE',  ( 0.000000000000000000, 0.5877852522924689183, -0.8090169943749504489 ) ) ;
#6445=FACE_OUTER_BOUND ( 'NONE', #10484, .T. ) ;
#6448=AXIS2_PLACEMENT_3D ( 'NONE', #46517, #23500, #8805 ) ;
#6449=DIRECTION ( 'NONE',  ( 0.000000000000000000, 0.5224985647159499091, -0.8526401643540916231 ) ) ;
#6450=VECTOR ( 'NONE', #19305, 1000.000000000000000 ) ;
#6453=CIRCLE ( 'NONE', #46321, 82.00000000000000000 ) ;
#6457=EDGE_CURVE ( 'NONE', #13942, #20542, #5841, .T. ) ;
#6459=ORIENTED_EDGE ( 'NONE', *, *, #35350, .T. ) ;
#6461=DIRECTION ( 'NONE',  ( 0.000000000000000000, -0.9510565162951565288, 0.3090169943749382919 ) ) ;
#6464=CARTESIAN_POINT ( 'NONE',  ( 11.99999999999999822, 63.18004540533030422, 44.88180994100399346 ) ) ;
#6465=VECTOR ( 'NONE', #4473, 1000.000000000000000 ) ;
#6470=CARTESIAN_POINT ( 'NONE',  ( 11.99999999999999822, -2.956366410620109519, -75.11725578898472122 ) ) ;
#6471=CYLINDRICAL_SURFACE ( 'NONE', #10078, 31.99999999999998579 ) ;
#6472=CARTESIAN_POINT ( 'NONE',  ( -10.00000000000000000, 0.000000000000000000, 0.000000000000000000 ) ) ;
#6479=CARTESIAN_POINT ( 'NONE',  ( 6.000000000000000000, 3.894527615417885169, 81.90746397400390322 ) ) ;
#6480=CARTESIAN_POINT ( 'NONE',  ( 0.000000000000000000, 2.543863470248399761, 81.96053171279903893 ) ) ;
#6482=DIRECTION ( 'NONE',  ( 0.000000000000000000, 0.000000000000000000, 1.000000000000000000 ) ) ;
#6487=CYLINDRICAL_SURFACE ( 'NONE', #20344, 31.99999999999998579 ) ;
#6492=AXIS2_PLACEMENT_3D ( 'NONE', #9368, #16483, #39736 ) ;
#6493=DIRECTION ( 'NONE',  ( -1.000000000000000000, -0.000000000000000000, 0.000000000000000000 ) ) ;
#6498=DIRECTION ( 'NONE',  ( 0.000000000000000000, 0.9510565162951536422, 0.3090169943749471182 ) ) ;
#6502=AXIS2_PLACEMENT_3D ( 'NONE', #17383, #25937, #44785 ) ;
#6506=AXIS2_PLACEMENT_3D ( 'NONE', #39913, #39687, #9322 ) ;
#6511=EDGE_CURVE ( 'NONE', #43483, #24537, #10943, .T. ) ;
#6512=LINE ( 'NONE', #43951, #26506 ) ;
#6514=ADVANCED_FACE ( 'NONE', ( #20893 ), #19972, .T. ) ;
#6515=VECTOR ( 'NONE', #5058, 1000.000000000000000 ) ;
#6516=AXIS2_PLACEMENT_3D ( 'NONE', #21127, #2775, #10126 ) ;
#6521=AXIS2_PLACEMENT_3D ( 'NONE', #6698, #21628, #22352 ) ;
#6522=DIRECTION ( 'NONE',  ( -0.000000000000000000, 0.4999999999999921174, -0.8660254037844432595 ) ) ;
#6528=EDGE_CURVE ( 'NONE', #2585, #21915, #879, .T. ) ;
#6533=ORIENTED_EDGE ( 'NONE', *, *, #35034, .T. ) ;
#6534=ORIENTED_EDGE ( 'NONE', *, *, #35331, .F. ) ;
#6535=CARTESIAN_POINT ( 'NONE',  ( -10.00000000000000000, 0.000000000000000000, 0.000000000000000000 ) ) ;
#6540=DIRECTION ( 'NONE',  ( -1.000000000000000000, -0.000000000000000000, -0.000000000000000000 ) ) ;
#6541=CYLINDRICAL_SURFACE ( 'NONE', #47142, 31.99999999999998579 ) ;
#6543=EDGE_CURVE ( 'NONE', #41290, #40106, #46502, .T. ) ;
#6547=ORIENTED_EDGE ( 'NONE', *, *, #24470, .F. ) ;
#6550=CIRCLE ( 'NONE', #32342, 31.99999999999998224 ) ;
#6560=CARTESIAN_POINT ( 'NONE',  ( 0.000000000000000000, 0.000000000000000000, 0.000000000000000000 ) ) ;
#6565=VERTEX_POINT ( 'NONE', #8238 ) ;
#6569=PLANE ( 'NONE',  #24928 ) ;
#6571=ORIENTED_EDGE ( 'NONE', *, *, #20567, .T. ) ;
#6575=DIRECTION ( 'NONE',  ( -1.000000000000000000, 0.000000000000000000, 0.000000000000000000 ) ) ;
#6579=VERTEX_POINT ( 'NONE', #7983 ) ;
#6582=ADVANCED_FACE ( 'NONE', ( #46169 ), #22919, .T. ) ;
#6585=ORIENTED_EDGE ( 'NONE', *, *, #43924, .F. ) ;
#6593=DIRECTION ( 'NONE',  ( 1.000000000000000000, -0.000000000000000000, -0.000000000000000000 ) ) ;
#6601=ORIENTED_EDGE ( 'NONE', *, *, #20273, .F. ) ;
#6605=ORIENTED_EDGE ( 'NONE', *, *, #48184, .T. ) ;
#6611=DIRECTION ( 'NONE',  ( 0.000000000000000000, -0.1564344650402381687, 0.9876883405951365491 ) ) ;
#6613=CARTESIAN_POINT ( 'NONE',  ( 0.000000000000000000, -75.11764819372145041, -2.946379043147127064 ) ) ;
#6614=CARTESIAN_POINT ( 'NONE',  ( 11.99999999999999822, 80.28980883073781172, -16.65972982744850128 ) ) ;
#6616=AXIS2_PLACEMENT_3D ( 'NONE', #35091, #42696, #9153 ) ;
#6618=DIRECTION ( 'NONE',  ( -0.000000000000000000, -0.9135454576426006446, 0.4067366430758008744 ) ) ;
#6619=DIRECTION ( 'NONE',  ( 0.000000000000000000, 0.000000000000000000, 1.000000000000000000 ) ) ;
#6620=PLANE ( 'NONE',  #45155 ) ;
#6621=ORIENTED_EDGE ( 'NONE', *, *, #21255, .T. ) ;
#6627=CARTESIAN_POINT ( 'NONE',  ( 0.000000000000000000, 55.16347631943042984, 60.67117009219156643 ) ) ;
#6637=ADVANCED_FACE ( 'NONE', ( #38338 ), #652, .T. ) ;
#6646=FACE_OUTER_BOUND ( 'NONE', #47628, .T. ) ;
#6648=ORIENTED_EDGE ( 'NONE', *, *, #32023, .T. ) ;
#6662=AXIS2_PLACEMENT_3D ( 'NONE', #41009, #33172, #33883 ) ;
#6663=VERTEX_POINT ( 'NONE', #10601 ) ;
#6670=CIRCLE ( 'NONE', #15271, 82.00000000000000000 ) ;
#6671=DIRECTION ( 'NONE',  ( -1.000000000000000000, 0.000000000000000000, -0.000000000000000000 ) ) ;
#6677=AXIS2_PLACEMENT_3D ( 'NONE', #8804, #32301, #17348 ) ;
#6681=AXIS2_PLACEMENT_3D ( 'NONE', #47770, #6683, #47069 ) ;
#6683=DIRECTION ( 'NONE',  ( -1.000000000000000000, -0.000000000000000000, -0.000000000000000000 ) ) ;
#6685=DIRECTION ( 'NONE',  ( -1.000000000000000000, -0.000000000000000000, 0.000000000000000000 ) ) ;
#6687=FACE_OUTER_BOUND ( 'NONE', #18730, .T. ) ;
#6689=CARTESIAN_POINT ( 'NONE',  ( 15.00000000000000000, -10.45096189432344502, -21.10159698893425784 ) ) ;
#6690=ORIENTED_EDGE ( 'NONE', *, *, #34104, .T. ) ;
#6691=ORIENTED_EDGE ( 'NONE', *, *, #11289, .T. ) ;
#6692=CIRCLE ( 'NONE', #21529, 31.99999999999998934 ) ;
#6693=LINE ( 'NONE', #33354, #16797 ) ;
#6695=EDGE_CURVE ( 'NONE', #19747, #37030, #3599, .T. ) ;
#6698=CARTESIAN_POINT ( 'NONE',  ( -10.00000000000000000, 0.000000000000000000, 0.000000000000000000 ) ) ;
#6702=CARTESIAN_POINT ( 'NONE',  ( 11.99999999999999822, -6.903761155837269570, -77.19088730480530103 ) ) ;
#6705=ADVANCED_FACE ( 'NONE', ( #43641 ), #32845, .T. ) ;
#6709=CARTESIAN_POINT ( 'NONE',  ( 11.99999999999999822, -55.19960302592104284, 51.03279382321070301 ) ) ;
#6710=DIRECTION ( 'NONE',  ( 0.000000000000000000, -0.1045284632676449221, 0.9945218953682741780 ) ) ;
#6721=VERTEX_POINT ( 'NONE', #17694 ) ;
#6722=ORIENTED_EDGE ( 'NONE', *, *, #35044, .F. ) ;
#6727=ORIENTED_EDGE ( 'NONE', *, *, #39568, .F. ) ;
#6737=EDGE_CURVE ( 'NONE', #23206, #40594, #25511, .T. ) ;
#6740=LINE ( 'NONE', #3286, #15127 ) ;
#6741=VECTOR ( 'NONE', #9307, 1000.000000000000000 ) ;
#6742=DIRECTION ( 'NONE',  ( 0.000000000000000000, 0.000000000000000000, 1.000000000000000000 ) ) ;
#6743=DIRECTION ( 'NONE',  ( 0.000000000000000000, 0.000000000000000000, 1.000000000000000000 ) ) ;
#6749=EDGE_CURVE ( 'NONE', #23663, #14950, #13795, .T. ) ;
#6751=DIRECTION ( 'NONE',  ( -0.000000000000000000, -0.3090169943749450088, 0.9510565162951543083 ) ) ;
#6763=AXIS2_PLACEMENT_3D ( 'NONE', #5824, #31786, #9471 ) ;
#6767=ORIENTED_EDGE ( 'NONE', *, *, #30194, .T. ) ;
#6772=ORIENTED_EDGE ( 'NONE', *, *, #21922, .T. ) ;
#6776=ORIENTED_EDGE ( 'NONE', *, *, #48236, .T. ) ;
#6779=VERTEX_POINT ( 'NONE', #25745 ) ;
#6780=LINE ( 'NONE', #47635, #30248 ) ;
#6786=CARTESIAN_POINT ( 'NONE',  ( 15.00000000000000000, -26.23277895567245466, 4.042438405570107918 ) ) ;
#6789=FACE_OUTER_BOUND ( 'NONE', #47645, .T. ) ;
#6793=CARTESIAN_POINT ( 'NONE',  ( 5.999999999999999112, 21.60688246758697062, -79.10210256391344785 ) ) ;
#6794=EDGE_CURVE ( 'NONE', #16815, #4851, #10668, .T. ) ;
#6799=DIRECTION ( 'NONE',  ( -1.000000000000000000, -0.000000000000000000, -0.000000000000000000 ) ) ;
#6801=CARTESIAN_POINT ( 'NONE',  ( 11.99999999999999822, 31.46837873495072913, -68.27212725128242710 ) ) ;
#6802=EDGE_CURVE ( 'NONE', #27047, #47844, #24802, .T. ) ;
#6803=DIRECTION ( 'NONE',  ( 0.000000000000000000, 0.9876883405951383255, -0.1564344650402276216 ) ) ;
#6807=DIRECTION ( 'NONE',  ( -1.000000000000000000, -0.000000000000000000, -0.000000000000000000 ) ) ;
#6816=CIRCLE ( 'NONE', #47441, 77.49899999999999523 ) ;
#6818=DIRECTION ( 'NONE',  ( 0.000000000000000000, -0.4067366430757908269, 0.9135454576426049744 ) ) ;
#6829=ORIENTED_EDGE ( 'NONE', *, *, #27531, .T. ) ;
#6832=EDGE_LOOP ( 'NONE', ( #7625, #30363, #19234, #45013 ) ) ;
#6834=CIRCLE ( 'NONE', #15436, 31.99999999999998224 ) ;
#6838=VERTEX_POINT ( 'NONE', #38226 ) ;
#6842=CIRCLE ( 'NONE', #45914, 31.99999999999998934 ) ;
#6843=VERTEX_POINT ( 'NONE', #44839 ) ;
#6844=ORIENTED_EDGE ( 'NONE', *, *, #5654, .F. ) ;
#6850=DIRECTION ( 'NONE',  ( 0.000000000000000000, -0.6494480483301738882, -0.7604059656000392575 ) ) ;
#6852=CARTESIAN_POINT ( 'NONE',  ( 11.99999999999999822, -31.46837873494930093, -68.27212725128309501 ) ) ;
#6854=EDGE_CURVE ( 'NONE', #24231, #27585, #7403, .T. ) ;
#6863=VERTEX_POINT ( 'NONE', #11328 ) ;
#6867=ORIENTED_EDGE ( 'NONE', *, *, #861, .F. ) ;
#6873=AXIS2_PLACEMENT_3D ( 'NONE', #34154, #11645, #41508 ) ;
#6880=ORIENTED_EDGE ( 'NONE', *, *, #26930, .T. ) ;
#6881=CIRCLE ( 'NONE', #24086, 31.99999999999998579 ) ;
#6883=CARTESIAN_POINT ( 'NONE',  ( 5.999999999999999112, 77.16300072079698680, -27.74655509720591340 ) ) ;
#6885=CARTESIAN_POINT ( 'NONE',  ( 11.99999999999999822, -2.956366410621191765, 75.11725578898467859 ) ) ;
#6891=CARTESIAN_POINT ( 'NONE',  ( 0.000000000000000000, 0.000000000000000000, 0.000000000000000000 ) ) ;
#6895=EDGE_LOOP ( 'NONE', ( #203, #25516, #11574, #39938 ) ) ;
#6900=DIRECTION ( 'NONE',  ( -1.000000000000000000, 0.000000000000000000, 0.000000000000000000 ) ) ;
#6908=DIRECTION ( 'NONE',  ( 1.000000000000000000, 0.000000000000000000, 0.000000000000000000 ) ) ;
#6909=ADVANCED_FACE ( 'NONE', ( #18649 ), #26727, .T. ) ;
#6913=EDGE_CURVE ( 'NONE', #20902, #8878, #22339, .T. ) ;
#6914=CARTESIAN_POINT ( 'NONE',  ( 0.000000000000000000, -80.55351364060599906, 15.33399622253457295 ) ) ;
#6917=CARTESIAN_POINT ( 'NONE',  ( 0.000000000000000000, 0.000000000000000000, 0.000000000000000000 ) ) ;
#6927=LINE ( 'NONE', #3236, #37079 ) ;
#6928=ORIENTED_EDGE ( 'NONE', *, *, #21744, .F. ) ;
#6929=EDGE_CURVE ( 'NONE', #23939, #27284, #27872, .T. ) ;
#6933=ORIENTED_EDGE ( 'NONE', *, *, #24605, .F. ) ;
#6936=VECTOR ( 'NONE', #29078, 1000.000000000000000 ) ;
#6937=ORIENTED_EDGE ( 'NONE', *, *, #32346, .F. ) ;
#6943=CARTESIAN_POINT ( 'NONE',  ( 0.000000000000000000, -59.75363087400035056, -56.15606465355020305 ) ) ;
#6944=CARTESIAN_POINT ( 'NONE',  ( 6.000000000000000000, -81.50828551894220197, -8.966570791701593990 ) ) ;
#6950=FACE_OUTER_BOUND ( 'NONE', #38546, .T. ) ;
#6954=CARTESIAN_POINT ( 'NONE',  ( 11.99999999999999822, 0.000000000000000000, 0.000000000000000000 ) ) ;
#6957=EDGE_CURVE ( 'NONE', #32773, #32651, #25498, .T. ) ;
#6959=DIRECTION ( 'NONE',  ( -1.000000000000000000, -0.000000000000000000, 0.000000000000000000 ) ) ;
#6968=CARTESIAN_POINT ( 'NONE',  ( 0.000000000000000000, 79.10210256391398786, -21.60688246758504505 ) ) ;
#6972=CYLINDRICAL_SURFACE ( 'NONE', #2900, 31.99999999999998579 ) ;
#6973=EDGE_CURVE ( 'NONE', #488, #37099, #8316, .T. ) ;
#6980=CARTESIAN_POINT ( 'NONE',  ( 15.00000000000000000, 20.85821328998741109, -10.92862929874522671 ) ) ;
#6992=DIRECTION ( 'NONE',  ( -1.000000000000000000, 0.000000000000000000, 0.000000000000000000 ) ) ;
#6995=ORIENTED_EDGE ( 'NONE', *, *, #5110, .T. ) ;
#6997=ORIENTED_EDGE ( 'NONE', *, *, #330, .F. ) ;
#7002=FACE_OUTER_BOUND ( 'NONE', #36511, .T. ) ;
#7003=ORIENTED_EDGE ( 'NONE', *, *, #21922, .F. ) ;
#7005=AXIS2_PLACEMENT_3D ( 'NONE', #23561, #41689, #41451 ) ;
#7007=ORIENTED_EDGE ( 'NONE', *, *, #21131, .T. ) ;
#7009=CARTESIAN_POINT ( 'NONE',  ( 11.99999999999999822, 51.02545421589324803, 55.20638768913779870 ) ) ;
#7012=DIRECTION ( 'NONE',  ( -1.000000000000000000, 0.000000000000000000, 0.000000000000000000 ) ) ;
#7013=EDGE_CURVE ( 'NONE', #29636, #12206, #33292, .T. ) ;
#7015=FACE_OUTER_BOUND ( 'NONE', #38426, .T. ) ;
#7021=EDGE_CURVE ( 'NONE', #5172, #32098, #18484, .T. ) ;
#7025=LINE ( 'NONE', #21952, #30614 ) ;
#7031=DIRECTION ( 'NONE',  ( 0.000000000000000000, 0.000000000000000000, 1.000000000000000000 ) ) ;
#7032=ORIENTED_EDGE ( 'NONE', *, *, #37094, .T. ) ;
#7033=AXIS2_PLACEMENT_3D ( 'NONE', #19328, #41144, #45779 ) ;
#7034=CARTESIAN_POINT ( 'NONE',  ( 6.000000000000000000, -78.73519480814938731, -22.90783923731713045 ) ) ;
#7038=ORIENTED_EDGE ( 'NONE', *, *, #31030, .T. ) ;
#7041=LINE ( 'NONE', #9997, #3827 ) ;
#7042=CARTESIAN_POINT ( 'NONE',  ( 11.99999999999999822, -3.894527615417340272, -81.90746397400391743 ) ) ;
#7043=ORIENTED_EDGE ( 'NONE', *, *, #30915, .T. ) ;
#7049=ORIENTED_EDGE ( 'NONE', *, *, #21877, .T. ) ;
#7051=AXIS2_PLACEMENT_3D ( 'NONE', #15552, #45404, #11884 ) ;
#7053=CIRCLE ( 'NONE', #34411, 31.99999999999998934 ) ;
#7057=LINE ( 'NONE', #32298, #12682 ) ;
#7058=AXIS2_PLACEMENT_3D ( 'NONE', #35623, #31480, #17011 ) ;
#7072=VECTOR ( 'NONE', #39419, 1000.000000000000000 ) ;
#7074=FACE_OUTER_BOUND ( 'NONE', #45705, .T. ) ;
#7079=CYLINDRICAL_SURFACE ( 'NONE', #39199, 31.99999999999998579 ) ;
#7080=CARTESIAN_POINT ( 'NONE',  ( 11.99999999999999822, -46.21855187248673502, 62.20884554314003623 ) ) ;
#7085=CARTESIAN_POINT ( 'NONE',  ( 11.99999999999999822, -62.50329211542407393, -41.76937507738853839 ) ) ;
#7093=VERTEX_POINT ( 'NONE', #6614 ) ;
#7097=FACE_OUTER_BOUND ( 'NONE', #39935, .T. ) ;
#7100=DIRECTION ( 'NONE',  ( 0.000000000000000000, 0.000000000000000000, 1.000000000000000000 ) ) ;
#7105=EDGE_CURVE ( 'NONE', #5392, #35187, #17373, .T. ) ;
#7110=ORIENTED_EDGE ( 'NONE', *, *, #21215, .F. ) ;
#7113=VERTEX_POINT ( 'NONE', #32565 ) ;
#7117=VERTEX_POINT ( 'NONE', #24965 ) ;
#7120=CARTESIAN_POINT ( 'NONE',  ( 11.99999999999999822, -28.89263327155796190, 71.91182617369179297 ) ) ;
#7123=DIRECTION ( 'NONE',  ( 0.000000000000000000, 0.000000000000000000, 1.000000000000000000 ) ) ;
#7124=VERTEX_POINT ( 'NONE', #40397 ) ;
#7132=CARTESIAN_POINT ( 'NONE',  ( 11.99999999999999822, -20.41045688087876897, 72.35160999960810102 ) ) ;
#7137=VERTEX_POINT ( 'NONE', #28656 ) ;
#7146=VERTEX_POINT ( 'NONE', #17858 ) ;
#7149=DIRECTION ( 'NONE',  ( -1.000000000000000000, 0.000000000000000000, -0.000000000000000000 ) ) ;
#7150=EDGE_CURVE ( 'NONE', #11148, #16517, #45749, .T. ) ;
#7153=CARTESIAN_POINT ( 'NONE',  ( 12.00000000000000000, -18.13022148937263012, -15.02647892043543898 ) ) ;
#7154=CARTESIAN_POINT ( 'NONE',  ( 5.999999999999999112, -60.67117009219175827, 55.16347631943019536 ) ) ;
#7155=DIRECTION ( 'NONE',  ( 0.000000000000000000, 0.000000000000000000, 1.000000000000000000 ) ) ;
#7164=CARTESIAN_POINT ( 'NONE',  ( 11.99999999999999822, 0.000000000000000000, 0.000000000000000000 ) ) ;
#7166=DIRECTION ( 'NONE',  ( 0.000000000000000000, 0.8660254037844363761, -0.5000000000000039968 ) ) ;
#7167=VERTEX_POINT ( 'NONE', #47707 ) ;
#7169=CIRCLE ( 'NONE', #26709, 82.00000000000000000 ) ;
#7170=CIRCLE ( 'NONE', #32209, 82.00000000000000000 ) ;
#7173=VERTEX_POINT ( 'NONE', #43348 ) ;
#7175=CIRCLE ( 'NONE', #32959, 31.99999999999998579 ) ;
#7179=CARTESIAN_POINT ( 'NONE',  ( 11.99999999999999822, -8.840884882374576037, -74.65374052328658649 ) ) ;
#7182=DIRECTION ( 'NONE',  ( 0.000000000000000000, 0.000000000000000000, -1.000000000000000000 ) ) ;
#7187=CARTESIAN_POINT ( 'NONE',  ( 11.99999999999999822, 62.20884554314085335, -46.21855187248562657 ) ) ;
#7188=CYLINDRICAL_SURFACE ( 'NONE', #42158, 31.99999999999998579 ) ;
#7195=FACE_OUTER_BOUND ( 'NONE', #44814, .T. ) ;
#7201=DIRECTION ( 'NONE',  ( 1.000000000000000000, -0.000000000000000000, 0.000000000000000000 ) ) ;
#7204=EDGE_CURVE ( 'NONE', #19747, #29191, #37437, .T. ) ;
#7205=DIRECTION ( 'NONE',  ( -1.000000000000000000, 0.000000000000000000, 0.000000000000000000 ) ) ;
#7208=CARTESIAN_POINT ( 'NONE',  ( 0.000000000000000000, 0.000000000000000000, 0.000000000000000000 ) ) ;
#7209=AXIS2_PLACEMENT_3D ( 'NONE', #46761, #5162, #42112 ) ;
#7210=LINE ( 'NONE', #26780, #2512 ) ;
#7215=EDGE_CURVE ( 'NONE', #33303, #7570, #424, .T. ) ;
#7217=CYLINDRICAL_SURFACE ( 'NONE', #31622, 77.49899999999999523 ) ;
#7218=CYLINDRICAL_SURFACE ( 'NONE', #45039, 31.99999999999998579 ) ;
#7224=EDGE_CURVE ( 'NONE', #33522, #44222, #40299, .T. ) ;
#7231=VECTOR ( 'NONE', #14243, 1000.000000000000000 ) ;
#7235=AXIS2_PLACEMENT_3D ( 'NONE', #12936, #43026, #39109 ) ;
#7241=AXIS2_PLACEMENT_3D ( 'NONE', #6200, #35080, #27998 ) ;
#7244=CARTESIAN_POINT ( 'NONE',  ( 5.999999999999999112, 60.67117009219134616, 55.16347631943062879 ) ) ;
#7254=CARTESIAN_POINT ( 'NONE',  ( 11.99999999999999822, -24.73286445877757345, 73.44644590900053061 ) ) ;
#7255=DIRECTION ( 'NONE',  ( 0.000000000000000000, 0.000000000000000000, 1.000000000000000000 ) ) ;
#7259=DIRECTION ( 'NONE',  ( -1.000000000000000000, -0.000000000000000000, -0.000000000000000000 ) ) ;
#7260=CARTESIAN_POINT ( 'NONE',  ( 0.000000000000000000, 0.000000000000000000, 0.000000000000000000 ) ) ;
#7271=CYLINDRICAL_SURFACE ( 'NONE', #46668, 82.00000000000000000 ) ;
#7272=CYLINDRICAL_SURFACE ( 'NONE', #3427, 82.00000000000000000 ) ;
#7274=AXIS2_PLACEMENT_3D ( 'NONE', #28441, #43385, #2486 ) ;
#7275=CARTESIAN_POINT ( 'NONE',  ( 11.99999999999999822, 10.30890764327501863, -81.34940948281324324 ) ) ;
#7285=EDGE_CURVE ( 'NONE', #27571, #18838, #17596, .T. ) ;
#7287=VERTEX_POINT ( 'NONE', #15417 ) ;
#7291=DIRECTION ( 'NONE',  ( -1.000000000000000000, 0.000000000000000000, -0.000000000000000000 ) ) ;
#7302=AXIS2_PLACEMENT_3D ( 'NONE', #11379, #48079, #34110 ) ;
#7308=ORIENTED_EDGE ( 'NONE', *, *, #17729, .T. ) ;
#7310=DIRECTION ( 'NONE',  ( -1.000000000000000000, -0.000000000000000000, -0.000000000000000000 ) ) ;
#7311=DIRECTION ( 'NONE',  ( -1.000000000000000000, 0.000000000000000000, -0.000000000000000000 ) ) ;
#7315=ORIENTED_EDGE ( 'NONE', *, *, #37685, .T. ) ;
#7317=DIRECTION ( 'NONE',  ( -1.000000000000000000, -0.000000000000000000, -0.000000000000000000 ) ) ;
#7318=CARTESIAN_POINT ( 'NONE',  ( 11.99999999999999822, 0.000000000000000000, 0.000000000000000000 ) ) ;
#7319=ORIENTED_EDGE ( 'NONE', *, *, #8301, .F. ) ;
#7320=CIRCLE ( 'NONE', #5804, 31.99999999999998579 ) ;
#7323=CYLINDRICAL_SURFACE ( 'NONE', #30591, 31.99999999999998579 ) ;
#7324=CARTESIAN_POINT ( 'NONE',  ( 6.000000000000000000, -71.87247863392384772, -39.47590169984923136 ) ) ;
#7328=EDGE_CURVE ( 'NONE', #15373, #41886, #15286, .T. ) ;
#7333=LINE ( 'NONE', #37197, #5739 ) ;
#7340=CIRCLE ( 'NONE', #30029, 31.99999999999998579 ) ;
#7343=AXIS2_PLACEMENT_3D ( 'NONE', #35386, #13131, #24627 ) ;
#7347=VERTEX_POINT ( 'NONE', #40622 ) ;
#7351=AXIS2_PLACEMENT_3D ( 'NONE', #40572, #18041, #7031 ) ;
#7353=AXIS2_PLACEMENT_3D ( 'NONE', #10522, #2678, #25435 ) ;
#7355=CIRCLE ( 'NONE', #48029, 77.49899999999999523 ) ;
#7356=ORIENTED_EDGE ( 'NONE', *, *, #24030, .F. ) ;
#7357=CARTESIAN_POINT ( 'NONE',  ( 11.99999999999999822, -60.67117009219096957, -55.16347631943106933 ) ) ;
#7361=EDGE_CURVE ( 'NONE', #12014, #23939, #19532, .T. ) ;
#7362=ORIENTED_EDGE ( 'NONE', *, *, #18272, .T. ) ;
#7363=CARTESIAN_POINT ( 'NONE',  ( 0.000000000000000000, -14.66109333815410487, -73.73191006444587003 ) ) ;
#7381=EDGE_LOOP ( 'NONE', ( #14241, #42122, #39035, #42487 ) ) ;
#7383=CARTESIAN_POINT ( 'NONE',  ( 15.00000000000000000, 26.49999999999999645, 1.499999999999995781 ) ) ;
#7386=EDGE_LOOP ( 'NONE', ( #4108, #47165, #16131, #37053 ) ) ;
#7388=CARTESIAN_POINT ( 'NONE',  ( 0.000000000000000000, -55.19960302592029677, -51.03279382321147750 ) ) ;
#7392=CARTESIAN_POINT ( 'NONE',  ( 11.99999999999999822, 60.67117009219215618, -55.16347631942976903 ) ) ;
#7394=EDGE_CURVE ( 'NONE', #10792, #36121, #12952, .T. ) ;
#7398=VECTOR ( 'NONE', #378, 1000.000000000000000 ) ;
#7402=CARTESIAN_POINT ( 'NONE',  ( 11.99999999999999822, -51.03279382321048985, -55.19960302592120627 ) ) ;
#7403=LINE ( 'NONE', #37988, #44266 ) ;
#7407=CARTESIAN_POINT ( 'NONE',  ( 0.000000000000000000, -2.543863470247813119, -81.96053171279903893 ) ) ;
#7412=ORIENTED_EDGE ( 'NONE', *, *, #37565, .F. ) ;
#7414=CARTESIAN_POINT ( 'NONE',  ( 11.99999999999999822, -63.97538442413463855, 51.29473840253199057 ) ) ;
#7416=DIRECTION ( 'NONE',  ( -1.000000000000000000, 0.000000000000000000, -0.000000000000000000 ) ) ;
#7418=ORIENTED_EDGE ( 'NONE', *, *, #20960, .T. ) ;
#7419=DIRECTION ( 'NONE',  ( -1.000000000000000000, -0.000000000000000000, -0.000000000000000000 ) ) ;
#7420=ORIENTED_EDGE ( 'NONE', *, *, #13609, .T. ) ;
#7422=EDGE_CURVE ( 'NONE', #923, #27585, #35211, .T. ) ;
#7425=LINE ( 'NONE', #6702, #23709 ) ;
#7434=ORIENTED_EDGE ( 'NONE', *, *, #2941, .F. ) ;
#7439=CARTESIAN_POINT ( 'NONE',  ( 0.000000000000000000, 77.49459641780886443, 0.8261519478433866359 ) ) ;
#7441=LINE ( 'NONE', #15277, #21241 ) ;
#7450=DIRECTION ( 'NONE',  ( -1.000000000000000000, -0.000000000000000000, -0.000000000000000000 ) ) ;
#7453=DIRECTION ( 'NONE',  ( -1.000000000000000000, 0.000000000000000000, 0.000000000000000000 ) ) ;
#7460=CARTESIAN_POINT ( 'NONE',  ( 12.00000000000000000, -18.13022148937242761, 15.02647892043569122 ) ) ;
#7464=DIRECTION ( 'NONE',  ( 0.000000000000000000, 0.2334453638559058908, -0.9723699203976764460 ) ) ;
#7476=AXIS2_PLACEMENT_3D ( 'NONE', #38697, #35729, #46516 ) ;
#7477=ORIENTED_EDGE ( 'NONE', *, *, #41611, .F. ) ;
#7478=EDGE_CURVE ( 'NONE', #13639, #41791, #29386, .T. ) ;
#7480=EDGE_CURVE ( 'NONE', #9901, #22127, #26912, .T. ) ;
#7481=ADVANCED_FACE ( 'NONE', ( #16146 ), #27160, .T. ) ;
#7486=ORIENTED_EDGE ( 'NONE', *, *, #41658, .F. ) ;
#7488=CIRCLE ( 'NONE', #29391, 77.49900000000000944 ) ;
#7494=CARTESIAN_POINT ( 'NONE',  ( 6.000000000000000000, 8.966570791701871102, -81.50828551894218776 ) ) ;
#7497=ORIENTED_EDGE ( 'NONE', *, *, #13544, .T. ) ;
#7500=CARTESIAN_POINT ( 'NONE',  ( 11.99999999999999822, 71.87247863392413194, 39.47590169984869846 ) ) ;
#7501=DIRECTION ( 'NONE',  ( 0.000000000000000000, 0.000000000000000000, 1.000000000000000000 ) ) ;
#7507=CARTESIAN_POINT ( 'NONE',  ( 11.99999999999999822, 31.46837873494978055, 68.27212725128286763 ) ) ;
#7512=FACE_OUTER_BOUND ( 'NONE', #18993, .T. ) ;
#7516=DIRECTION ( 'NONE',  ( 0.000000000000000000, 0.000000000000000000, 1.000000000000000000 ) ) ;
#7517=DIRECTION ( 'NONE',  ( 1.000000000000000000, 0.000000000000000000, 0.000000000000000000 ) ) ;
#7527=AXIS2_PLACEMENT_3D ( 'NONE', #4194, #3200, #45068 ) ;
#7533=ADVANCED_FACE ( 'NONE', ( #6327 ), #9986, .T. ) ;
#7535=EDGE_CURVE ( 'NONE', #31422, #3459, #43759, .T. ) ;
#7536=FACE_OUTER_BOUND ( 'NONE', #21679, .T. ) ;
#7540=EDGE_CURVE ( 'NONE', #36257, #38129, #10227, .T. ) ;
#7542=ORIENTED_EDGE ( 'NONE', *, *, #24869, .F. ) ;
#7545=DIRECTION ( 'NONE',  ( 0.000000000000000000, 0.5224985647159440250, 0.8526401643540951758 ) ) ;
#7549=CARTESIAN_POINT ( 'NONE',  ( 11.99999999999999822, 5.256550761633951296, -77.32052557432835727 ) ) ;
#7555=EDGE_CURVE ( 'NONE', #39954, #26342, #9052, .T. ) ;
#7557=ORIENTED_EDGE ( 'NONE', *, *, #6041, .F. ) ;
#7559=ORIENTED_EDGE ( 'NONE', *, *, #18220, .F. ) ;
#7561=DIRECTION ( 'NONE',  ( 0.000000000000000000, 1.000000000000000000, 3.469446951953615767E-15 ) ) ;
#7564=ORIENTED_EDGE ( 'NONE', *, *, #4613, .T. ) ;
#7567=EDGE_CURVE ( 'NONE', #42120, #42306, #5149, .T. ) ;
#7569=ORIENTED_EDGE ( 'NONE', *, *, #42987, .F. ) ;
#7570=VERTEX_POINT ( 'NONE', #32516 ) ;
#7582=FACE_OUTER_BOUND ( 'NONE', #37220, .T. ) ;
#7587=FACE_OUTER_BOUND ( 'NONE', #22039, .T. ) ;
#7588=VECTOR ( 'NONE', #20219, 1000.000000000000000 ) ;
#7589=DIRECTION ( 'NONE',  ( 0.000000000000000000, 0.8526401643540897357, 0.5224985647159527957 ) ) ;
#7598=CIRCLE ( 'NONE', #42799, 82.00000000000000000 ) ;
#7599=CARTESIAN_POINT ( 'NONE',  ( 15.00000000000000000, 14.60985201121703980, -18.46759930825707841 ) ) ;
#7603=ORIENTED_EDGE ( 'NONE', *, *, #44702, .F. ) ;
#7604=EDGE_LOOP ( 'NONE', ( #35071, #22915, #32636, #20043 ) ) ;
#7607=VERTEX_POINT ( 'NONE', #32043 ) ;
#7608=AXIS2_PLACEMENT_3D ( 'NONE', #42137, #1506, #46290 ) ;
#7611=LINE ( 'NONE', #19098, #43905 ) ;
#7614=CARTESIAN_POINT ( 'NONE',  ( 0.000000000000000000, -70.52718814184277107, 26.02418014898285037 ) ) ;
#7615=ORIENTED_EDGE ( 'NONE', *, *, #4825, .F. ) ;
#7619=EDGE_LOOP ( 'NONE', ( #28890, #36613, #38299, #26084 ) ) ;
#7625=ORIENTED_EDGE ( 'NONE', *, *, #9135, .T. ) ;
#7627=DIRECTION ( 'NONE',  ( -1.000000000000000000, 0.000000000000000000, 0.000000000000000000 ) ) ;
#7629=ORIENTED_EDGE ( 'NONE', *, *, #38441, .F. ) ;
#7631=DIRECTION ( 'NONE',  ( 0.000000000000000000, -0.9876883405951359940, -0.1564344650402420822 ) ) ;
#7635=FACE_OUTER_BOUND ( 'NONE', #26616, .T. ) ;
#7636=EDGE_CURVE ( 'NONE', #3648, #42120, #30992, .T. ) ;
#7642=EDGE_CURVE ( 'NONE', #3459, #34359, #15316, .T. ) ;
#7643=AXIS2_PLACEMENT_3D ( 'NONE', #5189, #20104, #45826 ) ;
#7649=ORIENTED_EDGE ( 'NONE', *, *, #1402, .T. ) ;
#7650=ORIENTED_EDGE ( 'NONE', *, *, #18574, .F. ) ;
#7653=CARTESIAN_POINT ( 'NONE',  ( 11.99999999999999822, 78.73519480814954363, 22.90783923731657268 ) ) ;
#7655=ORIENTED_EDGE ( 'NONE', *, *, #26269, .T. ) ;
#7669=AXIS2_PLACEMENT_3D ( 'NONE', #9242, #1917, #31789 ) ;
#7671=ADVANCED_FACE ( 'NONE', ( #46633 ), #38562, .T. ) ;
#7673=DIRECTION ( 'NONE',  ( 0.000000000000000000, 0.000000000000000000, 1.000000000000000000 ) ) ;
#7683=DIRECTION ( 'NONE',  ( -1.000000000000000000, 0.000000000000000000, 0.000000000000000000 ) ) ;
#7684=EDGE_LOOP ( 'NONE', ( #9004, #30482, #41099, #12907 ) ) ;
#7687=EDGE_CURVE ( 'NONE', #24923, #20697, #455, .T. ) ;
#7689=FACE_OUTER_BOUND ( 'NONE', #33263, .T. ) ;
#7690=DIRECTION ( 'NONE',  ( -1.000000000000000000, -0.000000000000000000, -0.000000000000000000 ) ) ;
#7691=DIRECTION ( 'NONE',  ( -1.000000000000000000, 0.000000000000000000, 0.000000000000000000 ) ) ;
#7692=DIRECTION ( 'NONE',  ( 0.000000000000000000, 0.000000000000000000, 1.000000000000000000 ) ) ;
#7693=CARTESIAN_POINT ( 'NONE',  ( 0.000000000000000000, -71.21200624218768382, -40.65526001592688488 ) ) ;
#7703=CIRCLE ( 'NONE', #7669, 31.99999999999998934 ) ;
#7705=CIRCLE ( 'NONE', #33482, 31.99999999999998579 ) ;
#7706=DIRECTION ( 'NONE',  ( -1.000000000000000000, 0.000000000000000000, 0.000000000000000000 ) ) ;
#7710=ORIENTED_EDGE ( 'NONE', *, *, #34911, .F. ) ;
#7722=ORIENTED_EDGE ( 'NONE', *, *, #14500, .T. ) ;
#7736=CARTESIAN_POINT ( 'NONE',  ( 11.99999999999999822, 0.000000000000000000, 0.000000000000000000 ) ) ;
#7743=AXIS2_PLACEMENT_3D ( 'NONE', #29697, #33382, #38023 ) ;
#7744=CARTESIAN_POINT ( 'NONE',  ( 5.999999999999999112, -51.29473840253269401, 63.97538442413407012 ) ) ;
#7748=CARTESIAN_POINT ( 'NONE',  ( 5.999999999999999112, 44.99326035066149387, -68.55367621811095091 ) ) ;
#7752=DIRECTION ( 'NONE',  ( -1.000000000000000000, 0.000000000000000000, -0.000000000000000000 ) ) ;
#7753=CIRCLE ( 'NONE', #41372, 31.99999999999998224 ) ;
#7755=DIRECTION ( 'NONE',  ( 1.000000000000000000, 0.000000000000000000, -0.000000000000000000 ) ) ;
#7758=DIRECTION ( 'NONE',  ( -1.000000000000000000, 0.000000000000000000, -0.000000000000000000 ) ) ;
#7759=ADVANCED_FACE ( 'NONE', ( #43450 ), #10635, .F. ) ;
#7766=AXIS2_PLACEMENT_3D ( 'NONE', #36520, #2985, #29170 ) ;
#7767=ORIENTED_EDGE ( 'NONE', *, *, #15584, .F. ) ;
#7768=AXIS2_PLACEMENT_3D ( 'NONE', #44678, #11157, #18724 ) ;
#7772=ORIENTED_EDGE ( 'NONE', *, *, #22543, .T. ) ;
#7775=ADVANCED_FACE ( 'NONE', ( #25058 ), #6471, .T. ) ;
#7776=ORIENTED_EDGE ( 'NONE', *, *, #4537, .T. ) ;
#7777=VERTEX_POINT ( 'NONE', #39775 ) ;
#7780=CARTESIAN_POINT ( 'NONE',  ( 6.000000000000000000, -81.90746397400391743, 3.894527615417579636 ) ) ;
#7787=ORIENTED_EDGE ( 'NONE', *, *, #4749, .F. ) ;
#7792=ORIENTED_EDGE ( 'NONE', *, *, #21286, .F. ) ;
#7795=AXIS2_PLACEMENT_3D ( 'NONE', #22984, #476, #26664 ) ;
#7797=ORIENTED_EDGE ( 'NONE', *, *, #814, .F. ) ;
#7806=DIRECTION ( 'NONE',  ( -1.000000000000000000, -0.000000000000000000, 0.000000000000000000 ) ) ;
#7819=PRESENTATION_STYLE_ASSIGNMENT (( #18820 ) ) ;
#7824=DIRECTION ( 'NONE',  ( 0.000000000000000000, 0.9238795325112878487, -0.3826834323650874503 ) ) ;
#7825=DIRECTION ( 'NONE',  ( -1.000000000000000000, 0.000000000000000000, 0.000000000000000000 ) ) ;
#7831=ORIENTED_EDGE ( 'NONE', *, *, #31084, .T. ) ;
#7832=EDGE_LOOP ( 'NONE', ( #18258, #12318, #5210, #17099 ) ) ;
#7838=AXIS2_PLACEMENT_3D ( 'NONE', #19865, #35777, #2238 ) ;
#7843=ADVANCED_FACE ( 'NONE', ( #40975 ), #40719, .T. ) ;
#7844=ORIENTED_EDGE ( 'NONE', *, *, #5687, .T. ) ;
#7847=LINE ( 'NONE', #15676, #1184 ) ;
#7851=DIRECTION ( 'NONE',  ( -1.000000000000000000, 0.000000000000000000, -0.000000000000000000 ) ) ;
#7854=CARTESIAN_POINT ( 'NONE',  ( 0.000000000000000000, 46.21855187248630159, 62.20884554314034176 ) ) ;
#7859=DIRECTION ( 'NONE',  ( 0.000000000000000000, -0.2334453638559126354, 0.9723699203976748917 ) ) ;
#7863=DIRECTION ( 'NONE',  ( -1.000000000000000000, -0.000000000000000000, -0.000000000000000000 ) ) ;
#7870=DIRECTION ( 'NONE',  ( 0.000000000000000000, 0.9969173337331281859, -0.07845909572784182107 ) ) ;
#7876=DIRECTION ( 'NONE',  ( -1.000000000000000000, 0.000000000000000000, 0.000000000000000000 ) ) ;
#7882=ORIENTED_EDGE ( 'NONE', *, *, #39703, .T. ) ;
#7885=AXIS2_PLACEMENT_3D ( 'NONE', #17603, #7310, #36207 ) ;
#7886=ORIENTED_EDGE ( 'NONE', *, *, #23157, .F. ) ;
#7891=CARTESIAN_POINT ( 'NONE',  ( 0.000000000000000000, -12.93880638057369659, 76.41127070299266677 ) ) ;
#7898=LINE ( 'NONE', #3747, #17953 ) ;
#7899=DIRECTION ( 'NONE',  ( -1.000000000000000000, 0.000000000000000000, 0.000000000000000000 ) ) ;
#7901=AXIS2_PLACEMENT_3D ( 'NONE', #2201, #36449, #28857 ) ;
#7904=EDGE_CURVE ( 'NONE', #15597, #20505, #4597, .T. ) ;
#7905=DIRECTION ( 'NONE',  ( -1.000000000000000000, -0.000000000000000000, -0.000000000000000000 ) ) ;
#7919=ORIENTED_EDGE ( 'NONE', *, *, #24648, .T. ) ;
#7920=DIRECTION ( 'NONE',  ( 0.000000000000000000, 0.000000000000000000, 1.000000000000000000 ) ) ;
#7922=CARTESIAN_POINT ( 'NONE',  ( 11.99999999999999822, 81.50828551894227303, 8.966570791700986476 ) ) ;
#7933=CARTESIAN_POINT ( 'NONE',  ( 11.99999999999999822, 20.40083707022882820, 72.35432306680490910 ) ) ;
#7935=VERTEX_POINT ( 'NONE', #41448 ) ;
#7936=CIRCLE ( 'NONE', #6407, 31.99999999999998579 ) ;
#7938=CIRCLE ( 'NONE', #7058, 31.99999999999998579 ) ;
#7947=ORIENTED_EDGE ( 'NONE', *, *, #15605, .F. ) ;
#7951=CARTESIAN_POINT ( 'NONE',  ( 11.99999999999999822, 0.000000000000000000, 0.000000000000000000 ) ) ;
#7953=ORIENTED_EDGE ( 'NONE', *, *, #9061, .F. ) ;
#7960=CARTESIAN_POINT ( 'NONE',  ( 15.00000000000000000, -22.32062822937469093, 14.36278369418830181 ) ) ;
#7962=ORIENTED_EDGE ( 'NONE', *, *, #7478, .T. ) ;
#7975=CARTESIAN_POINT ( 'NONE',  ( 15.00000000000000000, 23.49999999999999645, 1.499999999999995337 ) ) ;
#7977=ORIENTED_EDGE ( 'NONE', *, *, #37559, .F. ) ;
#7978=CARTESIAN_POINT ( 'NONE',  ( 11.99999999999999822, 44.88180994100376608, 63.18004540533043922 ) ) ;
#7980=ORIENTED_EDGE ( 'NONE', *, *, #19002, .T. ) ;
#7983=CARTESIAN_POINT ( 'NONE',  ( 0.000000000000000000, 68.67312586195046720, -35.91791733033404199 ) ) ;
#7986=ADVANCED_FACE ( 'NONE', ( #8154 ), #34322, .T. ) ;
#7990=EDGE_CURVE ( 'NONE', #34932, #35715, #31205, .T. ) ;
#7992=LINE ( 'NONE', #34658, #37338 ) ;
#7997=ORIENTED_EDGE ( 'NONE', *, *, #25941, .F. ) ;
#8002=ORIENTED_EDGE ( 'NONE', *, *, #8221, .F. ) ;
#8003=CARTESIAN_POINT ( 'NONE',  ( 11.99999999999999822, 76.41127070299290835, -12.93880638057234123 ) ) ;
#8004=CARTESIAN_POINT ( 'NONE',  ( 11.99999999999999822, 31.46837873494978055, 68.27212725128286763 ) ) ;
#8006=AXIS2_PLACEMENT_3D ( 'NONE', #590, #15520, #30451 ) ;
#8008=EDGE_CURVE ( 'NONE', #40594, #2738, #19499, .T. ) ;
#8013=ORIENTED_EDGE ( 'NONE', *, *, #5274, .T. ) ;
#8018=ORIENTED_EDGE ( 'NONE', *, *, #40181, .T. ) ;
#8022=ORIENTED_EDGE ( 'NONE', *, *, #27140, .T. ) ;
#8032=FILL_AREA_STYLE_COLOUR ( '', #27426 ) ;
#8044=DIRECTION ( 'NONE',  ( 0.000000000000000000, -0.1564344650402381687, 0.9876883405951365491 ) ) ;
#8046=CARTESIAN_POINT ( 'NONE',  ( 11.99999999999999822, -62.20884554313985149, -46.21855187248698371 ) ) ;
#8047=AXIS2_PLACEMENT_3D ( 'NONE', #6801, #43525, #2386 ) ;
#8048=DIRECTION ( 'NONE',  ( -1.000000000000000000, 0.000000000000000000, 0.000000000000000000 ) ) ;
#8051=DIRECTION ( 'NONE',  ( 0.000000000000000000, 0.8090169943749486725, -0.5877852522924713607 ) ) ;
#8052=CIRCLE ( 'NONE', #33063, 82.00000000000000000 ) ;
#8053=EDGE_CURVE ( 'NONE', #30740, #6106, #15570, .T. ) ;
#8062=CARTESIAN_POINT ( 'NONE',  ( 11.99999999999999822, 0.000000000000000000, 0.000000000000000000 ) ) ;
#8064=AXIS2_PLACEMENT_3D ( 'NONE', #25204, #47023, #35765 ) ;
#8065=PLANE ( 'NONE',  #34669 ) ;
#8069=EDGE_CURVE ( 'NONE', #24200, #22938, #27125, .T. ) ;
#8071=AXIS2_PLACEMENT_3D ( 'NONE', #36149, #13648, #24896 ) ;
#8072=AXIS2_PLACEMENT_3D ( 'NONE', #14961, #19757, #30144 ) ;
#8077=ORIENTED_EDGE ( 'NONE', *, *, #8458, .T. ) ;
#8087=CIRCLE ( 'NONE', #18246, 31.99999999999999289 ) ;
#8097=EDGE_LOOP ( 'NONE', ( #25811, #37643, #13167, #39458 ) ) ;
#8100=DIRECTION ( 'NONE',  ( 0.000000000000000000, 0.000000000000000000, 1.000000000000000000 ) ) ;
#8103=CARTESIAN_POINT ( 'NONE',  ( 11.99999999999999822, 23.16143007188426850, 73.95703589263983702 ) ) ;
#8105=LINE ( 'NONE', #19120, #36309 ) ;
#8107=DIRECTION ( 'NONE',  ( -1.000000000000000000, 0.000000000000000000, 0.000000000000000000 ) ) ;
#8108=DIRECTION ( 'NONE',  ( -1.000000000000000000, -0.000000000000000000, 0.000000000000000000 ) ) ;
#8109=DIRECTION ( 'NONE',  ( -1.000000000000000000, 0.000000000000000000, 0.000000000000000000 ) ) ;
#8117=AXIS2_PLACEMENT_3D ( 'NONE', #17788, #3334, #48372 ) ;
#8121=CARTESIAN_POINT ( 'NONE',  ( 0.000000000000000000, 33.71516098798741012, 74.74816331893441657 ) ) ;
#8122=LINE ( 'NONE', #23057, #20175 ) ;
#8123=CARTESIAN_POINT ( 'NONE',  ( 0.000000000000000000, 68.67312586194995561, 35.91791733033500122 ) ) ;
#8124=ADVANCED_FACE ( 'NONE', ( #14890 ), #26397, .T. ) ;
#8125=VERTEX_POINT ( 'NONE', #44740 ) ;
#8126=EDGE_CURVE ( 'NONE', #44023, #22951, #25712, .T. ) ;
#8132=CIRCLE ( 'NONE', #331, 31.99999999999998224 ) ;
#8133=LINE ( 'NONE', #11577, #6465 ) ;
#8134=AXIS2_PLACEMENT_3D ( 'NONE', #8319, #27169, #15902 ) ;
#8137=FACE_OUTER_BOUND ( 'NONE', #46465, .T. ) ;
#8140=DIRECTION ( 'NONE',  ( -1.000000000000000000, -0.000000000000000000, 0.000000000000000000 ) ) ;
#8144=DIRECTION ( 'NONE',  ( -1.000000000000000000, 0.000000000000000000, -0.000000000000000000 ) ) ;
#8147=ORIENTED_EDGE ( 'NONE', *, *, #46618, .T. ) ;
#8150=VECTOR ( 'NONE', #17661, 1000.000000000000000 ) ;
#8152=ORIENTED_EDGE ( 'NONE', *, *, #6046, .T. ) ;
#8153=CARTESIAN_POINT ( 'NONE',  ( 0.000000000000000000, 5.256550761632864166, 77.32052557432842832 ) ) ;
#8154=FACE_OUTER_BOUND ( 'NONE', #15022, .T. ) ;
#8155=DIRECTION ( 'NONE',  ( 0.000000000000000000, 0.000000000000000000, 1.000000000000000000 ) ) ;
#8162=ORIENTED_EDGE ( 'NONE', *, *, #17582, .T. ) ;
#8164=CIRCLE ( 'NONE', #34738, 31.99999999999998579 ) ;
#8170=ORIENTED_EDGE ( 'NONE', *, *, #5220, .T. ) ;
#8172=AXIS2_PLACEMENT_3D ( 'NONE', #41056, #7517, #34170 ) ;
#8173=DIRECTION ( 'NONE',  ( 0.000000000000000000, 0.8910065241883656784, 0.4539904997395511344 ) ) ;
#8174=CARTESIAN_POINT ( 'NONE',  ( 0.000000000000000000, 73.72996012237460661, -14.67089635893632504 ) ) ;
#8175=CARTESIAN_POINT ( 'NONE',  ( 0.000000000000000000, -74.65491531819124305, 8.830959090342128448 ) ) ;
#8178=DIRECTION ( 'NONE',  ( -1.000000000000000000, -0.000000000000000000, -0.000000000000000000 ) ) ;
#8187=DIRECTION ( 'NONE',  ( -1.000000000000000000, 0.000000000000000000, 0.000000000000000000 ) ) ;
#8198=ORIENTED_EDGE ( 'NONE', *, *, #24318, .T. ) ;
#8202=ORIENTED_EDGE ( 'NONE', *, *, #41548, .T. ) ;
#8208=ORIENTED_EDGE ( 'NONE', *, *, #32162, .T. ) ;
#8209=DIRECTION ( 'NONE',  ( 0.000000000000000000, -0.3826834323650970537, 0.9238795325112838519 ) ) ;
#8210=AXIS2_PLACEMENT_3D ( 'NONE', #31563, #9032, #42572 ) ;
#8211=ORIENTED_EDGE ( 'NONE', *, *, #6036, .T. ) ;
#8213=CARTESIAN_POINT ( 'NONE',  ( 11.99999999999999822, -40.65526001592564853, -71.21200624218839437 ) ) ;
#8215=ORIENTED_EDGE ( 'NONE', *, *, #39208, .F. ) ;
#8220=DIRECTION ( 'NONE',  ( -1.000000000000000000, 0.000000000000000000, 0.000000000000000000 ) ) ;
#8221=EDGE_CURVE ( 'NONE', #23540, #23651, #5329, .T. ) ;
#8222=DIRECTION ( 'NONE',  ( -1.000000000000000000, 0.000000000000000000, -0.000000000000000000 ) ) ;
#8224=CARTESIAN_POINT ( 'NONE',  ( 11.99999999999999822, 55.20638768913760686, 51.02545421589343988 ) ) ;
#8227=DIRECTION ( 'NONE',  ( 0.000000000000000000, 0.000000000000000000, 1.000000000000000000 ) ) ;
#8229=PLANE ( 'NONE',  #31392 ) ;
#8232=CARTESIAN_POINT ( 'NONE',  ( 11.99999999999999822, 5.256550761632864166, 77.32052557432842832 ) ) ;
#8237=DIRECTION ( 'NONE',  ( -1.000000000000000000, -0.000000000000000000, 0.000000000000000000 ) ) ;
#8238=CARTESIAN_POINT ( 'NONE',  ( 0.000000000000000000, 44.88180994100466847, -63.18004540532978552 ) ) ;
#8246=DIRECTION ( 'NONE',  ( 0.000000000000000000, 0.000000000000000000, 1.000000000000000000 ) ) ;
#8258=ORIENTED_EDGE ( 'NONE', *, *, #30845, .F. ) ;
#8263=DIRECTION ( 'NONE',  ( -1.000000000000000000, 0.000000000000000000, -0.000000000000000000 ) ) ;
#8265=VECTOR ( 'NONE', #12493, 1000.000000000000000 ) ;
#8266=FACE_OUTER_BOUND ( 'NONE', #15773, .T. ) ;
#8274=CARTESIAN_POINT ( 'NONE',  ( 11.99999999999999822, -14.67089635893764665, 73.72996012237435082 ) ) ;
#8282=ADVANCED_FACE ( 'NONE', ( #20003 ), #1415, .T. ) ;
#8286=ORIENTED_EDGE ( 'NONE', *, *, #45406, .F. ) ;
#8294=DIRECTION ( 'NONE',  ( -1.000000000000000000, 0.000000000000000000, 0.000000000000000000 ) ) ;
#8300=CARTESIAN_POINT ( 'NONE',  ( 12.00000000000000000, -3.948201729842032215, 23.21447184625297666 ) ) ;
#8301=EDGE_CURVE ( 'NONE', #2161, #44069, #23300, .T. ) ;
#8305=LINE ( 'NONE', #11504, #41945 ) ;
#8308=DIRECTION ( 'NONE',  ( 0.000000000000000000, -0.9969173337331287410, 0.07845909572783489605 ) ) ;
#8309=DIRECTION ( 'NONE',  ( 0.000000000000000000, 0.000000000000000000, 1.000000000000000000 ) ) ;
#8316=CIRCLE ( 'NONE', #20828, 31.99999999999998579 ) ;
#8318=CIRCLE ( 'NONE', #31794, 82.00000000000000000 ) ;
#8319=CARTESIAN_POINT ( 'NONE',  ( -10.00000000000000000, 0.000000000000000000, 0.000000000000000000 ) ) ;
#8325=ORIENTED_EDGE ( 'NONE', *, *, #28301, .F. ) ;
#8328=EDGE_CURVE ( 'NONE', #7146, #16268, #41302, .T. ) ;
#8329=ORIENTED_EDGE ( 'NONE', *, *, #37364, .F. ) ;
#8333=ORIENTED_EDGE ( 'NONE', *, *, #26841, .F. ) ;
#8336=DIRECTION ( 'NONE',  ( -1.000000000000000000, 0.000000000000000000, -0.000000000000000000 ) ) ;
#8340=EDGE_LOOP ( 'NONE', ( #44609, #12918, #28367, #36007 ) ) ;
#8345=CARTESIAN_POINT ( 'NONE',  ( 11.99999999999999822, 0.000000000000000000, 0.000000000000000000 ) ) ;
#8347=ORIENTED_EDGE ( 'NONE', *, *, #34971, .T. ) ;
#8349=CARTESIAN_POINT ( 'NONE',  ( 0.000000000000000000, 0.000000000000000000, 0.000000000000000000 ) ) ;
#8360=DIRECTION ( 'NONE',  ( -1.000000000000000000, -0.000000000000000000, 0.000000000000000000 ) ) ;
#8363=EDGE_CURVE ( 'NONE', #17765, #2093, #43633, .T. ) ;
#8365=CARTESIAN_POINT ( 'NONE',  ( 11.99999999999999822, 5.256550761632864166, 77.32052557432842832 ) ) ;
#8370=DIRECTION ( 'NONE',  ( 0.000000000000000000, 0.8090169943749486725, -0.5877852522924713607 ) ) ;
#8372=ORIENTED_EDGE ( 'NONE', *, *, #35034, .F. ) ;
#8373=EDGE_CURVE ( 'NONE', #46408, #5128, #20956, .T. ) ;
#8374=ORIENTED_EDGE ( 'NONE', *, *, #33058, .F. ) ;
#8375=AXIS2_PLACEMENT_3D ( 'NONE', #6954, #40982, #44639 ) ;
#8376=FACE_BOUND ( 'NONE', #34885, .T. ) ;
#8391=ADVANCED_FACE ( 'NONE', ( #24881 ), #32239, .T. ) ;
#8394=CARTESIAN_POINT ( 'NONE',  ( 11.99999999999999822, 0.000000000000000000, 0.000000000000000000 ) ) ;
#8395=CARTESIAN_POINT ( 'NONE',  ( 5.999999999999999112, 64.81221759200415988, -50.23322058963276504 ) ) ;
#8396=LINE ( 'NONE', #4166, #15010 ) ;
#8398=AXIS2_PLACEMENT_3D ( 'NONE', #2492, #12562, #2041 ) ;
#8403=ORIENTED_EDGE ( 'NONE', *, *, #30960, .T. ) ;
#8409=DIRECTION ( 'NONE',  ( 0.000000000000000000, 0.000000000000000000, 1.000000000000000000 ) ) ;
#8410=EDGE_LOOP ( 'NONE', ( #44745, #23311, #16285, #19016 ) ) ;
#8424=AXIS2_PLACEMENT_3D ( 'NONE', #29976, #41248, #44909 ) ;
#8430=LINE ( 'NONE', #18948, #41676 ) ;
#8439=EDGE_LOOP ( 'NONE', ( #21185, #10334, #34494, #17222 ) ) ;
#8440=ADVANCED_FACE ( 'NONE', ( #48359 ), #22895, .T. ) ;
#8442=EDGE_CURVE ( 'NONE', #40828, #46432, #48301, .T. ) ;
#8450=CARTESIAN_POINT ( 'NONE',  ( 11.99999999999999822, 68.27212725128275395, -31.46837873495001503 ) ) ;
#8452=LINE ( 'NONE', #22896, #35264 ) ;
#8454=ORIENTED_EDGE ( 'NONE', *, *, #25275, .F. ) ;
#8457=ORIENTED_EDGE ( 'NONE', *, *, #18499, .F. ) ;
#8458=EDGE_CURVE ( 'NONE', #17814, #14588, #626, .T. ) ;
#8459=DIRECTION ( 'NONE',  ( 0.000000000000000000, -0.7604059656000369261, 0.6494480483301767748 ) ) ;
#8460=CYLINDRICAL_SURFACE ( 'NONE', #2954, 31.99999999999998579 ) ;
#8465=CARTESIAN_POINT ( 'NONE',  ( 0.000000000000000000, 0.000000000000000000, 0.000000000000000000 ) ) ;
#8473=CARTESIAN_POINT ( 'NONE',  ( 12.00000000000000000, 5.835314593368470248, -22.81335362449854642 ) ) ;
#8477=LINE ( 'NONE', #12887, #14341 ) ;
#8480=DIRECTION ( 'NONE',  ( 0.000000000000000000, 0.000000000000000000, 1.000000000000000000 ) ) ;
#8482=FACE_OUTER_BOUND ( 'NONE', #5510, .T. ) ;
#8483=DIRECTION ( 'NONE',  ( 0.000000000000000000, 0.000000000000000000, -1.000000000000000000 ) ) ;
#8487=ORIENTED_EDGE ( 'NONE', *, *, #46423, .F. ) ;
#8495=CARTESIAN_POINT ( 'NONE',  ( 15.00000000000000000, -0.9646360437375368635, -23.52805723605589705 ) ) ;
#8496=AXIS2_PLACEMENT_3D ( 'NONE', #39344, #32018, #5829 ) ;
#8497=ORIENTED_EDGE ( 'NONE', *, *, #14400, .F. ) ;
#8501=DIRECTION ( 'NONE',  ( 1.000000000000000000, -0.000000000000000000, -0.000000000000000000 ) ) ;
#8502=LINE ( 'NONE', #6883, #21947 ) ;
#8503=CARTESIAN_POINT ( 'NONE',  ( 50.00005079999999680, 0.000000000000000000, 21.00000000000000000 ) ) ;
#8504=ORIENTED_EDGE ( 'NONE', *, *, #19387, .F. ) ;
#8507=EDGE_LOOP ( 'NONE', ( #45427, #40114, #25395, #28622 ) ) ;
#8509=DIRECTION ( 'NONE',  ( 0.000000000000000000, 0.7431448254773862505, -0.6691306063588671194 ) ) ;
#8513=DIRECTION ( 'NONE',  ( -1.000000000000000000, 0.000000000000000000, 0.000000000000000000 ) ) ;
#8516=ORIENTED_EDGE ( 'NONE', *, *, #6749, .F. ) ;
#8523=LINE ( 'NONE', #38397, #19150 ) ;
#8528=CARTESIAN_POINT ( 'NONE',  ( 15.00000000000000000, 0.000000000000000000, 0.000000000000000000 ) ) ;
#8530=LINE ( 'NONE', #4626, #18450 ) ;
#8531=CIRCLE ( 'NONE', #27311, 21.00000000000000000 ) ;
#8532=DIRECTION ( 'NONE',  ( -1.000000000000000000, -0.000000000000000000, 0.000000000000000000 ) ) ;
#8533=AXIS2_PLACEMENT_3D ( 'NONE', #3620, #48402, #11210 ) ;
#8537=EDGE_LOOP ( 'NONE', ( #33036, #45003, #26419, #37825 ) ) ;
#8544=CARTESIAN_POINT ( 'NONE',  ( 0.000000000000000000, 70.53064760720278059, 26.01480285779964774 ) ) ;
#8547=CARTESIAN_POINT ( 'NONE',  ( 0.000000000000000000, 40.65526001592611749, 71.21200624218811015 ) ) ;
#8549=ORIENTED_EDGE ( 'NONE', *, *, #7224, .T. ) ;
#8561=ORIENTED_EDGE ( 'NONE', *, *, #19661, .T. ) ;
#8567=DIRECTION ( 'NONE',  ( 0.000000000000000000, 0.2079116908177532086, -0.9781476007338069101 ) ) ;
#8568=ORIENTED_EDGE ( 'NONE', *, *, #21298, .F. ) ;
#8577=DIRECTION ( 'NONE',  ( -1.000000000000000000, 0.000000000000000000, 0.000000000000000000 ) ) ;
#8585=CARTESIAN_POINT ( 'NONE',  ( 11.99999999999999822, -2.956366410621191765, 75.11725578898467859 ) ) ;
#8587=DIRECTION ( 'NONE',  ( 0.000000000000000000, 0.8660254037844374864, -0.5000000000000019984 ) ) ;
#8588=DIRECTION ( 'NONE',  ( 0.000000000000000000, 0.000000000000000000, -1.000000000000000000 ) ) ;
#8591=CARTESIAN_POINT ( 'NONE',  ( 11.99999999999999822, 0.000000000000000000, 0.000000000000000000 ) ) ;
#8596=ADVANCED_FACE ( 'NONE', ( #42957 ), #8678, .F. ) ;
#8599=ORIENTED_EDGE ( 'NONE', *, *, #39703, .F. ) ;
#8604=ADVANCED_FACE ( 'NONE', ( #20419 ), #38816, .T. ) ;
#8606=AXIS2_PLACEMENT_3D ( 'NONE', #36094, #28522, #17733 ) ;
#8608=DIRECTION ( 'NONE',  ( -1.000000000000000000, -0.000000000000000000, -0.000000000000000000 ) ) ;
#8612=FACE_OUTER_BOUND ( 'NONE', #34990, .T. ) ;
#8615=EDGE_LOOP ( 'NONE', ( #26794, #37995, #18231, #35165 ) ) ;
#8627=CARTESIAN_POINT ( 'NONE',  ( 15.00000000000000000, -1.278221433540145391, 26.51162292216073979 ) ) ;
#8630=CYLINDRICAL_SURFACE ( 'NONE', #43473, 77.49899999999999523 ) ;
#8632=ORIENTED_EDGE ( 'NONE', *, *, #47009, .F. ) ;
#8633=CIRCLE ( 'NONE', #35995, 31.99999999999998579 ) ;
#8635=CARTESIAN_POINT ( 'NONE',  ( 11.99999999999999822, 0.000000000000000000, 0.000000000000000000 ) ) ;
#8637=VERTEX_POINT ( 'NONE', #39273 ) ;
#8643=DIRECTION ( 'NONE',  ( 0.000000000000000000, -0.5877852522924803536, 0.8090169943749422332 ) ) ;
#8644=DIRECTION ( 'NONE',  ( -1.000000000000000000, -0.000000000000000000, 0.000000000000000000 ) ) ;
#8645=DIRECTION ( 'NONE',  ( 0.000000000000000000, -0.9945218953682730678, 0.1045284632676569680 ) ) ;
#8647=DIRECTION ( 'NONE',  ( -1.000000000000000000, -0.000000000000000000, 0.000000000000000000 ) ) ;
#8657=EDGE_CURVE ( 'NONE', #39152, #40727, #7705, .T. ) ;
#8662=ORIENTED_EDGE ( 'NONE', *, *, #23365, .F. ) ;
#8663=CIRCLE ( 'NONE', #6314, 31.99999999999998934 ) ;
#8666=ORIENTED_EDGE ( 'NONE', *, *, #645, .F. ) ;
#8670=CARTESIAN_POINT ( 'NONE',  ( 11.99999999999999822, 0.000000000000000000, 0.000000000000000000 ) ) ;
#8673=CARTESIAN_POINT ( 'NONE',  ( 5.999999999999999112, -60.67117009219097667, -55.16347631943106933 ) ) ;
#8676=ORIENTED_EDGE ( 'NONE', *, *, #5110, .F. ) ;
#8678=PLANE ( 'NONE',  #13200 ) ;
#8682=ORIENTED_EDGE ( 'NONE', *, *, #38710, .T. ) ;
#8694=CARTESIAN_POINT ( 'NONE',  ( 0.000000000000000000, 77.49459641780886443, -0.8261519478433960728 ) ) ;
#8695=DIRECTION ( 'NONE',  ( -1.000000000000000000, 0.000000000000000000, 0.000000000000000000 ) ) ;
#8697=EDGE_CURVE ( 'NONE', #32725, #7093, #2085, .T. ) ;
#8702=AXIS2_PLACEMENT_3D ( 'NONE', #31958, #46873, #42723 ) ;
#8704=CIRCLE ( 'NONE', #20402, 77.49899999999999523 ) ;
#8706=DIRECTION ( 'NONE',  ( -1.000000000000000000, 0.000000000000000000, 0.000000000000000000 ) ) ;
#8707=CARTESIAN_POINT ( 'NONE',  ( 11.99999999999999822, 31.47745569255140552, 68.26794271651274926 ) ) ;
#8708=CARTESIAN_POINT ( 'NONE',  ( 0.000000000000000000, -59.03961581697432592, 46.53671651293927880 ) ) ;
#8712=CYLINDRICAL_SURFACE ( 'NONE', #23201, 31.99999999999998579 ) ;
#8713=DIRECTION ( 'NONE',  ( 0.000000000000000000, 0.000000000000000000, 1.000000000000000000 ) ) ;
#8722=VERTEX_POINT ( 'NONE', #40491 ) ;
#8728=FACE_OUTER_BOUND ( 'NONE', #11576, .T. ) ;
#8731=AXIS2_PLACEMENT_3D ( 'NONE', #8872, #13050, #16711 ) ;
#8734=CARTESIAN_POINT ( 'NONE',  ( 0.000000000000000000, 0.000000000000000000, 0.000000000000000000 ) ) ;
#8737=CIRCLE ( 'NONE', #19669, 77.49899999999999523 ) ;
#8740=CARTESIAN_POINT ( 'NONE',  ( 6.000000000000000000, -39.47590169984795239, -71.87247863392455827 ) ) ;
#8743=FACE_OUTER_BOUND ( 'NONE', #12669, .T. ) ;
#8748=EDGE_LOOP ( 'NONE', ( #32969, #11818, #13023, #728 ) ) ;
#8749=CARTESIAN_POINT ( 'NONE',  ( 6.000000000000000000, 80.28980883073758434, 16.65972982744962749 ) ) ;
#8753=DIRECTION ( 'NONE',  ( -1.000000000000000000, 0.000000000000000000, 0.000000000000000000 ) ) ;
#8756=ORIENTED_EDGE ( 'NONE', *, *, #43118, .T. ) ;
#8758=CARTESIAN_POINT ( 'NONE',  ( -10.00000000000000000, 0.000000000000000000, 0.000000000000000000 ) ) ;
#8760=DIRECTION ( 'NONE',  ( 1.000000000000000000, -0.000000000000000000, 0.000000000000000000 ) ) ;
#8761=ORIENTED_EDGE ( 'NONE', *, *, #40944, .T. ) ;
#8762=CARTESIAN_POINT ( 'NONE',  ( 15.00000000000000000, -23.29833615347104470, 3.418703333116808629 ) ) ;
#8777=CIRCLE ( 'NONE', #44733, 31.99999999999999289 ) ;
#8778=ORIENTED_EDGE ( 'NONE', *, *, #19428, .T. ) ;
#8782=VECTOR ( 'NONE', #10169, 1000.000000000000000 ) ;
#8784=DIRECTION ( 'NONE',  ( 0.000000000000000000, 0.000000000000000000, 1.000000000000000000 ) ) ;
#8788=VECTOR ( 'NONE', #12748, 1000.000000000000000 ) ;
#8789=EDGE_LOOP ( 'NONE', ( #16135, #43135, #14463, #5895 ) ) ;
#8797=ORIENTED_EDGE ( 'NONE', *, *, #47722, .F. ) ;
#8798=ORIENTED_EDGE ( 'NONE', *, *, #13609, .F. ) ;
#8804=CARTESIAN_POINT ( 'NONE',  ( 11.99999999999999822, 0.000000000000000000, 0.000000000000000000 ) ) ;
#8805=DIRECTION ( 'NONE',  ( 0.000000000000000000, 0.000000000000000000, 1.000000000000000000 ) ) ;
#8809=ORIENTED_EDGE ( 'NONE', *, *, #21298, .T. ) ;
#8811=FACE_OUTER_BOUND ( 'NONE', #11633, .T. ) ;
#8820=EDGE_CURVE ( 'NONE', #25146, #44798, #39774, .T. ) ;
#8821=CARTESIAN_POINT ( 'NONE',  ( 11.99999999999999822, -36.72794159290288718, 65.59268652807197952 ) ) ;
#8824=EDGE_CURVE ( 'NONE', #18965, #16392, #13166, .T. ) ;
#8825=DIRECTION ( 'NONE',  ( 0.000000000000000000, 0.000000000000000000, 1.000000000000000000 ) ) ;
#8826=DIRECTION ( 'NONE',  ( 0.000000000000000000, 0.000000000000000000, 1.000000000000000000 ) ) ;
#8843=CARTESIAN_POINT ( 'NONE',  ( 15.00000000000000000, -18.13022148937263012, -15.02647892043543898 ) ) ;
#8844=ORIENTED_EDGE ( 'NONE', *, *, #32751, .T. ) ;
#8845=CARTESIAN_POINT ( 'NONE',  ( 15.00000000000000000, 22.07842321921480888, -8.187992925817425771 ) ) ;
#8846=CIRCLE ( 'NONE', #23698, 31.99999999999998579 ) ;
#8859=CARTESIAN_POINT ( 'NONE',  ( 11.99999999999999822, -72.35432306680498016, 20.40083707022857951 ) ) ;
#8862=LINE ( 'NONE', #1533, #3968 ) ;
#8863=ORIENTED_EDGE ( 'NONE', *, *, #36353, .T. ) ;
#8865=ORIENTED_EDGE ( 'NONE', *, *, #25043, .F. ) ;
#8866=ORIENTED_EDGE ( 'NONE', *, *, #23542, .F. ) ;
#8867=EDGE_LOOP ( 'NONE', ( #13546, #6420, #7772, #260 ) ) ;
#8872=CARTESIAN_POINT ( 'NONE',  ( 15.00000000000000000, 8.688484142253932063, -21.88630264137371029 ) ) ;
#8874=CARTESIAN_POINT ( 'NONE',  ( 0.000000000000000000, 20.40083707022882820, 72.35432306680490910 ) ) ;
#8878=VERTEX_POINT ( 'NONE', #8153 ) ;
#8879=VERTEX_POINT ( 'NONE', #26520 ) ;
#8881=CARTESIAN_POINT ( 'NONE',  ( 11.99999999999999822, 36.72794159290241822, 65.59268652807223532 ) ) ;
#8882=AXIS2_PLACEMENT_3D ( 'NONE', #40332, #14125, #18020 ) ;
#8887=DIRECTION ( 'NONE',  ( -1.000000000000000000, -0.000000000000000000, 0.000000000000000000 ) ) ;
#8891=CYLINDRICAL_SURFACE ( 'NONE', #29143, 31.99999999999998579 ) ;
#8898=CARTESIAN_POINT ( 'NONE',  ( 15.00000000000000000, 14.60985201121703980, -18.46759930825707841 ) ) ;
#8900=AXIS2_PLACEMENT_3D ( 'NONE', #13256, #9103, #2014 ) ;
#8903=CIRCLE ( 'NONE', #4996, 82.00000000000000000 ) ;
#8905=ORIENTED_EDGE ( 'NONE', *, *, #4342, .F. ) ;
#8913=EDGE_CURVE ( 'NONE', #39232, #24980, #5056, .T. ) ;
#8914=CIRCLE ( 'NONE', #47969, 31.99999999999998224 ) ;
#8915=AXIS2_PLACEMENT_3D ( 'NONE', #37427, #30335, #48431 ) ;
#8921=CIRCLE ( 'NONE', #1092, 31.99999999999998579 ) ;
#8922=CARTESIAN_POINT ( 'NONE',  ( 15.00000000000000000, -1.278221433540507546, -26.51162292216071492 ) ) ;
#8935=ORIENTED_EDGE ( 'NONE', *, *, #24733, .T. ) ;
#8936=ADVANCED_FACE ( 'NONE', ( #73 ), #29942, .T. ) ;
#8940=ORIENTED_EDGE ( 'NONE', *, *, #22166, .F. ) ;
#8942=ADVANCED_FACE ( 'NONE', ( #41215 ), #11591, .T. ) ;
#8944=DIRECTION ( 'NONE',  ( 0.000000000000000000, 0.000000000000000000, 1.000000000000000000 ) ) ;
#8950=DIRECTION ( 'NONE',  ( -1.000000000000000000, -0.000000000000000000, -0.000000000000000000 ) ) ;
#8960=DIRECTION ( 'NONE',  ( -1.000000000000000000, -0.000000000000000000, -0.000000000000000000 ) ) ;
#8969=DIRECTION ( 'NONE',  ( 1.000000000000000000, 0.000000000000000000, 0.000000000000000000 ) ) ;
#8971=ORIENTED_EDGE ( 'NONE', *, *, #43604, .F. ) ;
#8973=VECTOR ( 'NONE', #6900, 1000.000000000000000 ) ;
#8976=DIRECTION ( 'NONE',  ( -1.000000000000000000, 0.000000000000000000, -0.000000000000000000 ) ) ;
#8980=VERTEX_POINT ( 'NONE', #7439 ) ;
#8982=CARTESIAN_POINT ( 'NONE',  ( 15.00000000000000000, 20.85821328998756385, 10.92862929874494249 ) ) ;
#8983=ORIENTED_EDGE ( 'NONE', *, *, #14084, .F. ) ;
#8984=ORIENTED_EDGE ( 'NONE', *, *, #10679, .F. ) ;
#8985=AXIS2_PLACEMENT_3D ( 'NONE', #3777, #18699, #26051 ) ;
#8991=ORIENTED_EDGE ( 'NONE', *, *, #29966, .F. ) ;
#8993=LINE ( 'NONE', #8740, #39147 ) ;
#8995=DIRECTION ( 'NONE',  ( -1.000000000000000000, 0.000000000000000000, 0.000000000000000000 ) ) ;
#8996=VECTOR ( 'NONE', #6710, 1000.000000000000227 ) ;
#9001=VERTEX_POINT ( 'NONE', #16709 ) ;
#9004=ORIENTED_EDGE ( 'NONE', *, *, #31031, .T. ) ;
#9005=EDGE_CURVE ( 'NONE', #44556, #22290, #34731, .T. ) ;
#9009=FACE_OUTER_BOUND ( 'NONE', #32352, .T. ) ;
#9010=EDGE_CURVE ( 'NONE', #9234, #4565, #46578, .T. ) ;
#9014=AXIS2_PLACEMENT_3D ( 'NONE', #2911, #40597, #25420 ) ;
#9017=EDGE_CURVE ( 'NONE', #27718, #17850, #47258, .T. ) ;
#9018=CARTESIAN_POINT ( 'NONE',  ( 5.999999999999999112, 50.23322058963442771, -64.81221759200288091 ) ) ;
#9021=FACE_OUTER_BOUND ( 'NONE', #28927, .T. ) ;
#9022=ORIENTED_EDGE ( 'NONE', *, *, #20098, .T. ) ;
#9023=DIRECTION ( 'NONE',  ( -1.000000000000000000, 0.000000000000000000, 0.000000000000000000 ) ) ;
#9024=FACE_OUTER_BOUND ( 'NONE', #38196, .T. ) ;
#9029=DIRECTION ( 'NONE',  ( -1.000000000000000000, 0.000000000000000000, 0.000000000000000000 ) ) ;
#9032=DIRECTION ( 'NONE',  ( -1.000000000000000000, 0.000000000000000000, 0.000000000000000000 ) ) ;
#9040=DIRECTION ( 'NONE',  ( 0.000000000000000000, 0.000000000000000000, 1.000000000000000000 ) ) ;
#9041=ORIENTED_EDGE ( 'NONE', *, *, #41962, .F. ) ;
#9047=CIRCLE ( 'NONE', #9014, 77.49899999999999523 ) ;
#9051=ORIENTED_EDGE ( 'NONE', *, *, #28276, .T. ) ;
#9052=CIRCLE ( 'NONE', #42676, 31.99999999999999289 ) ;
#9053=ORIENTED_EDGE ( 'NONE', *, *, #23519, .T. ) ;
#9054=AXIS2_PLACEMENT_3D ( 'NONE', #19196, #37321, #15530 ) ;
#9061=EDGE_CURVE ( 'NONE', #29866, #18807, #30726, .T. ) ;
#9067=ORIENTED_EDGE ( 'NONE', *, *, #20906, .T. ) ;
#9068=ADVANCED_FACE ( 'NONE', ( #27978 ), #9122, .T. ) ;
#9074=CARTESIAN_POINT ( 'NONE',  ( -10.00000000000000000, 0.000000000000000000, 0.000000000000000000 ) ) ;
#9075=ORIENTED_EDGE ( 'NONE', *, *, #32162, .F. ) ;
#9076=VERTEX_POINT ( 'NONE', #5691 ) ;
#9078=CARTESIAN_POINT ( 'NONE',  ( 0.000000000000000000, 23.16143007188530234, -73.95703589263949596 ) ) ;
#9084=VECTOR ( 'NONE', #12037, 1000.000000000000114 ) ;
#9085=CARTESIAN_POINT ( 'NONE',  ( 0.000000000000000000, 34.44570377933693806, -69.42325613327405165 ) ) ;
#9090=CARTESIAN_POINT ( 'NONE',  ( 0.000000000000000000, 0.000000000000000000, 0.000000000000000000 ) ) ;
#9103=DIRECTION ( 'NONE',  ( 1.000000000000000000, 0.000000000000000000, 0.000000000000000000 ) ) ;
#9105=CIRCLE ( 'NONE', #13800, 31.99999999999999645 ) ;
#9106=FACE_OUTER_BOUND ( 'NONE', #4051, .T. ) ;
#9114=CARTESIAN_POINT ( 'NONE',  ( 15.00000000000000000, 23.49999999999999645, 1.499999999999995337 ) ) ;
#9122=CYLINDRICAL_SURFACE ( 'NONE', #48013, 77.49899999999999523 ) ;
#9123=LINE ( 'NONE', #8395, #34065 ) ;
#9124=CYLINDRICAL_SURFACE ( 'NONE', #38444, 77.49899999999999523 ) ;
#9127=LINE ( 'NONE', #47292, #24236 ) ;
#9129=DIRECTION ( 'NONE',  ( 0.000000000000000000, -0.9781476007338065770, -0.2079116908177544853 ) ) ;
#9134=DIRECTION ( 'NONE',  ( 0.000000000000000000, 0.7071067811865437980, 0.7071067811865513475 ) ) ;
#9135=EDGE_CURVE ( 'NONE', #25765, #39311, #43140, .T. ) ;
#9138=ORIENTED_EDGE ( 'NONE', *, *, #13886, .F. ) ;
#9139=CARTESIAN_POINT ( 'NONE',  ( 0.000000000000000000, -17.28742895386137590, 75.54627589209937355 ) ) ;
#9140=LINE ( 'NONE', #31920, #26817 ) ;
#9142=CARTESIAN_POINT ( 'NONE',  ( 0.000000000000000000, -62.50884508063395373, -41.76106447765554464 ) ) ;
#9145=CARTESIAN_POINT ( 'NONE',  ( 0.000000000000000000, 41.76937507738875155, -62.50329211542393892 ) ) ;
#9149=CIRCLE ( 'NONE', #23998, 31.99999999999998579 ) ;
#9152=ORIENTED_EDGE ( 'NONE', *, *, #47155, .F. ) ;
#9153=DIRECTION ( 'NONE',  ( 0.000000000000000000, -0.9510565162951503115, 0.3090169943749573878 ) ) ;
#9168=DIRECTION ( 'NONE',  ( 0.000000000000000000, 0.000000000000000000, -1.000000000000000000 ) ) ;
#9177=EDGE_CURVE ( 'NONE', #38028, #9618, #36261, .T. ) ;
#9180=PLANE ( 'NONE',  #3206 ) ;
#9182=ORIENTED_EDGE ( 'NONE', *, *, #15584, .T. ) ;
#9185=CARTESIAN_POINT ( 'NONE',  ( 11.99999999999999822, 59.03961581697399907, 46.53671651293969802 ) ) ;
#9190=DIRECTION ( 'NONE',  ( 0.000000000000000000, -0.07845909572785234043, 0.9969173337331274087 ) ) ;
#9191=CARTESIAN_POINT ( 'NONE',  ( 12.00000000000000000, -19.89357724624986545, 12.59942793731086219 ) ) ;
#9194=ORIENTED_EDGE ( 'NONE', *, *, #3886, .F. ) ;
#9200=ORIENTED_EDGE ( 'NONE', *, *, #31456, .T. ) ;
#9202=DIRECTION ( 'NONE',  ( 1.000000000000000000, -0.000000000000000000, -0.000000000000000000 ) ) ;
#9203=CARTESIAN_POINT ( 'NONE',  ( 11.99999999999999822, 30.41916302227216562, -71.27951684757994144 ) ) ;
#9204=CYLINDRICAL_SURFACE ( 'NONE', #6030, 21.00000000000000000 ) ;
#9210=CARTESIAN_POINT ( 'NONE',  ( -10.00000000000000000, 0.000000000000000000, 0.000000000000000000 ) ) ;
#9217=EDGE_CURVE ( 'NONE', #46297, #44946, #12085, .T. ) ;
#9218=ORIENTED_EDGE ( 'NONE', *, *, #39972, .F. ) ;
#9219=EDGE_CURVE ( 'NONE', #30611, #11880, #5948, .T. ) ;
#9226=CARTESIAN_POINT ( 'NONE',  ( 11.99999999999999822, 69.42325613327440692, 34.44570377933622041 ) ) ;
#9234=VERTEX_POINT ( 'NONE', #2728 ) ;
#9235=VECTOR ( 'NONE', #33211, 1000.000000000000000 ) ;
#9238=DIRECTION ( 'NONE',  ( 0.000000000000000000, 0.000000000000000000, 1.000000000000000000 ) ) ;
#9240=ORIENTED_EDGE ( 'NONE', *, *, #12240, .F. ) ;
#9241=DIRECTION ( 'NONE',  ( -1.000000000000000000, -0.000000000000000000, -0.000000000000000000 ) ) ;
#9242=CARTESIAN_POINT ( 'NONE',  ( 0.000000000000000000, -75.11725578898466438, -2.956366410621452001 ) ) ;
#9247=FACE_OUTER_BOUND ( 'NONE', #31198, .T. ) ;
#9252=EDGE_CURVE ( 'NONE', #29586, #18510, #9721, .T. ) ;
#9257=CARTESIAN_POINT ( 'NONE',  ( 11.99999999999999822, -70.52718814184277107, 26.02418014898285037 ) ) ;
#9260=DIRECTION ( 'NONE',  ( -1.000000000000000000, 0.000000000000000000, -0.000000000000000000 ) ) ;
#9265=DIRECTION ( 'NONE',  ( -1.000000000000000000, 0.000000000000000000, -0.000000000000000000 ) ) ;
#9274=CARTESIAN_POINT ( 'NONE',  ( 11.99999999999999822, -27.74655509720618696, -77.16300072079690153 ) ) ;
#9276=EDGE_CURVE ( 'NONE', #11173, #28070, #45600, .T. ) ;
#9278=ORIENTED_EDGE ( 'NONE', *, *, #382, .T. ) ;
#9281=CARTESIAN_POINT ( 'NONE',  ( 11.99999999999999822, 74.65491531819118620, -8.830959090342659579 ) ) ;
#9283=ORIENTED_EDGE ( 'NONE', *, *, #25343, .F. ) ;
#9284=ORIENTED_EDGE ( 'NONE', *, *, #7990, .F. ) ;
#9286=EDGE_CURVE ( 'NONE', #26342, #4178, #47996, .T. ) ;
#9288=CARTESIAN_POINT ( 'NONE',  ( 0.000000000000000000, 29.01471420065563933, 76.69515212746026123 ) ) ;
#9291=EDGE_CURVE ( 'NONE', #37286, #675, #26037, .T. ) ;
#9292=EDGE_LOOP ( 'NONE', ( #29729, #36986, #18583, #14951 ) ) ;
#9294=FACE_OUTER_BOUND ( 'NONE', #30332, .T. ) ;
#9304=AXIS2_PLACEMENT_3D ( 'NONE', #38365, #19496, #437 ) ;
#9307=DIRECTION ( 'NONE',  ( -1.000000000000000000, 0.000000000000000000, 0.000000000000000000 ) ) ;
#9310=DIRECTION ( 'NONE',  ( -1.000000000000000000, -0.000000000000000000, 0.000000000000000000 ) ) ;
#9311=CARTESIAN_POINT ( 'NONE',  ( 0.000000000000000000, -49.70050353004931054, 59.46389618801946142 ) ) ;
#9312=DIRECTION ( 'NONE',  ( -1.000000000000000000, -0.000000000000000000, -0.000000000000000000 ) ) ;
#9314=LINE ( 'NONE', #39430, #44550 ) ;
#9320=CARTESIAN_POINT ( 'NONE',  ( 11.99999999999999822, -51.03279382321125723, 55.19960302592048862 ) ) ;
#9322=DIRECTION ( 'NONE',  ( 0.000000000000000000, -0.6494480483301739993, -0.7604059656000391465 ) ) ;
#9327=EDGE_LOOP ( 'NONE', ( #36957, #154, #3708, #12635 ) ) ;
#9331=EDGE_CURVE ( 'NONE', #38290, #46458, #9638, .T. ) ;
#9335=CYLINDRICAL_SURFACE ( 'NONE', #26055, 31.99999999999998579 ) ;
#9340=DIRECTION ( 'NONE',  ( 1.000000000000000000, -0.000000000000000000, -0.000000000000000000 ) ) ;
#9342=CARTESIAN_POINT ( 'NONE',  ( 15.00000000000000000, -13.04903810567675393, -19.60159698893424718 ) ) ;
#9346=VECTOR ( 'NONE', #23683, 1000.000000000000000 ) ;
#9347=CARTESIAN_POINT ( 'NONE',  ( 0.000000000000000000, 0.000000000000000000, 0.000000000000000000 ) ) ;
#9348=ORIENTED_EDGE ( 'NONE', *, *, #10374, .F. ) ;
#9350=EDGE_LOOP ( 'NONE', ( #30926, #21246, #23950, #41986 ) ) ;
#9351=EDGE_LOOP ( 'NONE', ( #31272, #27537, #9240, #46200 ) ) ;
#9357=DIRECTION ( 'NONE',  ( -1.000000000000000000, -0.000000000000000000, -0.000000000000000000 ) ) ;
#9358=ORIENTED_EDGE ( 'NONE', *, *, #22674, .T. ) ;
#9360=ORIENTED_EDGE ( 'NONE', *, *, #35594, .T. ) ;
#9366=ORIENTED_EDGE ( 'NONE', *, *, #17209, .F. ) ;
#9368=CARTESIAN_POINT ( 'NONE',  ( 11.99999999999999822, 46.53671651294032330, -59.03961581697353012 ) ) ;
#9369=CARTESIAN_POINT ( 'NONE',  ( 0.000000000000000000, 0.000000000000000000, 0.000000000000000000 ) ) ;
#9371=DIRECTION ( 'NONE',  ( 0.000000000000000000, 0.5877852522924743583, -0.8090169943749466741 ) ) ;
#9375=CARTESIAN_POINT ( 'NONE',  ( 11.99999999999999822, -2.543863470248965086, 81.96053171279902472 ) ) ;
#9384=VERTEX_POINT ( 'NONE', #33785 ) ;
#9388=DIRECTION ( 'NONE',  ( 0.000000000000000000, 0.000000000000000000, 1.000000000000000000 ) ) ;
#9395=VECTOR ( 'NONE', #15796, 1000.000000000000000 ) ;
#9396=CARTESIAN_POINT ( 'NONE',  ( 15.00000000000000000, -13.04903810567646971, 19.60159698893442481 ) ) ;
#9399=ORIENTED_EDGE ( 'NONE', *, *, #22398, .F. ) ;
#9402=EDGE_CURVE ( 'NONE', #38262, #43286, #11200, .T. ) ;
#9403=EDGE_LOOP ( 'NONE', ( #21580, #2788, #20525, #9200 ) ) ;
#9411=CARTESIAN_POINT ( 'NONE',  ( 0.000000000000000000, 0.000000000000000000, 0.000000000000000000 ) ) ;
#9412=VERTEX_POINT ( 'NONE', #18386 ) ;
#9415=CYLINDRICAL_SURFACE ( 'NONE', #41966, 31.99999999999998579 ) ;
#9416=EDGE_LOOP ( 'NONE', ( #27642, #27614, #22883, #44329 ) ) ;
#9419=CARTESIAN_POINT ( 'NONE',  ( 0.000000000000000000, -11.30684508768393570, 76.66974797899831628 ) ) ;
#9421=DIRECTION ( 'NONE',  ( 0.000000000000000000, 0.7431448254773954654, 0.6691306063588569053 ) ) ;
#9426=FACE_OUTER_BOUND ( 'NONE', #10704, .T. ) ;
#9428=ORIENTED_EDGE ( 'NONE', *, *, #19533, .F. ) ;
#9429=DIRECTION ( 'NONE',  ( -1.000000000000000000, -0.000000000000000000, 0.000000000000000000 ) ) ;
#9435=DIRECTION ( 'NONE',  ( 0.000000000000000000, -0.1045284632676558301, -0.9945218953682731788 ) ) ;
#9436=AXIS2_PLACEMENT_3D ( 'NONE', #589, #34112, #29483 ) ;
#9439=AXIS2_PLACEMENT_3D ( 'NONE', #32010, #17285, #9465 ) ;
#9448=EDGE_CURVE ( 'NONE', #19576, #9873, #12004, .T. ) ;
#9452=AXIS2_PLACEMENT_3D ( 'NONE', #29109, #39678, #2677 ) ;
#9455=EDGE_CURVE ( 'NONE', #2177, #41443, #24506, .T. ) ;
#9465=DIRECTION ( 'NONE',  ( 0.000000000000000000, 0.000000000000000000, -1.000000000000000000 ) ) ;
#9471=DIRECTION ( 'NONE',  ( 0.000000000000000000, 0.000000000000000000, 1.000000000000000000 ) ) ;
#9474=VECTOR ( 'NONE', #24473, 999.9999999999998863 ) ;
#9477=DIRECTION ( 'NONE',  ( 0.000000000000000000, 0.000000000000000000, 1.000000000000000000 ) ) ;
#9479=ORIENTED_EDGE ( 'NONE', *, *, #3491, .T. ) ;
#9480=AXIS2_PLACEMENT_3D ( 'NONE', #21037, #17844, #5893 ) ;
#9484=DIRECTION ( 'NONE',  ( -1.000000000000000000, -0.000000000000000000, 0.000000000000000000 ) ) ;
#9494=FACE_OUTER_BOUND ( 'NONE', #7832, .T. ) ;
#9501=CARTESIAN_POINT ( 'NONE',  ( 0.000000000000000000, 22.90783923731629201, 78.73519480814962890 ) ) ;
#9506=VERTEX_POINT ( 'NONE', #2370 ) ;
#9511=ORIENTED_EDGE ( 'NONE', *, *, #7555, .F. ) ;
#9521=ORIENTED_EDGE ( 'NONE', *, *, #4749, .T. ) ;
#9530=ORIENTED_EDGE ( 'NONE', *, *, #32231, .T. ) ;
#9532=LINE ( 'NONE', #46768, #7072 ) ;
#9533=DIRECTION ( 'NONE',  ( 0.000000000000000000, -0.5877852522924797984, -0.8090169943749426773 ) ) ;
#9534=DIRECTION ( 'NONE',  ( -1.000000000000000000, 0.000000000000000000, 0.000000000000000000 ) ) ;
#9536=ORIENTED_EDGE ( 'NONE', *, *, #31691, .F. ) ;
#9545=CARTESIAN_POINT ( 'NONE',  ( 11.99999999999999822, 0.000000000000000000, 0.000000000000000000 ) ) ;
#9548=CYLINDRICAL_SURFACE ( 'NONE', #31819, 31.99999999999998579 ) ;
#9552=DIRECTION ( 'NONE',  ( -0.000000000000000000, 0.9781476007338042455, -0.2079116908177663092 ) ) ;
#9555=CARTESIAN_POINT ( 'NONE',  ( 15.00000000000000000, -14.54903810567676636, -22.19967320028755964 ) ) ;
#9563=DIRECTION ( 'NONE',  ( -1.000000000000000000, 0.000000000000000000, -0.000000000000000000 ) ) ;
#9566=VERTEX_POINT ( 'NONE', #31792 ) ;
#9569=VECTOR ( 'NONE', #6593, 1000.000000000000000 ) ;
#9575=VECTOR ( 'NONE', #13066, 1000.000000000000000 ) ;
#9578=DIRECTION ( 'NONE',  ( 0.000000000000000000, 0.000000000000000000, 1.000000000000000000 ) ) ;
#9581=ORIENTED_EDGE ( 'NONE', *, *, #30622, .F. ) ;
#9582=CIRCLE ( 'NONE', #40107, 77.49900000000000944 ) ;
#9583=EDGE_LOOP ( 'NONE', ( #8971, #32310, #23132, #38544 ) ) ;
#9592=ORIENTED_EDGE ( 'NONE', *, *, #6096, .T. ) ;
#9594=LINE ( 'NONE', #28453, #25383 ) ;
#9595=ORIENTED_EDGE ( 'NONE', *, *, #26268, .T. ) ;
#9598=CARTESIAN_POINT ( 'NONE',  ( 11.99999999999999822, 59.03342792756263435, 46.54456581323825048 ) ) ;
#9600=EDGE_LOOP ( 'NONE', ( #28130, #734, #33604, #12330 ) ) ;
#9604=DIRECTION ( 'NONE',  ( 0.000000000000000000, -0.1564344650402170744, -0.9876883405951398798 ) ) ;
#9609=CARTESIAN_POINT ( 'NONE',  ( 11.99999999999999822, 80.55351364060588537, 15.33399622253511829 ) ) ;
#9612=DIRECTION ( 'NONE',  ( -1.000000000000000000, -0.000000000000000000, -0.000000000000000000 ) ) ;
#9613=DIRECTION ( 'NONE',  ( 0.000000000000000000, 0.000000000000000000, 1.000000000000000000 ) ) ;
#9615=CARTESIAN_POINT ( 'NONE',  ( 0.000000000000000000, 44.88180994100376608, 63.18004540533043922 ) ) ;
#9618=VERTEX_POINT ( 'NONE', #25127 ) ;
#9621=ORIENTED_EDGE ( 'NONE', *, *, #25340, .T. ) ;
#9625=VERTEX_POINT ( 'NONE', #36866 ) ;
#9626=EDGE_CURVE ( 'NONE', #38560, #2609, #47640, .T. ) ;
#9627=CARTESIAN_POINT ( 'NONE',  ( 11.99999999999999822, 0.000000000000000000, 0.000000000000000000 ) ) ;
#9629=EDGE_CURVE ( 'NONE', #19662, #5981, #25286, .T. ) ;
#9631=VECTOR ( 'NONE', #32518, 1000.000000000000000 ) ;
#9633=ORIENTED_EDGE ( 'NONE', *, *, #2817, .T. ) ;
#9638=CIRCLE ( 'NONE', #8072, 77.49899999999999523 ) ;
#9646=ORIENTED_EDGE ( 'NONE', *, *, #27366, .T. ) ;
#9650=EDGE_CURVE ( 'NONE', #34450, #12269, #9685, .T. ) ;
#9653=ORIENTED_EDGE ( 'NONE', *, *, #28013, .F. ) ;
#9654=ORIENTED_EDGE ( 'NONE', *, *, #15439, .F. ) ;
#9655=DIRECTION ( 'NONE',  ( 0.000000000000000000, 0.2334453638559058908, -0.9723699203976765570 ) ) ;
#9660=CIRCLE ( 'NONE', #24565, 77.49900000000000944 ) ;
#9663=DIRECTION ( 'NONE',  ( 1.000000000000000000, 0.000000000000000000, 0.000000000000000000 ) ) ;
#9664=EDGE_CURVE ( 'NONE', #19091, #16230, #12051, .T. ) ;
#9671=DIRECTION ( 'NONE',  ( 0.000000000000000000, -0.8090169943749401238, -0.5877852522924831291 ) ) ;
#9672=ORIENTED_EDGE ( 'NONE', *, *, #19813, .T. ) ;
#9680=CYLINDRICAL_SURFACE ( 'NONE', #42017, 31.99999999999998579 ) ;
#9682=EDGE_LOOP ( 'NONE', ( #33485, #37240, #41586, #39407 ) ) ;
#9684=CARTESIAN_POINT ( 'NONE',  ( 12.00000000000000000, -3.948201729842355068, -23.21447184625292692 ) ) ;
#9685=CIRCLE ( 'NONE', #8882, 77.49899999999999523 ) ;
#9687=ORIENTED_EDGE ( 'NONE', *, *, #7105, .T. ) ;
#9688=ORIENTED_EDGE ( 'NONE', *, *, #30411, .T. ) ;
#9694=CIRCLE ( 'NONE', #16734, 82.00000000000000000 ) ;
#9696=AXIS2_PLACEMENT_3D ( 'NONE', #8004, #33475, #31451 ) ;
#9697=CARTESIAN_POINT ( 'NONE',  ( -10.00000000000000000, 0.000000000000000000, 0.000000000000000000 ) ) ;
#9699=CIRCLE ( 'NONE', #5807, 82.00000000000000000 ) ;
#9700=EDGE_LOOP ( 'NONE', ( #47177, #26755, #34048, #33469 ) ) ;
#9701=CARTESIAN_POINT ( 'NONE',  ( 11.99999999999999822, -75.11764819372145041, -2.946379043147127064 ) ) ;
#9704=ORIENTED_EDGE ( 'NONE', *, *, #14418, .F. ) ;
#9711=DIRECTION ( 'NONE',  ( 0.000000000000000000, 0.000000000000000000, 1.000000000000000000 ) ) ;
#9714=DIRECTION ( 'NONE',  ( -1.000000000000000000, -0.000000000000000000, -0.000000000000000000 ) ) ;
#9716=DIRECTION ( 'NONE',  ( -1.000000000000000000, 0.000000000000000000, -0.000000000000000000 ) ) ;
#9721=CIRCLE ( 'NONE', #7274, 31.99999999999998934 ) ;
#9722=ADVANCED_FACE ( 'NONE', ( #37115 ), #3586, .T. ) ;
#9724=EDGE_CURVE ( 'NONE', #6346, #25011, #34693, .T. ) ;
#9725=EDGE_CURVE ( 'NONE', #7570, #40885, #47181, .T. ) ;
#9733=ADVANCED_FACE ( 'NONE', ( #9969 ), #24895, .F. ) ;
#9736=CARTESIAN_POINT ( 'NONE',  ( 11.99999999999999822, 28.89263327155849126, -71.91182617369157981 ) ) ;
#9741=DIRECTION ( 'NONE',  ( -1.000000000000000000, 0.000000000000000000, 0.000000000000000000 ) ) ;
#9742=AXIS2_PLACEMENT_3D ( 'NONE', #15573, #7259, #26831 ) ;
#9750=EDGE_CURVE ( 'NONE', #13159, #23062, #28811, .T. ) ;
#9754=ORIENTED_EDGE ( 'NONE', *, *, #21373, .T. ) ;
#9755=ORIENTED_EDGE ( 'NONE', *, *, #36786, .F. ) ;
#9758=DIRECTION ( 'NONE',  ( 0.000000000000000000, -0.7604059656000227152, -0.6494480483301934282 ) ) ;
#9765=EDGE_CURVE ( 'NONE', #12329, #26225, #23726, .T. ) ;
#9767=EDGE_LOOP ( 'NONE', ( #2315, #46040, #46319, #35115 ) ) ;
#9768=AXIS2_PLACEMENT_3D ( 'NONE', #41771, #36921, #44287 ) ;
#9769=VERTEX_POINT ( 'NONE', #34165 ) ;
#9771=VECTOR ( 'NONE', #21408, 1000.000000000000000 ) ;
#9775=EDGE_LOOP ( 'NONE', ( #29990, #10518, #27359, #23437 ) ) ;
#9777=AXIS2_PLACEMENT_3D ( 'NONE', #22512, #30573, #33750 ) ;
#9778=DIRECTION ( 'NONE',  ( 0.000000000000000000, 0.3826834323650904479, -0.9238795325112865164 ) ) ;
#9779=CARTESIAN_POINT ( 'NONE',  ( 11.99999999999999822, -73.44644590900077219, 24.73286445877677764 ) ) ;
#9781=ADVANCED_FACE ( 'NONE', ( #15346 ), #23387, .T. ) ;
#9782=DIRECTION ( 'NONE',  ( 0.000000000000000000, 0.8526401643540936215, -0.5224985647159469115 ) ) ;
#9783=EDGE_CURVE ( 'NONE', #42296, #30440, #286, .T. ) ;
#9792=DIRECTION ( 'NONE',  ( -1.000000000000000000, -0.000000000000000000, 0.000000000000000000 ) ) ;
#9797=DIRECTION ( 'NONE',  ( -1.000000000000000000, 0.000000000000000000, 0.000000000000000000 ) ) ;
#9799=CARTESIAN_POINT ( 'NONE',  ( 0.000000000000000000, -15.33399622253424432, -80.55351364060604169 ) ) ;
#9802=DIRECTION ( 'NONE',  ( -1.000000000000000000, 0.000000000000000000, -0.000000000000000000 ) ) ;
#9809=AXIS2_PLACEMENT_3D ( 'NONE', #27551, #30999, #8459 ) ;
#9810=DIRECTION ( 'NONE',  ( 1.000000000000000000, 0.000000000000000000, 0.000000000000000000 ) ) ;
#9813=ORIENTED_EDGE ( 'NONE', *, *, #40077, .T. ) ;
#9814=ORIENTED_EDGE ( 'NONE', *, *, #26306, .F. ) ;
#9815=DIRECTION ( 'NONE',  ( -1.000000000000000000, -0.000000000000000000, -0.000000000000000000 ) ) ;
#9816=CARTESIAN_POINT ( 'NONE',  ( 15.00000000000000000, -4.261787119644963262, 26.19803753235780164 ) ) ;
#9817=VECTOR ( 'NONE', #942, 1000.000000000000000 ) ;
#9824=CARTESIAN_POINT ( 'NONE',  ( 0.000000000000000000, 0.000000000000000000, 0.000000000000000000 ) ) ;
#9825=EDGE_CURVE ( 'NONE', #18873, #31959, #45636, .T. ) ;
#9832=ORIENTED_EDGE ( 'NONE', *, *, #19323, .F. ) ;
#9835=CIRCLE ( 'NONE', #24695, 31.99999999999999645 ) ;
#9836=EDGE_LOOP ( 'NONE', ( #16168, #42856, #21238, #44365 ) ) ;
#9849=ORIENTED_EDGE ( 'NONE', *, *, #39282, .F. ) ;
#9850=EDGE_CURVE ( 'NONE', #43802, #45904, #4327, .T. ) ;
#9851=LINE ( 'NONE', #36275, #42665 ) ;
#9854=DIRECTION ( 'NONE',  ( -1.000000000000000000, 0.000000000000000000, 0.000000000000000000 ) ) ;
#9855=DIRECTION ( 'NONE',  ( 0.000000000000000000, 0.000000000000000000, 1.000000000000000000 ) ) ;
#9859=DIRECTION ( 'NONE',  ( 1.000000000000000000, -0.000000000000000000, -0.000000000000000000 ) ) ;
#9860=DIRECTION ( 'NONE',  ( 0.000000000000000000, 0.2079116908177545131, -0.9781476007338066880 ) ) ;
#9863=CIRCLE ( 'NONE', #32532, 82.00000000000000000 ) ;
#9868=LINE ( 'NONE', #7154, #46687 ) ;
#9871=DIRECTION ( 'NONE',  ( 0.000000000000000000, -0.8526401643540970632, 0.5224985647159409163 ) ) ;
#9873=VERTEX_POINT ( 'NONE', #26101 ) ;
#9877=ORIENTED_EDGE ( 'NONE', *, *, #24528, .T. ) ;
#9882=CIRCLE ( 'NONE', #38731, 82.00000000000000000 ) ;
#9883=DIRECTION ( 'NONE',  ( -1.000000000000000000, -0.000000000000000000, 0.000000000000000000 ) ) ;
#9891=EDGE_CURVE ( 'NONE', #3320, #33272, #28454, .T. ) ;
#9901=VERTEX_POINT ( 'NONE', #20201 ) ;
#9906=CARTESIAN_POINT ( 'NONE',  ( 11.99999999999999822, 46.54456581323888997, -59.03342792756214408 ) ) ;
#9917=PLANE ( 'NONE',  #39361 ) ;
#9919=DIRECTION ( 'NONE',  ( -1.000000000000000000, 0.000000000000000000, -0.000000000000000000 ) ) ;
#9922=EDGE_CURVE ( 'NONE', #12455, #39152, #46421, .T. ) ;
#9925=AXIS2_PLACEMENT_3D ( 'NONE', #13304, #20157, #16737 ) ;
#9934=DIRECTION ( 'NONE',  ( 0.000000000000000000, 0.3090169943749480619, -0.9510565162951533091 ) ) ;
#9938=ORIENTED_EDGE ( 'NONE', *, *, #12131, .T. ) ;
#9940=ORIENTED_EDGE ( 'NONE', *, *, #41952, .F. ) ;
#9941=AXIS2_PLACEMENT_3D ( 'NONE', #34345, #23111, #41474 ) ;
#9942=ORIENTED_EDGE ( 'NONE', *, *, #5124, .F. ) ;
#9946=CIRCLE ( 'NONE', #1327, 31.99999999999998579 ) ;
#9953=CARTESIAN_POINT ( 'NONE',  ( 11.99999999999999822, -31.47745569255189224, 68.26794271651249346 ) ) ;
#9955=ORIENTED_EDGE ( 'NONE', *, *, #22162, .F. ) ;
#9957=EDGE_LOOP ( 'NONE', ( #42113, #25397, #30331, #35293 ) ) ;
#9959=LINE ( 'NONE', #24882, #22712 ) ;
#9962=ORIENTED_EDGE ( 'NONE', *, *, #15724, .T. ) ;
#9964=CYLINDRICAL_SURFACE ( 'NONE', #24726, 31.99999999999998579 ) ;
#9966=CARTESIAN_POINT ( 'NONE',  ( 11.99999999999999822, 73.73191006444551476, 14.66109333815590254 ) ) ;
#9969=FACE_OUTER_BOUND ( 'NONE', #10053, .T. ) ;
#9971=LINE ( 'NONE', #3096, #16490 ) ;
#9973=ORIENTED_EDGE ( 'NONE', *, *, #16917, .T. ) ;
#9975=ORIENTED_EDGE ( 'NONE', *, *, #5264, .T. ) ;
#9977=CARTESIAN_POINT ( 'NONE',  ( 0.000000000000000000, -58.39081064771786345, 50.95692526931308919 ) ) ;
#9983=CIRCLE ( 'NONE', #43598, 31.99999999999998579 ) ;
#9986=CYLINDRICAL_SURFACE ( 'NONE', #14513, 82.00000000000000000 ) ;
#9991=ORIENTED_EDGE ( 'NONE', *, *, #14084, .T. ) ;
#9997=CARTESIAN_POINT ( 'NONE',  ( 12.00000000000000000, -10.45096189432344502, -21.10159698893425784 ) ) ;
#10000=ORIENTED_EDGE ( 'NONE', *, *, #7642, .F. ) ;
#10001=AXIS2_PLACEMENT_3D ( 'NONE', #27678, #4909, #20811 ) ;
#10003=DIRECTION ( 'NONE',  ( -1.000000000000000000, 0.000000000000000000, 0.000000000000000000 ) ) ;
#10010=VECTOR ( 'NONE', #26091, 1000.000000000000000 ) ;
#10012=LINE ( 'NONE', #14412, #6343 ) ;
#10013=ORIENTED_EDGE ( 'NONE', *, *, #9010, .F. ) ;
#10014=CARTESIAN_POINT ( 'NONE',  ( 11.99999999999999822, 65.59268652807210742, 36.72794159290264560 ) ) ;
#10015=VERTEX_POINT ( 'NONE', #9419 ) ;
#10028=ORIENTED_EDGE ( 'NONE', *, *, #40899, .T. ) ;
#10030=LINE ( 'NONE', #1732, #19896 ) ;
#10032=ORIENTED_EDGE ( 'NONE', *, *, #43883, .T. ) ;
#10034=CYLINDRICAL_SURFACE ( 'NONE', #9452, 31.99999999999998579 ) ;
#10037=FACE_OUTER_BOUND ( 'NONE', #9957, .T. ) ;
#10042=AXIS2_PLACEMENT_3D ( 'NONE', #5420, #20330, #46545 ) ;
#10043=LINE ( 'NONE', #43812, #45560 ) ;
#10044=CIRCLE ( 'NONE', #2248, 77.49900000000000944 ) ;
#10050=DIRECTION ( 'NONE',  ( 0.000000000000000000, 0.000000000000000000, -1.000000000000000000 ) ) ;
#10051=ORIENTED_EDGE ( 'NONE', *, *, #23546, .F. ) ;
#10053=EDGE_LOOP ( 'NONE', ( #14398, #25603, #17903, #28488 ) ) ;
#10055=VERTEX_POINT ( 'NONE', #21881 ) ;
#10061=EDGE_CURVE ( 'NONE', #26795, #41290, #44672, .T. ) ;
#10069=PRODUCT_DEFINITION ( 'UNKNOWN', '', #14715, #26193 ) ;
#10076=AXIS2_PLACEMENT_3D ( 'NONE', #13642, #29044, #36624 ) ;
#10077=ORIENTED_EDGE ( 'NONE', *, *, #29253, .T. ) ;
#10078=AXIS2_PLACEMENT_3D ( 'NONE', #24831, #24598, #17948 ) ;
#10092=DIRECTION ( 'NONE',  ( 1.000000000000000000, 0.000000000000000000, 0.000000000000000000 ) ) ;
#10099=CARTESIAN_POINT ( 'NONE',  ( 11.99999999999999822, 74.18225833017937987, -34.94270380257559339 ) ) ;
#10104=DIRECTION ( 'NONE',  ( -1.000000000000000000, 0.000000000000000000, 0.000000000000000000 ) ) ;
#10107=DIRECTION ( 'NONE',  ( 0.000000000000000000, -0.3826834323650772363, -0.9238795325112919565 ) ) ;
#10108=ADVANCED_FACE ( 'NONE', ( #14305 ), #25788, .T. ) ;
#10110=DIRECTION ( 'NONE',  ( 0.000000000000000000, 0.000000000000000000, 1.000000000000000000 ) ) ;
#10115=LINE ( 'NONE', #33109, #13643 ) ;
#10116=AXIS2_PLACEMENT_3D ( 'NONE', #7951, #34148, #619 ) ;
#10119=CIRCLE ( 'NONE', #27316, 31.99999999999998579 ) ;
#10120=LINE ( 'NONE', #1816, #11984 ) ;
#10126=DIRECTION ( 'NONE',  ( 0.000000000000000000, 0.9876883405951371042, 0.1564344650402347547 ) ) ;
#10129=EDGE_CURVE ( 'NONE', #20327, #7093, #39891, .T. ) ;
#10131=FACE_OUTER_BOUND ( 'NONE', #16018, .T. ) ;
#10135=ORIENTED_EDGE ( 'NONE', *, *, #34739, .F. ) ;
#10142=LINE ( 'NONE', #47813, #23218 ) ;
#10147=CARTESIAN_POINT ( 'NONE',  ( 5.999999999999999112, 81.96053171279902472, -2.543863470248677316 ) ) ;
#10149=DIRECTION ( 'NONE',  ( 0.000000000000000000, -0.5877852522924624790, -0.8090169943749551118 ) ) ;
#10164=CARTESIAN_POINT ( 'NONE',  ( 11.99999999999999822, 41.19522573413733113, 65.64334221924924861 ) ) ;
#10169=DIRECTION ( 'NONE',  ( -1.000000000000000000, -0.000000000000000000, 0.000000000000000000 ) ) ;
#10181=FACE_OUTER_BOUND ( 'NONE', #25701, .T. ) ;
#10183=AXIS2_PLACEMENT_3D ( 'NONE', #38486, #2024, #43126 ) ;
#10190=ORIENTED_EDGE ( 'NONE', *, *, #4426, .T. ) ;
#10191=CARTESIAN_POINT ( 'NONE',  ( 11.99999999999999822, -66.50666863321974631, -39.78640506895675344 ) ) ;
#10192=EDGE_LOOP ( 'NONE', ( #12017, #22, #12678, #38471 ) ) ;
#10193=VERTEX_POINT ( 'NONE', #2799 ) ;
#10195=CARTESIAN_POINT ( 'NONE',  ( 0.000000000000000000, -36.72794159290197769, -65.59268652807249111 ) ) ;
#10200=DIRECTION ( 'NONE',  ( -1.000000000000000000, 0.000000000000000000, -0.000000000000000000 ) ) ;
#10205=CARTESIAN_POINT ( 'NONE',  ( 11.99999999999999822, 36.72794159290334903, -65.59268652807170952 ) ) ;
#10206=CARTESIAN_POINT ( 'NONE',  ( 15.00000000000000000, 23.49999999999999645, -1.500000000000003997 ) ) ;
#10207=AXIS2_PLACEMENT_3D ( 'NONE', #8174, #1559, #42427 ) ;
#10209=ORIENTED_EDGE ( 'NONE', *, *, #19533, .T. ) ;
#10210=VECTOR ( 'NONE', #39713, 1000.000000000000114 ) ;
#10223=DIRECTION ( 'NONE',  ( 0.000000000000000000, 0.9135454576426010886, -0.4067366430757998752 ) ) ;
#10227=LINE ( 'NONE', #25149, #43445 ) ;
#10228=EDGE_CURVE ( 'NONE', #46458, #36027, #14992, .T. ) ;
#10229=CARTESIAN_POINT ( 'NONE',  ( 11.99999999999999822, -77.16300072079681627, 27.74655509720640367 ) ) ;
#10243=ORIENTED_EDGE ( 'NONE', *, *, #48191, .T. ) ;
#10245=ADVANCED_FACE ( 'NONE', ( #23100 ), #30444, .T. ) ;
#10250=VERTEX_POINT ( 'NONE', #41957 ) ;
#10254=CARTESIAN_POINT ( 'NONE',  ( 0.000000000000000000, 0.000000000000000000, 0.000000000000000000 ) ) ;
#10255=DIRECTION ( 'NONE',  ( 1.000000000000000000, 0.000000000000000000, 0.000000000000000000 ) ) ;
#10256=ORIENTED_EDGE ( 'NONE', *, *, #13428, .F. ) ;
#10257=DIRECTION ( 'NONE',  ( -1.000000000000000000, 0.000000000000000000, 0.000000000000000000 ) ) ;
#10260=FACE_OUTER_BOUND ( 'NONE', #9292, .T. ) ;
#10262=ORIENTED_EDGE ( 'NONE', *, *, #15529, .T. ) ;
#10273=DIRECTION ( 'NONE',  ( -1.000000000000000000, 0.000000000000000000, -0.000000000000000000 ) ) ;
#10275=VECTOR ( 'NONE', #29758, 1000.000000000000000 ) ;
#10286=VECTOR ( 'NONE', #23889, 1000.000000000000000 ) ;
#10287=ORIENTED_EDGE ( 'NONE', *, *, #26993, .T. ) ;
#10300=FACE_OUTER_BOUND ( 'NONE', #70, .T. ) ;
#10304=LINE ( 'NONE', #25223, #40003 ) ;
#10307=ORIENTED_EDGE ( 'NONE', *, *, #9061, .T. ) ;
#10309=DIRECTION ( 'NONE',  ( 0.000000000000000000, 0.4067366430757989870, 0.9135454576426015327 ) ) ;
#10312=DIRECTION ( 'NONE',  ( -1.000000000000000000, -0.000000000000000000, -0.000000000000000000 ) ) ;
#10326=DIRECTION ( 'NONE',  ( -1.000000000000000000, 0.000000000000000000, -0.000000000000000000 ) ) ;
#10327=ORIENTED_EDGE ( 'NONE', *, *, #42211, .T. ) ;
#10329=CARTESIAN_POINT ( 'NONE',  ( 0.000000000000000000, -14.67089635893658794, -73.72996012237454977 ) ) ;
#10333=PLANE ( 'NONE',  #48165 ) ;
#10334=ORIENTED_EDGE ( 'NONE', *, *, #26979, .F. ) ;
#10342=EDGE_CURVE ( 'NONE', #45628, #1817, #48313, .T. ) ;
#10343=DIRECTION ( 'NONE',  ( 0.000000000000000000, 0.000000000000000000, 1.000000000000000000 ) ) ;
#10351=DIRECTION ( 'NONE',  ( 0.000000000000000000, -0.5000000000000028866, -0.8660254037844369313 ) ) ;
#10352=ORIENTED_EDGE ( 'NONE', *, *, #40618, .T. ) ;
#10353=DIRECTION ( 'NONE',  ( -1.000000000000000000, 0.000000000000000000, 0.000000000000000000 ) ) ;
#10356=DIRECTION ( 'NONE',  ( -1.000000000000000000, -0.000000000000000000, -0.000000000000000000 ) ) ;
#10358=ORIENTED_EDGE ( 'NONE', *, *, #27721, .T. ) ;
#10359=VECTOR ( 'NONE', #25313, 1000.000000000000000 ) ;
#10362=ORIENTED_EDGE ( 'NONE', *, *, #31922, .T. ) ;
#10363=ADVANCED_FACE ( 'NONE', ( #15034 ), #29954, .T. ) ;
#10368=DIRECTION ( 'NONE',  ( 0.000000000000000000, 0.000000000000000000, 1.000000000000000000 ) ) ;
#10369=AXIS2_PLACEMENT_3D ( 'NONE', #48197, #32551, #37182 ) ;
#10373=VECTOR ( 'NONE', #15968, 1000.000000000000000 ) ;
#10374=EDGE_CURVE ( 'NONE', #30611, #1277, #40646, .T. ) ;
#10379=VECTOR ( 'NONE', #29375, 1000.000000000000000 ) ;
#10382=DIRECTION ( 'NONE',  ( 1.000000000000000000, -0.000000000000000000, 0.000000000000000000 ) ) ;
#10384=VERTEX_POINT ( 'NONE', #28213 ) ;
#10385=VECTOR ( 'NONE', #14668, 1000.000000000000000 ) ;
#10386=DIRECTION ( 'NONE',  ( -1.000000000000000000, 0.000000000000000000, -0.000000000000000000 ) ) ;
#10387=CARTESIAN_POINT ( 'NONE',  ( -10.00000000000000000, 0.000000000000000000, 0.000000000000000000 ) ) ;
#10388=AXIS2_PLACEMENT_3D ( 'NONE', #35426, #8753, #46213 ) ;
#10395=EDGE_CURVE ( 'NONE', #36977, #17963, #4708, .T. ) ;
#10398=DIRECTION ( 'NONE',  ( 0.000000000000000000, 0.4067366430757887730, -0.9135454576426059736 ) ) ;
#10401=ORIENTED_EDGE ( 'NONE', *, *, #31339, .T. ) ;
#10408=FACE_OUTER_BOUND ( 'NONE', #31470, .T. ) ;
#10422=VERTEX_POINT ( 'NONE', #20625 ) ;
#10424=AXIS2_PLACEMENT_3D ( 'NONE', #11090, #4710, #38743 ) ;
#10425=AXIS2_PLACEMENT_3D ( 'NONE', #1869, #35636, #24620 ) ;
#10429=CIRCLE ( 'NONE', #34631, 77.49900000000000944 ) ;
#10431=EDGE_CURVE ( 'NONE', #1684, #44007, #12811, .T. ) ;
#10435=ORIENTED_EDGE ( 'NONE', *, *, #38081, .F. ) ;
#10454=EDGE_CURVE ( 'NONE', #32354, #5700, #35566, .T. ) ;
#10457=DIRECTION ( 'NONE',  ( -1.000000000000000000, -0.000000000000000000, -0.000000000000000000 ) ) ;
#10470=EDGE_LOOP ( 'NONE', ( #27142, #8258, #34593, #10729 ) ) ;
#10471=AXIS2_PLACEMENT_3D ( 'NONE', #29137, #44077, #10555 ) ;
#10472=VECTOR ( 'NONE', #16741, 1000.000000000000000 ) ;
#10479=CIRCLE ( 'NONE', #22220, 82.00000000000000000 ) ;
#10481=ORIENTED_EDGE ( 'NONE', *, *, #8458, .F. ) ;
#10483=LINE ( 'NONE', #35943, #44122 ) ;
#10484=EDGE_LOOP ( 'NONE', ( #5312, #16880, #42672, #47593 ) ) ;
#10485=DIRECTION ( 'NONE',  ( -1.000000000000000000, -0.000000000000000000, -0.000000000000000000 ) ) ;
#10489=ORIENTED_EDGE ( 'NONE', *, *, #19347, .T. ) ;
#10494=ADVANCED_FACE ( 'NONE', ( #2046 ), #23825, .T. ) ;
#10495=EDGE_CURVE ( 'NONE', #39822, #2924, #38357, .T. ) ;
#10497=VECTOR ( 'NONE', #14926, 1000.000000000000000 ) ;
#10498=EDGE_CURVE ( 'NONE', #33807, #1013, #36769, .T. ) ;
#10506=DIRECTION ( 'NONE',  ( -1.000000000000000000, 0.000000000000000000, 0.000000000000000000 ) ) ;
#10512=DIRECTION ( 'NONE',  ( 0.000000000000000000, 0.7431448254773939111, 0.6691306063588584596 ) ) ;
#10517=CARTESIAN_POINT ( 'NONE',  ( 15.00000000000000000, -23.29833615347109088, -3.418703333116486665 ) ) ;
#10518=ORIENTED_EDGE ( 'NONE', *, *, #24319, .T. ) ;
#10522=CARTESIAN_POINT ( 'NONE',  ( -10.00000000000000000, 0.000000000000000000, 0.000000000000000000 ) ) ;
#10526=EDGE_CURVE ( 'NONE', #46424, #30381, #32141, .T. ) ;
#10537=ORIENTED_EDGE ( 'NONE', *, *, #31152, .T. ) ;
#10544=DIRECTION ( 'NONE',  ( 0.000000000000000000, 0.9945218953682740670, 0.1045284632676459352 ) ) ;
#10550=EDGE_CURVE ( 'NONE', #19364, #13412, #40207, .T. ) ;
#10551=ORIENTED_EDGE ( 'NONE', *, *, #31424, .F. ) ;
#10555=DIRECTION ( 'NONE',  ( 0.000000000000000000, 0.000000000000000000, 1.000000000000000000 ) ) ;
#10556=ORIENTED_EDGE ( 'NONE', *, *, #40243, .F. ) ;
#10565=ORIENTED_EDGE ( 'NONE', *, *, #15103, .T. ) ;
#10568=VERTEX_POINT ( 'NONE', #25244 ) ;
#10569=DIRECTION ( 'NONE',  ( -1.000000000000000000, 0.000000000000000000, -0.000000000000000000 ) ) ;
#10571=ORIENTED_EDGE ( 'NONE', *, *, #38834, .F. ) ;
#10577=AXIS2_PLACEMENT_3D ( 'NONE', #12608, #23861, #19680 ) ;
#10585=EDGE_LOOP ( 'NONE', ( #36497, #36781, #7710, #37356 ) ) ;
#10586=FACE_OUTER_BOUND ( 'NONE', #15395, .T. ) ;
#10587=CIRCLE ( 'NONE', #9768, 77.49899999999999523 ) ;
#10590=ORIENTED_EDGE ( 'NONE', *, *, #22772, .T. ) ;
#10592=CARTESIAN_POINT ( 'NONE',  ( 11.99999999999999822, 0.000000000000000000, 0.000000000000000000 ) ) ;
#10594=LINE ( 'NONE', #15233, #40746 ) ;
#10596=ORIENTED_EDGE ( 'NONE', *, *, #39300, .T. ) ;
#10601=CARTESIAN_POINT ( 'NONE',  ( 0.000000000000000000, -80.28980883073747066, -16.65972982745017461 ) ) ;
#10608=CIRCLE ( 'NONE', #46561, 31.99999999999999289 ) ;
#10613=CARTESIAN_POINT ( 'NONE',  ( 11.99999999999999822, 0.000000000000000000, 0.000000000000000000 ) ) ;
#10615=ADVANCED_FACE ( 'NONE', ( #28707 ), #18139, .T. ) ;
#10616=DIRECTION ( 'NONE',  ( 0.000000000000000000, 0.000000000000000000, 1.000000000000000000 ) ) ;
#10618=VERTEX_POINT ( 'NONE', #36279 ) ;
#10622=EDGE_CURVE ( 'NONE', #37774, #23927, #29748, .T. ) ;
#10623=DIRECTION ( 'NONE',  ( -1.000000000000000000, 0.000000000000000000, -0.000000000000000000 ) ) ;
#10626=DIRECTION ( 'NONE',  ( 1.000000000000000000, -0.000000000000000000, 0.000000000000000000 ) ) ;
#10630=AXIS2_PLACEMENT_3D ( 'NONE', #46731, #38404, #12235 ) ;
#10635=PLANE ( 'NONE',  #25457 ) ;
#10639=DIRECTION ( 'NONE',  ( -1.000000000000000000, 0.000000000000000000, -0.000000000000000000 ) ) ;
#10644=DIRECTION ( 'NONE',  ( -1.000000000000000000, -0.000000000000000000, -0.000000000000000000 ) ) ;
#10649=AXIS2_PLACEMENT_3D ( 'NONE', #23894, #1867, #28053 ) ;
#10654=CIRCLE ( 'NONE', #45842, 31.99999999999998934 ) ;
#10660=DIRECTION ( 'NONE',  ( -1.000000000000000000, -0.000000000000000000, -0.000000000000000000 ) ) ;
#10663=DIRECTION ( 'NONE',  ( -1.000000000000000000, -0.000000000000000000, 0.000000000000000000 ) ) ;
#10664=CLOSED_SHELL ( 'NONE', ( #3639, #16505, #7671, #37342, #47079, #28099, #13063, #35542, #40522, #1891, #38968, #8440, #14662, #10245, #24264, #8942, #44877, #930, #48411, #13644, #28031, #24379, #19276, #28682, #12239, #30004, #11855, #41631, #24698, #6909, #34096, #28182, #35766, #32687, #44140, #11711, #26201, #6150, #13362, #362, #4817, #17957, #39497, #46866, #22654, #25923, #18348, #5921, #14589, #13016, #1172, #18580, #36521, #16207, #16369, #13977, #39589, #8936, #14194, #20081, #34915, #373, #23477, #13212, #34351, #15852, #3017, #7533, #40566, #46763, #22936, #41581, #37287, #2692, #24900, #29310, #5421, #45470, #24779, #34559, #1434, #31459, #5625, #16046, #1566, #23857, #33933, #14806, #8604, #5190, #215, #15135, #18046, #35477, #2524, #46427, #28489, #4591, #42681, #34423, #47242, #43254, #17797, #23418, #26868, #10363, #21567, #13440, #42498, #15728, #13028, #1896, #39745, #6038, #14672, #2111, #16034, #8391, #19501, #36011, #43058, #4283, #47920, #6705, #16963, #19990, #13538, #33106, #34436, #20333, #32974, #20600, #29304, #5752, #21387, #39817, #35114, #19643, #12564, #14494, #39021, #42502, #10936, #7775, #21505, #18409, #18047, #25856, #8124, #39265, #26685, #223, #31641, #15419, #7481, #10108, #37980, #19716, #39683, #8282, #21442, #3650, #31401, #2568, #33425, #4813, #45443, #19431, #42738, #25762, #33641, #34246, #42384, #18060, #39844, #5417, #28163, #11656, #44929, #2550, #39024, #29341, #29667, #37513, #46194, #16921, #38373, #15591, #15488, #13776, #48030, #46773, #3295, #41772, #27533, #44517, #6090, #28586, #573, #30587, #24694, #5582, #37809, #44107, #17085, #45836, #13695, #42525, #34250, #26742, #33758, #32275, #44861, #15363, #12657, #11081, #35310, #29822, #15151, #28030, #6582, #47952, #345, #23504, #38204, #40591, #41404, #25129, #14561, #5741, #45318, #32571, #20024, #39332, #492, #11101, #13788, #46302, #17274, #43241, #3877, #2620, #37736, #37467, #745, #38191, #16634, #6637, #12949, #46811, #37801, #43760, #26801, #31474, #709, #9781, #6514, #20185, #32173, #29370, #46986, #4423, #27991, #40755, #31020, #5864, #46923, #867, #36841, #40693, #43848, #9722, #1222, #9068, #30839, #24811, #21895, #24057, #33740, #41724, #37691, #26675, #22876, #2269, #21872, #24490, #40619, #6263, #41910, #15383, #29035, #16562, #7843, #11129, #10494, #43475, #31398, #16622, #14268, #36941, #30111, #10615, #161, #5322, #33858, #33392, #32560, #32220, #44931, #43918, #7986, #13018, #32193, #11348, #14153, #42043, #5086, #28451, #611, #19649, #32856, #14545, #32587, #35340, #11156, #32095, #15580, #121, #44868, #28455, #1401, #20428, #19481, #39749, #36136, #47520, #24560, #37088, #11303, #16313, #26648, #36403, #18784, #40291, #46489, #25425, #43128, #39474, #25582, #4277, #34983, #14769, #4045, #12847, #39686, #31296, #41338, #4860, #2413, #15493, #23236, #33954, #12391, #34679, #445, #41612, #8596, #20261, #2716, #25635, #9733, #2071, #1388, #11095, #28334, #47359, #36662, #4485, #48347, #42684, #2698, #7759, #1683, #22702, #31570, #26110, #11991, #38259, #14114, #40609, #40082, #45574, #42834, #33484, #29876, #20002, #40007, #39859, #37083, #40022, #42568, #29840, #32652, #43107 ) ) ;
#10668=CIRCLE ( 'NONE', #42704, 31.99999999999998934 ) ;
#10671=DIRECTION ( 'NONE',  ( 0.000000000000000000, 0.000000000000000000, 1.000000000000000000 ) ) ;
#10672=ORIENTED_EDGE ( 'NONE', *, *, #32695, .T. ) ;
#10674=ORIENTED_EDGE ( 'NONE', *, *, #32760, .F. ) ;
#10675=DIRECTION ( 'NONE',  ( 0.000000000000000000, 0.9876883405951383255, -0.1564344650402277048 ) ) ;
#10679=EDGE_CURVE ( 'NONE', #26682, #28743, #3714, .T. ) ;
#10680=ORIENTED_EDGE ( 'NONE', *, *, #16686, .T. ) ;
#10681=CIRCLE ( 'NONE', #38044, 31.99999999999998579 ) ;
#10683=CARTESIAN_POINT ( 'NONE',  ( 11.99999999999999822, -33.71516098798685590, -74.74816331893465815 ) ) ;
#10684=CARTESIAN_POINT ( 'NONE',  ( 11.99999999999999822, 30.41916302227114599, 71.27951684758035356 ) ) ;
#10691=ORIENTED_EDGE ( 'NONE', *, *, #30296, .F. ) ;
#10698=ORIENTED_EDGE ( 'NONE', *, *, #47425, .T. ) ;
#10704=EDGE_LOOP ( 'NONE', ( #37108, #38646, #3770, #28414 ) ) ;
#10707=PLANE ( 'NONE',  #22519 ) ;
#10711=ORIENTED_EDGE ( 'NONE', *, *, #31372, .T. ) ;
#10712=DIRECTION ( 'NONE',  ( -1.000000000000000000, 0.000000000000000000, 0.000000000000000000 ) ) ;
#10716=CARTESIAN_POINT ( 'NONE',  ( 11.99999999999999822, 0.8261519478441983200, -77.49459641780885022 ) ) ;
#10718=VECTOR ( 'NONE', #14298, 1000.000000000000000 ) ;
#10725=DIRECTION ( 'NONE',  ( 0.000000000000000000, 0.8526401643540936215, -0.5224985647159469115 ) ) ;
#10729=ORIENTED_EDGE ( 'NONE', *, *, #27208, .T. ) ;
#10730=ORIENTED_EDGE ( 'NONE', *, *, #18885, .F. ) ;
#10731=ORIENTED_EDGE ( 'NONE', *, *, #721, .T. ) ;
#10733=EDGE_LOOP ( 'NONE', ( #11768, #31209, #15853, #3985 ) ) ;
#10736=ORIENTED_EDGE ( 'NONE', *, *, #27272, .T. ) ;
#10738=EDGE_CURVE ( 'NONE', #10741, #41750, #27464, .T. ) ;
#10739=CIRCLE ( 'NONE', #31863, 82.00000000000000000 ) ;
#10740=DIRECTION ( 'NONE',  ( 0.000000000000000000, 0.000000000000000000, 1.000000000000000000 ) ) ;
#10741=VERTEX_POINT ( 'NONE', #36991 ) ;
#10742=ORIENTED_EDGE ( 'NONE', *, *, #36190, .T. ) ;
#10747=DIRECTION ( 'NONE',  ( -1.000000000000000000, 0.000000000000000000, 0.000000000000000000 ) ) ;
#10749=DIRECTION ( 'NONE',  ( -1.000000000000000000, -0.000000000000000000, -0.000000000000000000 ) ) ;
#10753=ORIENTED_EDGE ( 'NONE', *, *, #29902, .F. ) ;
#10765=DIRECTION ( 'NONE',  ( -1.000000000000000000, -0.000000000000000000, 0.000000000000000000 ) ) ;
#10771=DIRECTION ( 'NONE',  ( 0.000000000000000000, 0.000000000000000000, 1.000000000000000000 ) ) ;
#10773=VERTEX_POINT ( 'NONE', #22562 ) ;
#10774=EDGE_CURVE ( 'NONE', #11405, #39311, #1672, .T. ) ;
#10776=LINE ( 'NONE', #25681, #10497 ) ;
#10779=EDGE_CURVE ( 'NONE', #46892, #23962, #18835, .T. ) ;
#10790=EDGE_CURVE ( 'NONE', #23962, #3340, #30557, .T. ) ;
#10792=VERTEX_POINT ( 'NONE', #9311 ) ;
#10795=ORIENTED_EDGE ( 'NONE', *, *, #19163, .F. ) ;
#10805=CYLINDRICAL_SURFACE ( 'NONE', #19933, 31.99999999999998579 ) ;
#10806=DIRECTION ( 'NONE',  ( -1.000000000000000000, -0.000000000000000000, -0.000000000000000000 ) ) ;
#10807=ORIENTED_EDGE ( 'NONE', *, *, #12401, .T. ) ;
#10809=DIRECTION ( 'NONE',  ( 0.000000000000000000, 0.9945218953682742891, 0.1045284632676436315 ) ) ;
#10817=ORIENTED_EDGE ( 'NONE', *, *, #4161, .F. ) ;
#10818=DIRECTION ( 'NONE',  ( 0.000000000000000000, 2.312964634635746211E-15, -1.000000000000000000 ) ) ;
#10821=DIRECTION ( 'NONE',  ( 0.000000000000000000, 0.000000000000000000, 1.000000000000000000 ) ) ;
#10824=CARTESIAN_POINT ( 'NONE',  ( 11.99999999999999822, 76.66974797899837313, 11.30684508768366747 ) ) ;
#10840=DIRECTION ( 'NONE',  ( -1.000000000000000000, 0.000000000000000000, 0.000000000000000000 ) ) ;
#10848=CARTESIAN_POINT ( 'NONE',  ( 15.00000000000000000, 22.07842321921492612, 8.187992925817123790 ) ) ;
#10853=CIRCLE ( 'NONE', #10076, 77.49899999999999523 ) ;
#10855=VECTOR ( 'NONE', #44472, 1000.000000000000000 ) ;
#10864=ORIENTED_EDGE ( 'NONE', *, *, #927, .F. ) ;
#10866=CARTESIAN_POINT ( 'NONE',  ( 11.99999999999999822, 74.65374052328648702, 8.840884882375350529 ) ) ;
#10868=EDGE_CURVE ( 'NONE', #6289, #11748, #42303, .T. ) ;
#10870=ORIENTED_EDGE ( 'NONE', *, *, #10495, .F. ) ;
#10877=CYLINDRICAL_SURFACE ( 'NONE', #5614, 31.99999999999997868 ) ;
#10879=CYLINDRICAL_SURFACE ( 'NONE', #23725, 31.99999999999998579 ) ;
#10883=CARTESIAN_POINT ( 'NONE',  ( 11.99999999999999822, 14.66109333815460225, 73.73191006444577056 ) ) ;
#10884=ORIENTED_EDGE ( 'NONE', *, *, #29284, .T. ) ;
#10886=DIRECTION ( 'NONE',  ( -0.000000000000000000, 0.9781476007338042455, -0.2079116908177663092 ) ) ;
#10890=VECTOR ( 'NONE', #42039, 1000.000000000000000 ) ;
#10893=EDGE_CURVE ( 'NONE', #13081, #11259, #38217, .T. ) ;
#10897=VECTOR ( 'NONE', #23088, 1000.000000000000000 ) ;
#10899=EDGE_CURVE ( 'NONE', #47426, #17270, #21186, .T. ) ;
#10900=CARTESIAN_POINT ( 'NONE',  ( 11.99999999999999822, 24.73286445877808148, -73.44644590900034586 ) ) ;
#10905=EDGE_LOOP ( 'NONE', ( #43125, #40318, #3281, #47524 ) ) ;
#10910=DIRECTION ( 'NONE',  ( 0.000000000000000000, 0.9510565162951503115, -0.3090169943749573878 ) ) ;
#10916=DIRECTION ( 'NONE',  ( -1.000000000000000000, -0.000000000000000000, -0.000000000000000000 ) ) ;
#10922=CARTESIAN_POINT ( 'NONE',  ( 11.99999999999999822, -59.46389618801929089, -49.70050353004953081 ) ) ;
#10923=FACE_OUTER_BOUND ( 'NONE', #22650, .T. ) ;
#10925=EDGE_LOOP ( 'NONE', ( #39136, #8983, #30712, #25678 ) ) ;
#10930=DIRECTION ( 'NONE',  ( -1.000000000000000000, -0.000000000000000000, 0.000000000000000000 ) ) ;
#10933=CARTESIAN_POINT ( 'NONE',  ( 15.00000000000000000, 23.49999999999999645, 1.499999999999995337 ) ) ;
#10934=CARTESIAN_POINT ( 'NONE',  ( 0.000000000000000000, 0.000000000000000000, 0.000000000000000000 ) ) ;
#10936=ADVANCED_FACE ( 'NONE', ( #32778 ), #10034, .T. ) ;
#10937=DIRECTION ( 'NONE',  ( -1.000000000000000000, 0.000000000000000000, 0.000000000000000000 ) ) ;
#10939=CARTESIAN_POINT ( 'NONE',  ( 12.00000000000000000, 9.615535125378768200, -24.73947219025917121 ) ) ;
#10940=DIRECTION ( 'NONE',  ( -0.000000000000000000, 0.8090169943749503378, 0.5877852522924690293 ) ) ;
#10941=ORIENTED_EDGE ( 'NONE', *, *, #37125, .F. ) ;
#10943=LINE ( 'NONE', #31015, #1929 ) ;
#10945=LINE ( 'NONE', #44477, #18238 ) ;
#10954=AXIS2_PLACEMENT_3D ( 'NONE', #20916, #13819, #44149 ) ;
#10960=CIRCLE ( 'NONE', #35203, 31.99999999999997868 ) ;
#10961=ORIENTED_EDGE ( 'NONE', *, *, #38970, .F. ) ;
#10963=AXIS2_PLACEMENT_3D ( 'NONE', #11376, #4976, #42177 ) ;
#10965=ORIENTED_EDGE ( 'NONE', *, *, #32758, .F. ) ;
#10966=EDGE_CURVE ( 'NONE', #19037, #11173, #33697, .T. ) ;
#10973=ORIENTED_EDGE ( 'NONE', *, *, #44033, .T. ) ;
#10979=DIRECTION ( 'NONE',  ( 0.000000000000000000, 0.000000000000000000, 1.000000000000000000 ) ) ;
#10990=ORIENTED_EDGE ( 'NONE', *, *, #30605, .F. ) ;
#10991=VECTOR ( 'NONE', #42914, 1000.000000000000000 ) ;
#10998=LINE ( 'NONE', #36688, #41861 ) ;
#10999=ORIENTED_EDGE ( 'NONE', *, *, #24101, .T. ) ;
#11000=CARTESIAN_POINT ( 'NONE',  ( 0.000000000000000000, 36.72794159290334903, -65.59268652807170952 ) ) ;
#11003=FACE_OUTER_BOUND ( 'NONE', #4371, .T. ) ;
#11004=DIRECTION ( 'NONE',  ( -1.000000000000000000, 0.000000000000000000, -0.000000000000000000 ) ) ;
#11019=CARTESIAN_POINT ( 'NONE',  ( 6.000000000000000000, -15.33399622253541317, 80.55351364060584274 ) ) ;
#11021=CIRCLE ( 'NONE', #11798, 31.99999999999998579 ) ;
#11023=ORIENTED_EDGE ( 'NONE', *, *, #15294, .F. ) ;
#11035=ORIENTED_EDGE ( 'NONE', *, *, #43551, .T. ) ;
#11036=ORIENTED_EDGE ( 'NONE', *, *, #32452, .T. ) ;
#11040=CARTESIAN_POINT ( 'NONE',  ( 11.99999999999999822, 65.59268652807263322, -36.72794159290169347 ) ) ;
#11044=CARTESIAN_POINT ( 'NONE',  ( 11.99999999999999822, 70.52718814184260054, 26.02418014898334420 ) ) ;
#11052=CARTESIAN_POINT ( 'NONE',  ( 0.000000000000000000, 15.33399622253483408, 80.55351364060595643 ) ) ;
#11062=CARTESIAN_POINT ( 'NONE',  ( 0.000000000000000000, 0.000000000000000000, 0.000000000000000000 ) ) ;
#11065=PLANE ( 'NONE',  #11816 ) ;
#11066=EDGE_CURVE ( 'NONE', #15059, #5004, #13376, .T. ) ;
#11076=CARTESIAN_POINT ( 'NONE',  ( 11.99999999999999822, 0.000000000000000000, 0.000000000000000000 ) ) ;
#11081=ADVANCED_FACE ( 'NONE', ( #25919 ), #7079, .T. ) ;
#11084=CARTESIAN_POINT ( 'NONE',  ( 6.000000000000000000, -2.543863470247820224, -81.96053171279903893 ) ) ;
#11086=CYLINDRICAL_SURFACE ( 'NONE', #12783, 31.99999999999998579 ) ;
#11089=AXIS2_PLACEMENT_3D ( 'NONE', #4316, #19876, #25835 ) ;
#11090=CARTESIAN_POINT ( 'NONE',  ( 15.00000000000000000, -10.45096189432314127, 21.10159698893440350 ) ) ;
#11095=ADVANCED_FACE ( 'NONE', ( #33274 ), #40614, .F. ) ;
#11097=CARTESIAN_POINT ( 'NONE',  ( 6.000000000000000000, -10.30890764327441289, 81.34940948281332851 ) ) ;
#11101=ADVANCED_FACE ( 'NONE', ( #47950 ), #7323, .T. ) ;
#11102=DIRECTION ( 'NONE',  ( -1.000000000000000000, 0.000000000000000000, 0.000000000000000000 ) ) ;
#11104=EDGE_CURVE ( 'NONE', #39227, #6663, #41117, .T. ) ;
#11113=ORIENTED_EDGE ( 'NONE', *, *, #19438, .F. ) ;
#11117=VECTOR ( 'NONE', #1439, 1000.000000000000000 ) ;
#11118=CARTESIAN_POINT ( 'NONE',  ( 11.99999999999999822, 14.66109333815564852, -73.73191006444555740 ) ) ;
#11119=DIRECTION ( 'NONE',  ( -1.000000000000000000, 0.000000000000000000, -0.000000000000000000 ) ) ;
#11129=ADVANCED_FACE ( 'NONE', ( #14917 ), #29836, .T. ) ;
#11130=LINE ( 'NONE', #7460, #25540 ) ;
#11132=CIRCLE ( 'NONE', #6448, 82.00000000000000000 ) ;
#11133=CYLINDRICAL_SURFACE ( 'NONE', #43169, 82.00000000000000000 ) ;
#11134=DIRECTION ( 'NONE',  ( 0.000000000000000000, 0.000000000000000000, 1.000000000000000000 ) ) ;
#11135=CIRCLE ( 'NONE', #40865, 31.99999999999998224 ) ;
#11140=CARTESIAN_POINT ( 'NONE',  ( 11.99999999999999822, 0.000000000000000000, 0.000000000000000000 ) ) ;
#11148=VERTEX_POINT ( 'NONE', #45991 ) ;
#11149=VERTEX_POINT ( 'NONE', #12457 ) ;
#11156=ADVANCED_FACE ( 'NONE', ( #9024 ), #42311, .T. ) ;
#11157=DIRECTION ( 'NONE',  ( -1.000000000000000000, -0.000000000000000000, 0.000000000000000000 ) ) ;
#11167=CYLINDRICAL_SURFACE ( 'NONE', #5567, 31.99999999999998579 ) ;
#11169=AXIS2_PLACEMENT_3D ( 'NONE', #45925, #38579, #35127 ) ;
#11172=FACE_OUTER_BOUND ( 'NONE', #33771, .T. ) ;
#11173=VERTEX_POINT ( 'NONE', #38658 ) ;
#11177=DIRECTION ( 'NONE',  ( -1.000000000000000000, 0.000000000000000000, -0.000000000000000000 ) ) ;
#11178=FACE_OUTER_BOUND ( 'NONE', #9416, .T. ) ;
#11182=LINE ( 'NONE', #44233, #29542 ) ;
#11189=DIRECTION ( 'NONE',  ( 0.000000000000000000, 0.3090169943749410675, 0.9510565162951556406 ) ) ;
#11194=FACE_OUTER_BOUND ( 'NONE', #31785, .T. ) ;
#11200=CIRCLE ( 'NONE', #32299, 77.49899999999999523 ) ;
#11201=DIRECTION ( 'NONE',  ( 0.000000000000000000, -0.8090169943749531134, 0.5877852522924653655 ) ) ;
#11202=CIRCLE ( 'NONE', #11978, 31.99999999999998579 ) ;
#11206=AXIS2_PLACEMENT_3D ( 'NONE', #32865, #29453, #10616 ) ;
#11210=DIRECTION ( 'NONE',  ( 0.000000000000000000, -0.6494480483301904306, 0.7604059656000251577 ) ) ;
#11216=ORIENTED_EDGE ( 'NONE', *, *, #32874, .T. ) ;
#11218=EDGE_CURVE ( 'NONE', #7093, #23167, #13038, .T. ) ;
#11222=ORIENTED_EDGE ( 'NONE', *, *, #44618, .T. ) ;
#11223=CARTESIAN_POINT ( 'NONE',  ( 11.99999999999999822, 0.000000000000000000, 0.000000000000000000 ) ) ;
#11226=ORIENTED_EDGE ( 'NONE', *, *, #8053, .T. ) ;
#11230=AXIS2_PLACEMENT_3D ( 'NONE', #25791, #16252, #27507 ) ;
#11231=VECTOR ( 'NONE', #21707, 999.9999999999998863 ) ;
#11234=CARTESIAN_POINT ( 'NONE',  ( 11.99999999999999822, -31.46837873495025306, 68.27212725128265447 ) ) ;
#11236=ORIENTED_EDGE ( 'NONE', *, *, #25890, .F. ) ;
#11240=AXIS2_PLACEMENT_3D ( 'NONE', #31646, #6162, #2022 ) ;
#11242=ORIENTED_EDGE ( 'NONE', *, *, #42333, .T. ) ;
#11244=AXIS2_PLACEMENT_3D ( 'NONE', #30160, #7863, #30629 ) ;
#11246=VERTEX_POINT ( 'NONE', #16602 ) ;
#11247=VECTOR ( 'NONE', #43595, 1000.000000000000000 ) ;
#11250=EDGE_CURVE ( 'NONE', #38548, #19364, #31554, .T. ) ;
#11251=DIRECTION ( 'NONE',  ( -1.000000000000000000, 0.000000000000000000, 0.000000000000000000 ) ) ;
#11253=CARTESIAN_POINT ( 'NONE',  ( 0.000000000000000000, -62.50329211542407393, -41.76937507738853839 ) ) ;
#11255=AXIS2_PLACEMENT_3D ( 'NONE', #16452, #31403, #32120 ) ;
#11256=FACE_OUTER_BOUND ( 'NONE', #33970, .T. ) ;
#11259=VERTEX_POINT ( 'NONE', #12950 ) ;
#11261=DIRECTION ( 'NONE',  ( 0.000000000000000000, 0.000000000000000000, 1.000000000000000000 ) ) ;
#11263=CIRCLE ( 'NONE', #38622, 77.49899999999999523 ) ;
#11264=ORIENTED_EDGE ( 'NONE', *, *, #44587, .F. ) ;
#11273=DIRECTION ( 'NONE',  ( 0.000000000000000000, 0.000000000000000000, -1.000000000000000000 ) ) ;
#11275=ORIENTED_EDGE ( 'NONE', *, *, #22756, .F. ) ;
#11276=CIRCLE ( 'NONE', #29227, 31.99999999999997868 ) ;
#11279=CARTESIAN_POINT ( 'NONE',  ( 6.000000000000000000, -74.18225833017864090, -34.94270380257717790 ) ) ;
#11286=CARTESIAN_POINT ( 'NONE',  ( 11.99999999999999822, -75.11764819372145041, 29.05362095685286050 ) ) ;
#11287=AXIS2_PLACEMENT_3D ( 'NONE', #43672, #41371, #14936 ) ;
#11289=EDGE_CURVE ( 'NONE', #41663, #21229, #30825, .T. ) ;
#11294=ORIENTED_EDGE ( 'NONE', *, *, #29765, .T. ) ;
#11295=AXIS2_PLACEMENT_3D ( 'NONE', #38401, #42314, #33809 ) ;
#11301=DIRECTION ( 'NONE',  ( 0.000000000000000000, 0.000000000000000000, 1.000000000000000000 ) ) ;
#11303=ADVANCED_FACE ( 'NONE', ( #15883 ), #45747, .F. ) ;
#11305=AXIS2_PLACEMENT_3D ( 'NONE', #20817, #38714, #43339 ) ;
#11307=ORIENTED_EDGE ( 'NONE', *, *, #39568, .T. ) ;
#11309=ORIENTED_EDGE ( 'NONE', *, *, #42116, .F. ) ;
#11310=ORIENTED_EDGE ( 'NONE', *, *, #23270, .F. ) ;
#11315=AXIS2_PLACEMENT_3D ( 'NONE', #36301, #17699, #47784 ) ;
#11316=LINE ( 'NONE', #18867, #37884 ) ;
#11321=DIRECTION ( 'NONE',  ( 0.000000000000000000, 0.000000000000000000, -1.000000000000000000 ) ) ;
#11322=LINE ( 'NONE', #18644, #20818 ) ;
#11323=CIRCLE ( 'NONE', #29265, 77.49900000000000944 ) ;
#11327=CARTESIAN_POINT ( 'NONE',  ( -10.00000000000000000, 0.000000000000000000, 0.000000000000000000 ) ) ;
#11328=CARTESIAN_POINT ( 'NONE',  ( 11.99999999999999822, 28.89263327155849126, -71.91182617369157981 ) ) ;
#11333=CARTESIAN_POINT ( 'NONE',  ( 0.000000000000000000, -65.64334221924937651, 41.19522573413711797 ) ) ;
#11335=AXIS2_PLACEMENT_3D ( 'NONE', #7507, #139, #396 ) ;
#11336=ORIENTED_EDGE ( 'NONE', *, *, #21555, .T. ) ;
#11337=EDGE_CURVE ( 'NONE', #14595, #28447, #43522, .T. ) ;
#11338=CARTESIAN_POINT ( 'NONE',  ( 12.00000000000000000, 0.000000000000000000, 0.000000000000000000 ) ) ;
#11340=FACE_OUTER_BOUND ( 'NONE', #10925, .T. ) ;
#11341=EDGE_CURVE ( 'NONE', #5777, #44023, #37236, .T. ) ;
#11345=ORIENTED_EDGE ( 'NONE', *, *, #21016, .F. ) ;
#11346=VECTOR ( 'NONE', #10886, 999.9999999999998863 ) ;
#11347=VECTOR ( 'NONE', #25071, 1000.000000000000000 ) ;
#11348=ADVANCED_FACE ( 'NONE', ( #32261 ), #33162, .T. ) ;
#11350=EDGE_LOOP ( 'NONE', ( #45531, #18002, #26411, #12846 ) ) ;
#11351=ORIENTED_EDGE ( 'NONE', *, *, #10738, .F. ) ;
#11365=CARTESIAN_POINT ( 'NONE',  ( 0.000000000000000000, 74.65374052328660071, -8.840884882374309583 ) ) ;
#11369=ORIENTED_EDGE ( 'NONE', *, *, #17993, .T. ) ;
#11371=ORIENTED_EDGE ( 'NONE', *, *, #43550, .F. ) ;
#11376=CARTESIAN_POINT ( 'NONE',  ( 11.99999999999999822, 0.000000000000000000, 0.000000000000000000 ) ) ;
#11378=ORIENTED_EDGE ( 'NONE', *, *, #7904, .F. ) ;
#11379=CARTESIAN_POINT ( 'NONE',  ( 11.99999999999999822, 41.76106447765580043, -62.50884508063379741 ) ) ;
#11384=CARTESIAN_POINT ( 'NONE',  ( 15.00000000000000000, 24.81905959214275370, 9.408202855044498492 ) ) ;
#11387=CARTESIAN_POINT ( 'NONE',  ( 0.000000000000000000, -76.69515212746036070, 29.01471420065536932 ) ) ;
#11391=VERTEX_POINT ( 'NONE', #9977 ) ;
#11398=EDGE_CURVE ( 'NONE', #15864, #27438, #24906, .T. ) ;
#11401=LINE ( 'NONE', #18226, #14280 ) ;
#11402=EDGE_CURVE ( 'NONE', #25709, #12123, #22402, .T. ) ;
#11405=VERTEX_POINT ( 'NONE', #24189 ) ;
#11407=ORIENTED_EDGE ( 'NONE', *, *, #15479, .F. ) ;
#11411=ORIENTED_EDGE ( 'NONE', *, *, #45700, .T. ) ;
#11413=CIRCLE ( 'NONE', #3563, 82.00000000000000000 ) ;
#11417=CYLINDRICAL_SURFACE ( 'NONE', #363, 77.49899999999999523 ) ;
#11418=EDGE_LOOP ( 'NONE', ( #13863, #14830, #37695, #21344 ) ) ;
#11423=CARTESIAN_POINT ( 'NONE',  ( 6.000000000000000000, 81.34940948281337114, 10.30890764327411446 ) ) ;
#11426=VECTOR ( 'NONE', #46263, 1000.000000000000000 ) ;
#11431=ORIENTED_EDGE ( 'NONE', *, *, #32056, .F. ) ;
#11432=DIRECTION ( 'NONE',  ( -1.000000000000000000, 0.000000000000000000, -0.000000000000000000 ) ) ;
#11433=VECTOR ( 'NONE', #29903, 1000.000000000000000 ) ;
#11438=DIRECTION ( 'NONE',  ( 0.000000000000000000, -0.1045284632676570791, -0.9945218953682730678 ) ) ;
#11443=ORIENTED_EDGE ( 'NONE', *, *, #6306, .T. ) ;
#11451=LINE ( 'NONE', #3600, #1696 ) ;
#11454=CARTESIAN_POINT ( 'NONE',  ( 11.99999999999999822, 31.47745569255237896, -68.26794271651228030 ) ) ;
#11461=DIRECTION ( 'NONE',  ( -1.000000000000000000, -0.000000000000000000, 0.000000000000000000 ) ) ;
#11466=ORIENTED_EDGE ( 'NONE', *, *, #41288, .T. ) ;
#11467=AXIS2_PLACEMENT_3D ( 'NONE', #36698, #40394, #25675 ) ;
#11469=DIRECTION ( 'NONE',  ( 0.000000000000000000, 1.000000000000000000, 1.301042606982602757E-15 ) ) ;
#11470=ORIENTED_EDGE ( 'NONE', *, *, #17227, .F. ) ;
#11472=CARTESIAN_POINT ( 'NONE',  ( 11.99999999999999822, 0.000000000000000000, 0.000000000000000000 ) ) ;
#11473=ORIENTED_EDGE ( 'NONE', *, *, #5124, .T. ) ;
#11483=DIRECTION ( 'NONE',  ( 0.000000000000000000, 0.000000000000000000, 1.000000000000000000 ) ) ;
#11484=DIRECTION ( 'NONE',  ( -1.000000000000000000, -0.000000000000000000, -0.000000000000000000 ) ) ;
#11488=CIRCLE ( 'NONE', #13826, 31.99999999999998579 ) ;
#11490=VECTOR ( 'NONE', #40546, 1000.000000000000114 ) ;
#11492=ORIENTED_EDGE ( 'NONE', *, *, #24273, .F. ) ;
#11494=ORIENTED_EDGE ( 'NONE', *, *, #32329, .T. ) ;
#11500=CARTESIAN_POINT ( 'NONE',  ( 11.99999999999999822, -50.95692526931287603, -58.39081064771804819 ) ) ;
#11502=CARTESIAN_POINT ( 'NONE',  ( 0.000000000000000000, -72.35432306680498016, 20.40083707022857951 ) ) ;
#11504=CARTESIAN_POINT ( 'NONE',  ( 15.00000000000000000, 23.59884966291538078, 12.14883922797231008 ) ) ;
#11512=ORIENTED_EDGE ( 'NONE', *, *, #13477, .F. ) ;
#11513=VECTOR ( 'NONE', #28774, 1000.000000000000114 ) ;
#11515=CYLINDRICAL_SURFACE ( 'NONE', #34650, 31.99999999999998579 ) ;
#11520=VERTEX_POINT ( 'NONE', #4284 ) ;
#11523=ORIENTED_EDGE ( 'NONE', *, *, #28596, .F. ) ;
#11528=CARTESIAN_POINT ( 'NONE',  ( 15.00000000000000000, 18.84667830672579569, -18.68964196561269375 ) ) ;
#11530=AXIS2_PLACEMENT_3D ( 'NONE', #7402, #30637, #25989 ) ;
#11531=VERTEX_POINT ( 'NONE', #11387 ) ;
#11535=CARTESIAN_POINT ( 'NONE',  ( -10.00000000000000000, 0.000000000000000000, 0.000000000000000000 ) ) ;
#11538=DIRECTION ( 'NONE',  ( 0.000000000000000000, 0.000000000000000000, 1.000000000000000000 ) ) ;
#11540=ORIENTED_EDGE ( 'NONE', *, *, #6528, .F. ) ;
#11541=AXIS2_PLACEMENT_3D ( 'NONE', #30702, #30962, #13735 ) ;
#11544=DIRECTION ( 'NONE',  ( 0.000000000000000000, -0.9510565162951536422, -0.3090169943749471182 ) ) ;
#11552=EDGE_CURVE ( 'NONE', #34978, #40483, #1334, .T. ) ;
#11555=CARTESIAN_POINT ( 'NONE',  ( 0.000000000000000000, 76.41127070299290835, -12.93880638057234123 ) ) ;
#11566=VECTOR ( 'NONE', #16206, 1000.000000000000000 ) ;
#11569=CARTESIAN_POINT ( 'NONE',  ( 11.99999999999999822, -26.01480285779885904, 70.53064760720306481 ) ) ;
#11574=ORIENTED_EDGE ( 'NONE', *, *, #33079, .F. ) ;
#11575=FACE_BOUND ( 'NONE', #9351, .T. ) ;
#11576=EDGE_LOOP ( 'NONE', ( #22966, #11643, #43417, #48003 ) ) ;
#11577=CARTESIAN_POINT ( 'NONE',  ( 15.00000000000000000, -0.9646360437375368635, -23.52805723605589705 ) ) ;
#11585=DIRECTION ( 'NONE',  ( -1.000000000000000000, 0.000000000000000000, -0.000000000000000000 ) ) ;
#11591=CYLINDRICAL_SURFACE ( 'NONE', #3470, 82.00000000000000000 ) ;
#11594=FACE_OUTER_BOUND ( 'NONE', #1928, .T. ) ;
#11608=EDGE_CURVE ( 'NONE', #4566, #42537, #48239, .T. ) ;
#11609=CYLINDRICAL_SURFACE ( 'NONE', #37757, 31.99999999999998579 ) ;
#11614=LINE ( 'NONE', #19654, #15295 ) ;
#11617=EDGE_CURVE ( 'NONE', #39337, #31941, #30266, .T. ) ;
#11618=CYLINDRICAL_SURFACE ( 'NONE', #15802, 31.99999999999998579 ) ;
#11622=CARTESIAN_POINT ( 'NONE',  ( 11.99999999999999822, 0.000000000000000000, 0.000000000000000000 ) ) ;
#11626=ORIENTED_EDGE ( 'NONE', *, *, #18107, .F. ) ;
#11627=VECTOR ( 'NONE', #32487, 1000.000000000000000 ) ;
#11632=EDGE_CURVE ( 'NONE', #23778, #45628, #6816, .T. ) ;
#11633=EDGE_LOOP ( 'NONE', ( #135, #44409, #24395, #14497 ) ) ;
#11636=AXIS2_PLACEMENT_3D ( 'NONE', #13959, #6619, #3667 ) ;
#11637=LINE ( 'NONE', #1093, #36311 ) ;
#11639=CYLINDRICAL_SURFACE ( 'NONE', #24584, 77.49899999999999523 ) ;
#11643=ORIENTED_EDGE ( 'NONE', *, *, #14094, .F. ) ;
#11644=ORIENTED_EDGE ( 'NONE', *, *, #34412, .T. ) ;
#11645=DIRECTION ( 'NONE',  ( -1.000000000000000000, -0.000000000000000000, -0.000000000000000000 ) ) ;
#11650=ORIENTED_EDGE ( 'NONE', *, *, #45402, .T. ) ;
#11652=CARTESIAN_POINT ( 'NONE',  ( 11.99999999999999822, 67.80270845531956070, -46.11716303203111522 ) ) ;
#11656=ADVANCED_FACE ( 'NONE', ( #46114 ), #35326, .T. ) ;
#11658=AXIS2_PLACEMENT_3D ( 'NONE', #650, #7752, #18753 ) ;
#11661=CYLINDRICAL_SURFACE ( 'NONE', #46243, 82.00000000000000000 ) ;
#11670=ORIENTED_EDGE ( 'NONE', *, *, #20889, .F. ) ;
#11681=ORIENTED_EDGE ( 'NONE', *, *, #5598, .T. ) ;
#11682=FACE_OUTER_BOUND ( 'NONE', #23874, .T. ) ;
#11685=DIRECTION ( 'NONE',  ( 0.000000000000000000, -0.2079116908177641998, -0.9781476007338046896 ) ) ;
#11688=CIRCLE ( 'NONE', #1523, 31.99999999999999289 ) ;
#11692=FACE_OUTER_BOUND ( 'NONE', #46123, .T. ) ;
#11694=EDGE_CURVE ( 'NONE', #31325, #2585, #24314, .T. ) ;
#11697=EDGE_LOOP ( 'NONE', ( #4468, #46750, #48230, #35173 ) ) ;
#11698=ORIENTED_EDGE ( 'NONE', *, *, #7990, .T. ) ;
#11705=ORIENTED_EDGE ( 'NONE', *, *, #35350, .F. ) ;
#11706=CARTESIAN_POINT ( 'NONE',  ( 15.00000000000000000, 22.07842321921480888, -8.187992925817425771 ) ) ;
#11710=DIRECTION ( 'NONE',  ( -1.000000000000000000, 0.000000000000000000, 0.000000000000000000 ) ) ;
#11711=ADVANCED_FACE ( 'NONE', ( #12824 ), #39501, .T. ) ;
#11714=VERTEX_POINT ( 'NONE', #19908 ) ;
#11719=AXIS2_PLACEMENT_3D ( 'NONE', #48118, #10916, #44446 ) ;
#11724=EDGE_CURVE ( 'NONE', #11880, #20505, #34929, .T. ) ;
#11730=CARTESIAN_POINT ( 'NONE',  ( 6.000000000000000000, -80.28980883073747066, -16.65972982745017461 ) ) ;
#11731=DIRECTION ( 'NONE',  ( -1.000000000000000000, 0.000000000000000000, 0.000000000000000000 ) ) ;
#11735=CIRCLE ( 'NONE', #32806, 31.99999999999998934 ) ;
#11736=DIRECTION ( 'NONE',  ( 0.000000000000000000, 0.4539904997395413089, 0.8910065241883705633 ) ) ;
#11737=CARTESIAN_POINT ( 'NONE',  ( 11.99999999999999822, -34.94270380257692921, 74.18225833017875459 ) ) ;
#11738=DIRECTION ( 'NONE',  ( -1.000000000000000000, 0.000000000000000000, -0.000000000000000000 ) ) ;
#11741=DIRECTION ( 'NONE',  ( -1.000000000000000000, -0.000000000000000000, 0.000000000000000000 ) ) ;
#11744=DIRECTION ( 'NONE',  ( 0.000000000000000000, 0.000000000000000000, 1.000000000000000000 ) ) ;
#11745=CARTESIAN_POINT ( 'NONE',  ( 11.99999999999999822, 28.89263327155746097, 71.91182617369197771 ) ) ;
#11748=VERTEX_POINT ( 'NONE', #25744 ) ;
#11756=ORIENTED_EDGE ( 'NONE', *, *, #5220, .F. ) ;
#11758=ORIENTED_EDGE ( 'NONE', *, *, #14094, .T. ) ;
#11759=ORIENTED_EDGE ( 'NONE', *, *, #24048, .F. ) ;
#11764=ORIENTED_EDGE ( 'NONE', *, *, #47009, .T. ) ;
#11768=ORIENTED_EDGE ( 'NONE', *, *, #6511, .T. ) ;
#11769=DIRECTION ( 'NONE',  ( -1.000000000000000000, 0.000000000000000000, 0.000000000000000000 ) ) ;
#11770=EDGE_CURVE ( 'NONE', #39596, #42540, #9868, .T. ) ;
#11773=ORIENTED_EDGE ( 'NONE', *, *, #8442, .T. ) ;
#11775=ORIENTED_EDGE ( 'NONE', *, *, #927, .T. ) ;
#11776=DIRECTION ( 'NONE',  ( 0.000000000000000000, 0.9238795325112851842, 0.3826834323650938341 ) ) ;
#11777=VERTEX_POINT ( 'NONE', #43412 ) ;
#11787=CARTESIAN_POINT ( 'NONE',  ( 11.99999999999999822, -46.53671651293907274, -59.03961581697448935 ) ) ;
#11789=CYLINDRICAL_SURFACE ( 'NONE', #32909, 82.00000000000000000 ) ;
#11790=DIRECTION ( 'NONE',  ( -1.000000000000000000, -0.000000000000000000, 0.000000000000000000 ) ) ;
#11792=ORIENTED_EDGE ( 'NONE', *, *, #26851, .T. ) ;
#11793=AXIS2_PLACEMENT_3D ( 'NONE', #21695, #44451, #17535 ) ;
#11797=CIRCLE ( 'NONE', #17261, 82.00000000000000000 ) ;
#11798=AXIS2_PLACEMENT_3D ( 'NONE', #18787, #18314, #25895 ) ;
#11807=FACE_OUTER_BOUND ( 'NONE', #13707, .T. ) ;
#11811=CARTESIAN_POINT ( 'NONE',  ( 15.00000000000000000, 26.49999999999999645, 1.499999999999995781 ) ) ;
#11816=AXIS2_PLACEMENT_3D ( 'NONE', #37492, #276, #44113 ) ;
#11818=ORIENTED_EDGE ( 'NONE', *, *, #29087, .F. ) ;
#11823=CIRCLE ( 'NONE', #18829, 31.99999999999998934 ) ;
#11824=ORIENTED_EDGE ( 'NONE', *, *, #48016, .F. ) ;
#11833=DIRECTION ( 'NONE',  ( 0.000000000000000000, 0.000000000000000000, 1.000000000000000000 ) ) ;
#11834=DIRECTION ( 'NONE',  ( -1.000000000000000000, -0.000000000000000000, 0.000000000000000000 ) ) ;
#11837=ORIENTED_EDGE ( 'NONE', *, *, #42954, .F. ) ;
#11843=DIRECTION ( 'NONE',  ( 0.000000000000000000, 0.000000000000000000, 1.000000000000000000 ) ) ;
#11844=DIRECTION ( 'NONE',  ( 0.000000000000000000, 0.000000000000000000, 1.000000000000000000 ) ) ;
#11846=DIRECTION ( 'NONE',  ( -1.000000000000000000, 0.000000000000000000, 0.000000000000000000 ) ) ;
#11847=CARTESIAN_POINT ( 'NONE',  ( 11.99999999999999822, -59.03342792756297541, 46.54456581323783126 ) ) ;
#11851=CARTESIAN_POINT ( 'NONE',  ( 0.000000000000000000, -70.53064760720297954, -26.01480285779911839 ) ) ;
#11855=ADVANCED_FACE ( 'NONE', ( #36 ), #14993, .T. ) ;
#11856=DIRECTION ( 'NONE',  ( 0.000000000000000000, 0.1564344650402312020, -0.9876883405951376593 ) ) ;
#11858=DIRECTION ( 'NONE',  ( -1.000000000000000000, 0.000000000000000000, 0.000000000000000000 ) ) ;
#11859=VECTOR ( 'NONE', #45685, 1000.000000000000000 ) ;
#11860=DIRECTION ( 'NONE',  ( 0.000000000000000000, 0.000000000000000000, 1.000000000000000000 ) ) ;
#11866=AXIS2_PLACEMENT_3D ( 'NONE', #36810, #3274, #10149 ) ;
#11873=EDGE_CURVE ( 'NONE', #42556, #28383, #4512, .T. ) ;
#11874=ORIENTED_EDGE ( 'NONE', *, *, #45631, .T. ) ;
#11875=ORIENTED_EDGE ( 'NONE', *, *, #20289, .T. ) ;
#11880=VERTEX_POINT ( 'NONE', #14749 ) ;
#11884=DIRECTION ( 'NONE',  ( 0.000000000000000000, -0.7071067811865389130, -0.7071067811865562325 ) ) ;
#11887=EDGE_CURVE ( 'NONE', #48421, #41493, #23051, .T. ) ;
#11890=DIRECTION ( 'NONE',  ( -1.000000000000000000, -0.000000000000000000, 0.000000000000000000 ) ) ;
#11895=DIRECTION ( 'NONE',  ( -1.000000000000000000, 0.000000000000000000, 0.000000000000000000 ) ) ;
#11896=ORIENTED_EDGE ( 'NONE', *, *, #44815, .F. ) ;
#11898=CARTESIAN_POINT ( 'NONE',  ( 11.99999999999999822, 26.01480285779837232, 70.53064760720326376 ) ) ;
#11900=CARTESIAN_POINT ( 'NONE',  ( 0.000000000000000000, 18.89407956138362010, -75.16055320797013906 ) ) ;
#11904=AXIS2_PLACEMENT_3D ( 'NONE', #31245, #17017, #32442 ) ;
#11906=FACE_OUTER_BOUND ( 'NONE', #40837, .T. ) ;
#11912=ORIENTED_EDGE ( 'NONE', *, *, #21857, .F. ) ;
#11914=AXIS2_PLACEMENT_3D ( 'NONE', #29010, #7706, #22631 ) ;
#11917=LINE ( 'NONE', #1622, #47933 ) ;
#11918=AXIS2_PLACEMENT_3D ( 'NONE', #46230, #43284, #39625 ) ;
#11919=CARTESIAN_POINT ( 'NONE',  ( 0.000000000000000000, 65.59268652807263322, -36.72794159290169347 ) ) ;
#11929=EDGE_CURVE ( 'NONE', #20488, #14224, #39671, .T. ) ;
#11930=AXIS2_PLACEMENT_3D ( 'NONE', #31689, #27037, #16740 ) ;
#11935=ORIENTED_EDGE ( 'NONE', *, *, #36564, .T. ) ;
#11938=VERTEX_POINT ( 'NONE', #4462 ) ;
#11943=VECTOR ( 'NONE', #14086, 1000.000000000000000 ) ;
#11947=EDGE_CURVE ( 'NONE', #40215, #10055, #38119, .T. ) ;
#11952=ORIENTED_EDGE ( 'NONE', *, *, #21753, .F. ) ;
#11954=EDGE_CURVE ( 'NONE', #40825, #32445, #6842, .T. ) ;
#11958=LINE ( 'NONE', #26890, #27587 ) ;
#11962=ORIENTED_EDGE ( 'NONE', *, *, #17729, .F. ) ;
#11971=CARTESIAN_POINT ( 'NONE',  ( 0.000000000000000000, -67.80270845531921964, 46.11716303203162681 ) ) ;
#11978=AXIS2_PLACEMENT_3D ( 'NONE', #1198, #38400, #23704 ) ;
#11979=DIRECTION ( 'NONE',  ( 0.000000000000000000, -0.8660254037844432595, -0.4999999999999919509 ) ) ;
#11980=AXIS2_PLACEMENT_3D ( 'NONE', #20883, #28217, #13294 ) ;
#11983=ORIENTED_EDGE ( 'NONE', *, *, #15154, .F. ) ;
#11984=VECTOR ( 'NONE', #38792, 1000.000000000000000 ) ;
#11988=VERTEX_POINT ( 'NONE', #12047 ) ;
#11991=ADVANCED_FACE ( 'NONE', ( #540 ), #15471, .F. ) ;
#11992=DIRECTION ( 'NONE',  ( -1.000000000000000000, -0.000000000000000000, -0.000000000000000000 ) ) ;
#11993=AXIS2_PLACEMENT_3D ( 'NONE', #33525, #14698, #30356 ) ;
#11997=EDGE_CURVE ( 'NONE', #5001, #4198, #24041, .T. ) ;
#11998=CIRCLE ( 'NONE', #47921, 82.00000000000000000 ) ;
#11999=EDGE_CURVE ( 'NONE', #48421, #29406, #35023, .T. ) ;
#12000=ORIENTED_EDGE ( 'NONE', *, *, #2640, .F. ) ;
#12002=CARTESIAN_POINT ( 'NONE',  ( 0.000000000000000000, 72.35160999960817207, 20.41045688087850607 ) ) ;
#12003=VECTOR ( 'NONE', #43923, 1000.000000000000000 ) ;
#12004=CIRCLE ( 'NONE', #18233, 82.00000000000000000 ) ;
#12009=EDGE_LOOP ( 'NONE', ( #6571, #12741, #27802, #25695 ) ) ;
#12014=VERTEX_POINT ( 'NONE', #20325 ) ;
#12017=ORIENTED_EDGE ( 'NONE', *, *, #13926, .F. ) ;
#12023=DIRECTION ( 'NONE',  ( 0.000000000000000000, 0.8090169943749445647, 0.5877852522924770229 ) ) ;
#12032=ORIENTED_EDGE ( 'NONE', *, *, #36373, .T. ) ;
#12035=VERTEX_POINT ( 'NONE', #19842 ) ;
#12037=DIRECTION ( 'NONE',  ( 0.000000000000000000, 0.9135454576426055295, 0.4067366430757899387 ) ) ;
#12039=CARTESIAN_POINT ( 'NONE',  ( 11.99999999999999822, -75.11725578898470701, 2.956366410620372864 ) ) ;
#12044=EDGE_CURVE ( 'NONE', #24231, #38560, #12292, .T. ) ;
#12047=CARTESIAN_POINT ( 'NONE',  ( 11.99999999999999822, -44.88180994100329713, -63.18004540533077318 ) ) ;
#12048=DIRECTION ( 'NONE',  ( 0.000000000000000000, 0.000000000000000000, 1.000000000000000000 ) ) ;
#12051=CIRCLE ( 'NONE', #39393, 82.00000000000000000 ) ;
#12052=VECTOR ( 'NONE', #13858, 1000.000000000000000 ) ;
#12056=CARTESIAN_POINT ( 'NONE',  ( 11.99999999999999822, -81.34940948281344220, 10.30890764327355491 ) ) ;
#12061=FACE_BOUND ( 'NONE', #4445, .T. ) ;
#12064=AXIS2_PLACEMENT_3D ( 'NONE', #36927, #33993, #47951 ) ;
#12066=LINE ( 'NONE', #1016, #40880 ) ;
#12081=DIRECTION ( 'NONE',  ( 0.000000000000000000, -0.8526401643540970632, 0.5224985647159410274 ) ) ;
#12085=CIRCLE ( 'NONE', #39440, 31.99999999999998579 ) ;
#12101=LINE ( 'NONE', #30216, #42260 ) ;
#12106=DIRECTION ( 'NONE',  ( -1.000000000000000000, -0.000000000000000000, -0.000000000000000000 ) ) ;
#12110=DIRECTION ( 'NONE',  ( 0.000000000000000000, 1.000000000000000000, 1.301042606982602757E-15 ) ) ;
#12116=DIRECTION ( 'NONE',  ( -1.000000000000000000, -0.000000000000000000, -0.000000000000000000 ) ) ;
#12123=VERTEX_POINT ( 'NONE', #24024 ) ;
#12131=EDGE_CURVE ( 'NONE', #10568, #28195, #6092, .T. ) ;
#12133=ORIENTED_EDGE ( 'NONE', *, *, #31085, .T. ) ;
#12135=ORIENTED_EDGE ( 'NONE', *, *, #1501, .F. ) ;
#12137=CARTESIAN_POINT ( 'NONE',  ( 11.99999999999999822, -56.15606465354916566, -59.75363087400133111 ) ) ;
#12142=LINE ( 'NONE', #4054, #7398 ) ;
#12146=AXIS2_PLACEMENT_3D ( 'NONE', #28402, #29372, #2448 ) ;
#12147=ORIENTED_EDGE ( 'NONE', *, *, #10129, .F. ) ;
#12150=CARTESIAN_POINT ( 'NONE',  ( 0.000000000000000000, 59.75363087400153006, -56.15606465354896670 ) ) ;
#12155=VERTEX_POINT ( 'NONE', #42032 ) ;
#12156=CIRCLE ( 'NONE', #1986, 77.49900000000000944 ) ;
#12157=DIRECTION ( 'NONE',  ( -1.000000000000000000, 0.000000000000000000, 0.000000000000000000 ) ) ;
#12159=DIRECTION ( 'NONE',  ( -1.000000000000000000, 0.000000000000000000, 0.000000000000000000 ) ) ;
#12164=DIRECTION ( 'NONE',  ( 0.000000000000000000, -0.7071067811865535679, 0.7071067811865414665 ) ) ;
#12166=CARTESIAN_POINT ( 'NONE',  ( 11.99999999999999822, -55.20638768913724448, -51.02545421589383068 ) ) ;
#12168=VECTOR ( 'NONE', #7899, 1000.000000000000000 ) ;
#12171=ORIENTED_EDGE ( 'NONE', *, *, #3424, .F. ) ;
#12172=CARTESIAN_POINT ( 'NONE',  ( 0.000000000000000000, 39.47590169984945163, -71.87247863392373404 ) ) ;
#12173=EDGE_CURVE ( 'NONE', #26066, #29937, #20119, .T. ) ;
#12183=VECTOR ( 'NONE', #32735, 1000.000000000000000 ) ;
#12190=LINE ( 'NONE', #38362, #10890 ) ;
#12193=ORIENTED_EDGE ( 'NONE', *, *, #38189, .F. ) ;
#12199=DIRECTION ( 'NONE',  ( 0.000000000000000000, -0.8090169943749531134, 0.5877852522924653655 ) ) ;
#12206=VERTEX_POINT ( 'NONE', #42257 ) ;
#12208=CARTESIAN_POINT ( 'NONE',  ( 12.00000000000000000, 14.60985201121729737, 18.46759930825687235 ) ) ;
#12211=AXIS2_PLACEMENT_3D ( 'NONE', #42631, #46059, #30894 ) ;
#12212=CARTESIAN_POINT ( 'NONE',  ( 11.99999999999999822, -46.54456581323847786, 59.03342792756247093 ) ) ;
#12213=LINE ( 'NONE', #31793, #25210 ) ;
#12214=AXIS2_PLACEMENT_3D ( 'NONE', #11622, #11858, #26549 ) ;
#12220=EDGE_CURVE ( 'NONE', #19509, #25968, #9983, .T. ) ;
#12221=ORIENTED_EDGE ( 'NONE', *, *, #2125, .F. ) ;
#12222=ORIENTED_EDGE ( 'NONE', *, *, #1264, .T. ) ;
#12225=EDGE_CURVE ( 'NONE', #30064, #46329, #7992, .T. ) ;
#12226=CYLINDRICAL_SURFACE ( 'NONE', #37105, 31.99999999999998579 ) ;
#12228=CARTESIAN_POINT ( 'NONE',  ( 11.99999999999999822, 81.96053171279901051, 2.543863470248673764 ) ) ;
#12229=DIRECTION ( 'NONE',  ( -1.000000000000000000, -0.000000000000000000, -0.000000000000000000 ) ) ;
#12234=CARTESIAN_POINT ( 'NONE',  ( 11.99999999999999822, 31.46837873495072913, -68.27212725128242710 ) ) ;
#12235=DIRECTION ( 'NONE',  ( 0.000000000000000000, 0.000000000000000000, 1.000000000000000000 ) ) ;
#12239=ADVANCED_FACE ( 'NONE', ( #30767 ), #5066, .T. ) ;
#12240=EDGE_CURVE ( 'NONE', #31605, #43990, #41543, .T. ) ;
#12244=FACE_OUTER_BOUND ( 'NONE', #43972, .T. ) ;
#12254=ORIENTED_EDGE ( 'NONE', *, *, #17632, .F. ) ;
#12257=CARTESIAN_POINT ( 'NONE',  ( 0.000000000000000000, 72.35432306680485226, -20.40083707022909110 ) ) ;
#12260=CARTESIAN_POINT ( 'NONE',  ( 15.00000000000000000, 9.615535125379096826, 24.73947219025905042 ) ) ;
#12265=CARTESIAN_POINT ( 'NONE',  ( 5.999999999999999112, -64.81221759200379040, 50.23322058963324110 ) ) ;
#12267=ORIENTED_EDGE ( 'NONE', *, *, #27987, .F. ) ;
#12269=VERTEX_POINT ( 'NONE', #30521 ) ;
#12272=ORIENTED_EDGE ( 'NONE', *, *, #825, .F. ) ;
#12275=ORIENTED_EDGE ( 'NONE', *, *, #20720, .F. ) ;
#12279=ORIENTED_EDGE ( 'NONE', *, *, #16790, .F. ) ;
#12283=CARTESIAN_POINT ( 'NONE',  ( 15.00000000000000000, -23.29833615347104470, 3.418703333116808629 ) ) ;
#12284=AXIS2_PLACEMENT_3D ( 'NONE', #41304, #37863, #8246 ) ;
#12292=LINE ( 'NONE', #16429, #20928 ) ;
#12295=ORIENTED_EDGE ( 'NONE', *, *, #11929, .T. ) ;
#12297=CARTESIAN_POINT ( 'NONE',  ( 11.99999999999999822, 0.000000000000000000, 0.000000000000000000 ) ) ;
#12302=CIRCLE ( 'NONE', #25580, 31.99999999999998224 ) ;
#12303=DIRECTION ( 'NONE',  ( 0.000000000000000000, 0.4067366430757887730, -0.9135454576426059736 ) ) ;
#12310=EDGE_CURVE ( 'NONE', #13430, #35720, #35873, .T. ) ;
#12312=CARTESIAN_POINT ( 'NONE',  ( 11.99999999999999822, -31.46837873495025306, 68.27212725128265447 ) ) ;
#12313=ORIENTED_EDGE ( 'NONE', *, *, #3741, .T. ) ;
#12317=DIRECTION ( 'NONE',  ( -1.000000000000000000, -0.000000000000000000, -0.000000000000000000 ) ) ;
#12318=ORIENTED_EDGE ( 'NONE', *, *, #7636, .F. ) ;
#12319=CARTESIAN_POINT ( 'NONE',  ( 11.99999999999999822, 0.000000000000000000, 0.000000000000000000 ) ) ;
#12320=ORIENTED_EDGE ( 'NONE', *, *, #15202, .F. ) ;
#12329=VERTEX_POINT ( 'NONE', #27833 ) ;
#12330=ORIENTED_EDGE ( 'NONE', *, *, #32508, .F. ) ;
#12334=EDGE_CURVE ( 'NONE', #20027, #22296, #29217, .T. ) ;
#12341=EDGE_CURVE ( 'NONE', #24133, #14824, #36113, .T. ) ;
#12346=CARTESIAN_POINT ( 'NONE',  ( 5.999999999999999112, -50.23322058963299241, -64.81221759200397514 ) ) ;
#12353=AXIS2_PLACEMENT_3D ( 'NONE', #13249, #28170, #24499 ) ;
#12356=ORIENTED_EDGE ( 'NONE', *, *, #25576, .T. ) ;
#12361=CIRCLE ( 'NONE', #1418, 77.49899999999999523 ) ;
#12364=CIRCLE ( 'NONE', #46747, 82.00000000000000000 ) ;
#12369=CARTESIAN_POINT ( 'NONE',  ( 12.00000000000000000, -23.29833615347109088, -3.418703333116486665 ) ) ;
#12370=ORIENTED_EDGE ( 'NONE', *, *, #44723, .F. ) ;
#12371=DIRECTION ( 'NONE',  ( 0.000000000000000000, 0.000000000000000000, -1.000000000000000000 ) ) ;
#12382=ORIENTED_EDGE ( 'NONE', *, *, #44235, .T. ) ;
#12385=EDGE_CURVE ( 'NONE', #2031, #12921, #23906, .T. ) ;
#12386=DIRECTION ( 'NONE',  ( 0.000000000000000000, 0.000000000000000000, 1.000000000000000000 ) ) ;
#12387=CARTESIAN_POINT ( 'NONE',  ( 0.000000000000000000, 0.000000000000000000, 0.000000000000000000 ) ) ;
#12390=CARTESIAN_POINT ( 'NONE',  ( 15.00000000000000000, 9.615535125378766423, -24.73947219025917121 ) ) ;
#12391=ADVANCED_FACE ( 'NONE', ( #47130 ), #20457, .F. ) ;
#12396=LINE ( 'NONE', #7978, #10286 ) ;
#12397=CARTESIAN_POINT ( 'NONE',  ( 11.99999999999999822, -5.256550761633395297, 77.32052557432841411 ) ) ;
#12398=ORIENTED_EDGE ( 'NONE', *, *, #41952, .T. ) ;
#12401=EDGE_CURVE ( 'NONE', #7113, #15986, #17511, .T. ) ;
#12404=VECTOR ( 'NONE', #24186, 1000.000000000000000 ) ;
#12413=ORIENTED_EDGE ( 'NONE', *, *, #9664, .T. ) ;
#12416=ORIENTED_EDGE ( 'NONE', *, *, #6973, .T. ) ;
#12420=ORIENTED_EDGE ( 'NONE', *, *, #9331, .F. ) ;
#12427=ORIENTED_EDGE ( 'NONE', *, *, #6973, .F. ) ;
#12430=EDGE_CURVE ( 'NONE', #3463, #21150, #21425, .T. ) ;
#12432=DIRECTION ( 'NONE',  ( -1.000000000000000000, 0.000000000000000000, -0.000000000000000000 ) ) ;
#12434=CARTESIAN_POINT ( 'NONE',  ( 11.99999999999999822, -81.50828551894234408, 8.966570791700414489 ) ) ;
#12438=ORIENTED_EDGE ( 'NONE', *, *, #34994, .F. ) ;
#12441=ORIENTED_EDGE ( 'NONE', *, *, #33647, .F. ) ;
#12449=ORIENTED_EDGE ( 'NONE', *, *, #24148, .F. ) ;
#12452=LINE ( 'NONE', #9018, #29786 ) ;
#12455=VERTEX_POINT ( 'NONE', #18480 ) ;
#12457=CARTESIAN_POINT ( 'NONE',  ( 11.99999999999999822, 41.19522573413733113, 65.64334221924924861 ) ) ;
#12460=DIRECTION ( 'NONE',  ( -1.000000000000000000, 0.000000000000000000, 0.000000000000000000 ) ) ;
#12466=AXIS2_PLACEMENT_3D ( 'NONE', #9281, #1960, #16879 ) ;
#12478=EDGE_CURVE ( 'NONE', #1469, #4110, #41006, .T. ) ;
#12483=EDGE_CURVE ( 'NONE', #6361, #36067, #26117, .T. ) ;
#12487=ORIENTED_EDGE ( 'NONE', *, *, #924, .T. ) ;
#12492=ORIENTED_EDGE ( 'NONE', *, *, #9825, .F. ) ;
#12493=DIRECTION ( 'NONE',  ( -1.000000000000000000, 0.000000000000000000, -0.000000000000000000 ) ) ;
#12497=CYLINDRICAL_SURFACE ( 'NONE', #35600, 82.00000000000000000 ) ;
#12502=LINE ( 'NONE', #12740, #5574 ) ;
#12504=ORIENTED_EDGE ( 'NONE', *, *, #9177, .T. ) ;
#12505=CARTESIAN_POINT ( 'NONE',  ( 0.000000000000000000, 28.89263327155746097, 71.91182617369197771 ) ) ;
#12510=CIRCLE ( 'NONE', #45332, 77.49899999999999523 ) ;
#12511=VERTEX_POINT ( 'NONE', #32678 ) ;
#12514=CARTESIAN_POINT ( 'NONE',  ( 15.00000000000000000, -1.278221433540507546, -26.51162292216071492 ) ) ;
#12516=DIRECTION ( 'NONE',  ( 0.000000000000000000, 0.000000000000000000, 1.000000000000000000 ) ) ;
#12518=DIRECTION ( 'NONE',  ( 0.000000000000000000, -0.2079116908177641998, -0.9781476007338046896 ) ) ;
#12524=DIRECTION ( 'NONE',  ( 0.000000000000000000, 0.3826834323650841752, 0.9238795325112891810 ) ) ;
#12538=DIRECTION ( 'NONE',  ( -1.000000000000000000, 0.000000000000000000, -0.000000000000000000 ) ) ;
#12546=EDGE_CURVE ( 'NONE', #37697, #34943, #29497, .T. ) ;
#12550=CARTESIAN_POINT ( 'NONE',  ( 12.00000000000000000, 23.49999999999999645, 1.499999999999995337 ) ) ;
#12551=ORIENTED_EDGE ( 'NONE', *, *, #21256, .T. ) ;
#12555=DIRECTION ( 'NONE',  ( 0.000000000000000000, 0.000000000000000000, 1.000000000000000000 ) ) ;
#12556=LINE ( 'NONE', #19879, #24747 ) ;
#12562=DIRECTION ( 'NONE',  ( -1.000000000000000000, 0.000000000000000000, 0.000000000000000000 ) ) ;
#12564=ADVANCED_FACE ( 'NONE', ( #40749 ), #7217, .T. ) ;
#12565=CARTESIAN_POINT ( 'NONE',  ( 15.00000000000000000, 16.83928648764922542, -16.46020748918050458 ) ) ;
#12570=CARTESIAN_POINT ( 'NONE',  ( 11.99999999999999822, -72.35160999960801576, -20.41045688087902121 ) ) ;
#12572=CARTESIAN_POINT ( 'NONE',  ( 0.000000000000000000, -39.47590169984795239, -71.87247863392457248 ) ) ;
#12573=CARTESIAN_POINT ( 'NONE',  ( 15.00000000000000000, -10.45096189432344502, -21.10159698893425784 ) ) ;
#12581=APPLICATION_CONTEXT ( 'automotive_design' ) ;
#12587=PLANE ( 'NONE',  #6616 ) ;
#12591=CARTESIAN_POINT ( 'NONE',  ( 0.000000000000000000, 0.000000000000000000, 0.000000000000000000 ) ) ;
#12595=AXIS2_PLACEMENT_3D ( 'NONE', #21526, #2666, #9782 ) ;
#12597=EDGE_CURVE ( 'NONE', #20955, #20223, #23119, .T. ) ;
#12598=ORIENTED_EDGE ( 'NONE', *, *, #21877, .F. ) ;
#12599=EDGE_CURVE ( 'NONE', #14436, #44520, #5009, .T. ) ;
#12604=DIRECTION ( 'NONE',  ( 0.000000000000000000, -0.6691306063588579045, 0.7431448254773945772 ) ) ;
#12608=CARTESIAN_POINT ( 'NONE',  ( 11.99999999999999822, 0.000000000000000000, 0.000000000000000000 ) ) ;
#12609=ORIENTED_EDGE ( 'NONE', *, *, #43049, .T. ) ;
#12611=EDGE_LOOP ( 'NONE', ( #579, #15198, #30675, #8568 ) ) ;
#12625=LINE ( 'NONE', #9191, #17220 ) ;
#12629=DIRECTION ( 'NONE',  ( 0.000000000000000000, 0.000000000000000000, 1.000000000000000000 ) ) ;
#12635=ORIENTED_EDGE ( 'NONE', *, *, #45344, .T. ) ;
#12637=AXIS2_PLACEMENT_3D ( 'NONE', #15556, #11890, #41999 ) ;
#12638=CARTESIAN_POINT ( 'NONE',  ( 11.99999999999999822, -31.46837873494930093, -68.27212725128309501 ) ) ;
#12639=VECTOR ( 'NONE', #34635, 1000.000000000000000 ) ;
#12644=AXIS2_PLACEMENT_3D ( 'NONE', #42018, #26833, #41528 ) ;
#12645=CYLINDRICAL_SURFACE ( 'NONE', #1340, 31.99999999999998579 ) ;
#12646=CARTESIAN_POINT ( 'NONE',  ( 0.000000000000000000, 0.000000000000000000, 77.49899999999999523 ) ) ;
#12649=ORIENTED_EDGE ( 'NONE', *, *, #21016, .T. ) ;
#12653=CARTESIAN_POINT ( 'NONE',  ( 5.999999999999999112, -74.74816331893453025, 33.71516098798714722 ) ) ;
#12654=ORIENTED_EDGE ( 'NONE', *, *, #9217, .F. ) ;
#12656=ORIENTED_EDGE ( 'NONE', *, *, #22478, .F. ) ;
#12657=ADVANCED_FACE ( 'NONE', ( #45889 ), #42196, .T. ) ;
#12659=CARTESIAN_POINT ( 'NONE',  ( 11.99999999999999822, -8.966570791701281351, 81.50828551894223040 ) ) ;
#12663=AXIS2_PLACEMENT_3D ( 'NONE', #42668, #15989, #42168 ) ;
#12665=DIRECTION ( 'NONE',  ( 0.000000000000000000, 0.9969173337331276308, 0.07845909572784874608 ) ) ;
#12667=DIRECTION ( 'NONE',  ( 1.000000000000000000, 0.000000000000000000, 0.000000000000000000 ) ) ;
#12669=EDGE_LOOP ( 'NONE', ( #3046, #46163, #15914, #47676 ) ) ;
#12671=AXIS2_PLACEMENT_3D ( 'NONE', #44174, #21887, #44652 ) ;
#12676=EDGE_LOOP ( 'NONE', ( #31853, #1657, #3797, #27230 ) ) ;
#12678=ORIENTED_EDGE ( 'NONE', *, *, #29902, .T. ) ;
#12680=CARTESIAN_POINT ( 'NONE',  ( 0.000000000000000000, 76.41127070299273782, 12.93880638057342836 ) ) ;
#12681=CARTESIAN_POINT ( 'NONE',  ( 0.000000000000000000, 0.000000000000000000, 0.000000000000000000 ) ) ;
#12682=VECTOR ( 'NONE', #10749, 1000.000000000000000 ) ;
#12684=DIRECTION ( 'NONE',  ( -1.000000000000000000, -0.000000000000000000, -0.000000000000000000 ) ) ;
#12686=DIRECTION ( 'NONE',  ( 0.000000000000000000, 0.000000000000000000, 1.000000000000000000 ) ) ;
#12687=ORIENTED_EDGE ( 'NONE', *, *, #3557, .F. ) ;
#12689=LINE ( 'NONE', #16360, #26653 ) ;
#12690=DIRECTION ( 'NONE',  ( 0.000000000000000000, 1.445602896647339410E-16, -1.000000000000000000 ) ) ;
#12691=EDGE_LOOP ( 'NONE', ( #35785, #27240, #37288, #24394 ) ) ;
#12692=DIRECTION ( 'NONE',  ( 1.000000000000000000, -0.000000000000000000, -0.000000000000000000 ) ) ;
#12693=ORIENTED_EDGE ( 'NONE', *, *, #9219, .T. ) ;
#12695=FACE_OUTER_BOUND ( 'NONE', #2974, .T. ) ;
#12696=CARTESIAN_POINT ( 'NONE',  ( 15.00000000000000000, 23.49999999999999645, 1.499999999999995337 ) ) ;
#12701=CYLINDRICAL_SURFACE ( 'NONE', #582, 82.00000000000000000 ) ;
#12705=ORIENTED_EDGE ( 'NONE', *, *, #11954, .T. ) ;
#12706=CIRCLE ( 'NONE', #7209, 31.99999999999998934 ) ;
#12716=EDGE_LOOP ( 'NONE', ( #6066, #17255, #14971, #10243 ) ) ;
#12718=ORIENTED_EDGE ( 'NONE', *, *, #28071, .T. ) ;
#12721=ORIENTED_EDGE ( 'NONE', *, *, #9922, .F. ) ;
#12722=EDGE_LOOP ( 'NONE', ( #30852, #34071, #11896, #40587 ) ) ;
#12725=CIRCLE ( 'NONE', #35391, 77.49899999999999523 ) ;
#12730=VERTEX_POINT ( 'NONE', #31694 ) ;
#12733=DIRECTION ( 'NONE',  ( 0.000000000000000000, 0.9723699203976756689, 0.2334453638559094157 ) ) ;
#12740=CARTESIAN_POINT ( 'NONE',  ( 11.99999999999999822, 24.73286445877705475, 73.44644590900068692 ) ) ;
#12741=ORIENTED_EDGE ( 'NONE', *, *, #41797, .F. ) ;
#12745=FACE_OUTER_BOUND ( 'NONE', #38537, .T. ) ;
#12748=DIRECTION ( 'NONE',  ( -1.000000000000000000, -0.000000000000000000, -0.000000000000000000 ) ) ;
#12752=CARTESIAN_POINT ( 'NONE',  ( 11.99999999999999822, 0.000000000000000000, 0.000000000000000000 ) ) ;
#12762=FACE_OUTER_BOUND ( 'NONE', #33239, .T. ) ;
#12763=DIRECTION ( 'NONE',  ( -1.000000000000000000, 0.000000000000000000, 0.000000000000000000 ) ) ;
#12765=CIRCLE ( 'NONE', #11993, 77.49899999999999523 ) ;
#12768=ORIENTED_EDGE ( 'NONE', *, *, #45344, .F. ) ;
#12770=ORIENTED_EDGE ( 'NONE', *, *, #41962, .T. ) ;
#12773=AXIS2_PLACEMENT_3D ( 'NONE', #4330, #11438, #401 ) ;
#12781=CIRCLE ( 'NONE', #6516, 77.49900000000000944 ) ;
#12783=AXIS2_PLACEMENT_3D ( 'NONE', #25272, #29926, #28956 ) ;
#12787=VECTOR ( 'NONE', #35834, 1000.000000000000000 ) ;
#12803=LINE ( 'NONE', #42671, #40481 ) ;
#12805=CIRCLE ( 'NONE', #40165, 82.00000000000000000 ) ;
#12811=LINE ( 'NONE', #4734, #10991 ) ;
#12813=VERTEX_POINT ( 'NONE', #5726 ) ;
#12816=DIRECTION ( 'NONE',  ( 0.000000000000000000, 0.000000000000000000, -1.000000000000000000 ) ) ;
#12818=DIRECTION ( 'NONE',  ( 0.000000000000000000, 0.000000000000000000, 1.000000000000000000 ) ) ;
#12822=CARTESIAN_POINT ( 'NONE',  ( 11.99999999999999822, 0.000000000000000000, 0.000000000000000000 ) ) ;
#12824=FACE_OUTER_BOUND ( 'NONE', #3938, .T. ) ;
#12831=CIRCLE ( 'NONE', #46436, 31.99999999999998579 ) ;
#12833=ORIENTED_EDGE ( 'NONE', *, *, #30510, .T. ) ;
#12836=CARTESIAN_POINT ( 'NONE',  ( 11.99999999999999822, -51.02545421589363883, 55.20638768913742922 ) ) ;
#12841=CIRCLE ( 'NONE', #44102, 31.99999999999998934 ) ;
#12843=CARTESIAN_POINT ( 'NONE',  ( 0.000000000000000000, 68.55367621811141987, 44.99326035066079044 ) ) ;
#12846=ORIENTED_EDGE ( 'NONE', *, *, #26268, .F. ) ;
#12847=ADVANCED_FACE ( 'NONE', ( #35584 ), #12587, .F. ) ;
#12849=AXIS2_PLACEMENT_3D ( 'NONE', #48213, #17862, #2690 ) ;
#12850=DIRECTION ( 'NONE',  ( 0.000000000000000000, 0.9238795325112851842, 0.3826834323650938341 ) ) ;
#12852=DIRECTION ( 'NONE',  ( 1.000000000000000000, 0.000000000000000000, 0.000000000000000000 ) ) ;
#12857=VERTEX_POINT ( 'NONE', #16744 ) ;
#12861=DIRECTION ( 'NONE',  ( -1.000000000000000000, 0.000000000000000000, 0.000000000000000000 ) ) ;
#12864=ORIENTED_EDGE ( 'NONE', *, *, #17949, .T. ) ;
#12868=DIRECTION ( 'NONE',  ( 0.000000000000000000, -0.9876883405951359940, -0.1564344650402420822 ) ) ;
#12870=CARTESIAN_POINT ( 'NONE',  ( 11.99999999999999822, 0.000000000000000000, 0.000000000000000000 ) ) ;
#12872=DIRECTION ( 'NONE',  ( 0.000000000000000000, 0.4067366430757989870, 0.9135454576426015327 ) ) ;
#12880=DIRECTION ( 'NONE',  ( -1.000000000000000000, 0.000000000000000000, 0.000000000000000000 ) ) ;
#12887=CARTESIAN_POINT ( 'NONE',  ( 6.000000000000000000, -29.01471420065506379, -76.69515212746047439 ) ) ;
#12891=FACE_OUTER_BOUND ( 'NONE', #29204, .T. ) ;
#12896=ORIENTED_EDGE ( 'NONE', *, *, #46418, .F. ) ;
#12904=CIRCLE ( 'NONE', #26164, 31.99999999999999289 ) ;
#12907=ORIENTED_EDGE ( 'NONE', *, *, #5937, .T. ) ;
#12908=EDGE_CURVE ( 'NONE', #31098, #16116, #6927, .T. ) ;
#12912=EDGE_CURVE ( 'NONE', #22184, #41493, #6693, .T. ) ;
#12916=DIRECTION ( 'NONE',  ( -1.000000000000000000, 0.000000000000000000, 0.000000000000000000 ) ) ;
#12918=ORIENTED_EDGE ( 'NONE', *, *, #14929, .F. ) ;
#12919=DIRECTION ( 'NONE',  ( -1.000000000000000000, -0.000000000000000000, 0.000000000000000000 ) ) ;
#12920=CARTESIAN_POINT ( 'NONE',  ( 0.000000000000000000, -17.28742895386031719, -75.54627589209962935 ) ) ;
#12921=VERTEX_POINT ( 'NONE', #7414 ) ;
#12936=CARTESIAN_POINT ( 'NONE',  ( 11.99999999999999822, -55.19960302592104284, 51.03279382321070301 ) ) ;
#12937=AXIS2_PLACEMENT_3D ( 'NONE', #22847, #40730, #3271 ) ;
#12940=EDGE_LOOP ( 'NONE', ( #9152, #36255, #25407, #46641 ) ) ;
#12942=CARTESIAN_POINT ( 'NONE',  ( 0.000000000000000000, -15.33399622253541317, 80.55351364060584274 ) ) ;
#12945=EDGE_CURVE ( 'NONE', #15777, #25011, #10115, .T. ) ;
#12947=ORIENTED_EDGE ( 'NONE', *, *, #15294, .T. ) ;
#12949=ADVANCED_FACE ( 'NONE', ( #37016 ), #25517, .T. ) ;
#12950=CARTESIAN_POINT ( 'NONE',  ( 12.00000000000000000, -23.29833615347109088, -3.418703333116486665 ) ) ;
#12952=CIRCLE ( 'NONE', #8210, 31.99999999999999289 ) ;
#12953=DIRECTION ( 'NONE',  ( -1.000000000000000000, 0.000000000000000000, -0.000000000000000000 ) ) ;
#12955=DIRECTION ( 'NONE',  ( 0.000000000000000000, 0.7604059656000322631, -0.6494480483301821039 ) ) ;
#12957=CIRCLE ( 'NONE', #36377, 31.99999999999998224 ) ;
#12969=VECTOR ( 'NONE', #10398, 1000.000000000000000 ) ;
#12970=DIRECTION ( 'NONE',  ( -1.000000000000000000, -0.000000000000000000, 0.000000000000000000 ) ) ;
#12974=FACE_OUTER_BOUND ( 'NONE', #15903, .T. ) ;
#12975=ORIENTED_EDGE ( 'NONE', *, *, #721, .F. ) ;
#12979=VECTOR ( 'NONE', #3053, 1000.000000000000000 ) ;
#12982=ORIENTED_EDGE ( 'NONE', *, *, #20177, .F. ) ;
#12983=ORIENTED_EDGE ( 'NONE', *, *, #29319, .F. ) ;
#12985=ORIENTED_EDGE ( 'NONE', *, *, #1238, .F. ) ;
#12988=DIRECTION ( 'NONE',  ( 0.000000000000000000, -0.3090169943749548342, 0.9510565162951510887 ) ) ;
#12991=DIRECTION ( 'NONE',  ( 0.000000000000000000, 0.000000000000000000, 1.000000000000000000 ) ) ;
#12997=VERTEX_POINT ( 'NONE', #29677 ) ;
#13000=DIRECTION ( 'NONE',  ( 0.000000000000000000, -0.9510565162951566398, 0.3090169943749380144 ) ) ;
#13003=CARTESIAN_POINT ( 'NONE',  ( 11.99999999999999822, -74.65374052328644439, -8.840884882375878107 ) ) ;
#13004=AXIS2_PLACEMENT_3D ( 'NONE', #21350, #16967, #2988 ) ;
#13006=DIRECTION ( 'NONE',  ( -1.000000000000000000, -0.000000000000000000, -0.000000000000000000 ) ) ;
#13012=VERTEX_POINT ( 'NONE', #32401 ) ;
#13013=CARTESIAN_POINT ( 'NONE',  ( 0.000000000000000000, 0.000000000000000000, 0.000000000000000000 ) ) ;
#13016=ADVANCED_FACE ( 'NONE', ( #47327 ), #13801, .T. ) ;
#13018=ADVANCED_FACE ( 'NONE', ( #6445 ), #32628, .T. ) ;
#13021=DIRECTION ( 'NONE',  ( -1.000000000000000000, -0.000000000000000000, -0.000000000000000000 ) ) ;
#13023=ORIENTED_EDGE ( 'NONE', *, *, #19007, .F. ) ;
#13027=DIRECTION ( 'NONE',  ( -1.000000000000000000, 0.000000000000000000, 0.000000000000000000 ) ) ;
#13028=ADVANCED_FACE ( 'NONE', ( #21622 ), #3004, .T. ) ;
#13032=DIRECTION ( 'NONE',  ( 0.000000000000000000, -0.8090169943749497827, -0.5877852522924698064 ) ) ;
#13035=ORIENTED_EDGE ( 'NONE', *, *, #33647, .T. ) ;
#13037=DIRECTION ( 'NONE',  ( -1.000000000000000000, -0.000000000000000000, -0.000000000000000000 ) ) ;
#13038=CIRCLE ( 'NONE', #16939, 31.99999999999998579 ) ;
#13046=DIRECTION ( 'NONE',  ( -1.000000000000000000, 0.000000000000000000, 0.000000000000000000 ) ) ;
#13050=DIRECTION ( 'NONE',  ( 0.000000000000000000, 0.3090169943749450088, -0.9510565162951544194 ) ) ;
#13055=CARTESIAN_POINT ( 'NONE',  ( -10.00000000000000000, 0.000000000000000000, 0.000000000000000000 ) ) ;
#13060=DIRECTION ( 'NONE',  ( -1.000000000000000000, -0.000000000000000000, -0.000000000000000000 ) ) ;
#13063=ADVANCED_FACE ( 'NONE', ( #11575, #19144, #4229, #12061, #8376, #45563, #15964, #11807, #23302, #26990, #3983, #23061, #550, #30414, #38236, #19376, #19608 ), #30906, .F. ) ;
#13064=EDGE_CURVE ( 'NONE', #22172, #14427, #18888, .T. ) ;
#13065=CARTESIAN_POINT ( 'NONE',  ( 0.000000000000000000, -54.21277698773636899, -55.38113227695839669 ) ) ;
#13066=DIRECTION ( 'NONE',  ( -1.000000000000000000, 0.000000000000000000, -0.000000000000000000 ) ) ;
#13072=AXIS2_PLACEMENT_3D ( 'NONE', #19781, #8048, #11736 ) ;
#13074=FACE_OUTER_BOUND ( 'NONE', #22831, .T. ) ;
#13081=VERTEX_POINT ( 'NONE', #295 ) ;
#13085=ORIENTED_EDGE ( 'NONE', *, *, #12478, .T. ) ;
#13086=EDGE_CURVE ( 'NONE', #23062, #25598, #26262, .T. ) ;
#13087=CIRCLE ( 'NONE', #13865, 31.99999999999998579 ) ;
#13088=EDGE_CURVE ( 'NONE', #39316, #40825, #39471, .T. ) ;
#13089=FACE_OUTER_BOUND ( 'NONE', #12722, .T. ) ;
#13090=DIRECTION ( 'NONE',  ( -1.000000000000000000, -0.000000000000000000, -0.000000000000000000 ) ) ;
#13094=CIRCLE ( 'NONE', #45134, 31.99999999999998579 ) ;
#13100=DIRECTION ( 'NONE',  ( -1.000000000000000000, 0.000000000000000000, 0.000000000000000000 ) ) ;
#13102=ORIENTED_EDGE ( 'NONE', *, *, #26628, .T. ) ;
#13110=CARTESIAN_POINT ( 'NONE',  ( 0.000000000000000000, 0.000000000000000000, 0.000000000000000000 ) ) ;
#13112=DIRECTION ( 'NONE',  ( 0.000000000000000000, -0.2334453638558922628, -0.9723699203976798877 ) ) ;
#13115=ORIENTED_EDGE ( 'NONE', *, *, #42534, .F. ) ;
#13121=LINE ( 'NONE', #27088, #20750 ) ;
#13122=VERTEX_POINT ( 'NONE', #20336 ) ;
#13131=DIRECTION ( 'NONE',  ( -1.000000000000000000, -0.000000000000000000, -0.000000000000000000 ) ) ;
#13145=CARTESIAN_POINT ( 'NONE',  ( 0.000000000000000000, 0.000000000000000000, 0.000000000000000000 ) ) ;
#13150=EDGE_CURVE ( 'NONE', #3749, #45952, #16681, .T. ) ;
#13159=VERTEX_POINT ( 'NONE', #13253 ) ;
#13162=CIRCLE ( 'NONE', #40521, 77.49899999999999523 ) ;
#13165=CARTESIAN_POINT ( 'NONE',  ( 0.000000000000000000, 3.894527615417885169, 81.90746397400390322 ) ) ;
#13166=CIRCLE ( 'NONE', #17069, 31.99999999999997868 ) ;
#13167=ORIENTED_EDGE ( 'NONE', *, *, #28339, .F. ) ;
#13174=CARTESIAN_POINT ( 'NONE',  ( 6.000000000000000000, -2.543863470248951320, 81.96053171279901051 ) ) ;
#13184=DIRECTION ( 'NONE',  ( -1.000000000000000000, -0.000000000000000000, 0.000000000000000000 ) ) ;
#13195=VERTEX_POINT ( 'NONE', #5668 ) ;
#13197=AXIS2_PLACEMENT_3D ( 'NONE', #32726, #3099, #40561 ) ;
#13200=AXIS2_PLACEMENT_3D ( 'NONE', #1840, #46871, #19686 ) ;
#13204=CYLINDRICAL_SURFACE ( 'NONE', #37886, 31.99999999999998579 ) ;
#13206=EDGE_LOOP ( 'NONE', ( #18907, #46388, #14710, #45050 ) ) ;
#13212=ADVANCED_FACE ( 'NONE', ( #39447 ), #5427, .T. ) ;
#13214=EDGE_CURVE ( 'NONE', #46211, #12014, #6550, .T. ) ;
#13220=CARTESIAN_POINT ( 'NONE',  ( 0.000000000000000000, 0.000000000000000000, 0.000000000000000000 ) ) ;
#13225=EDGE_LOOP ( 'NONE', ( #32790, #29420, #40296, #40662 ) ) ;
#13226=DIRECTION ( 'NONE',  ( -0.000000000000000000, 0.9135454576426060846, 0.4067366430757888285 ) ) ;
#13227=CARTESIAN_POINT ( 'NONE',  ( 5.999999999999999112, 27.74655509720669500, 77.16300072079670258 ) ) ;
#13230=AXIS2_PLACEMENT_3D ( 'NONE', #11472, #26394, #38128 ) ;
#13233=CARTESIAN_POINT ( 'NONE',  ( 12.00000000000000000, -25.60904388321925040, -6.976881207771167048 ) ) ;
#13234=ORIENTED_EDGE ( 'NONE', *, *, #14464, .T. ) ;
#13240=CYLINDRICAL_SURFACE ( 'NONE', #20852, 77.49899999999999523 ) ;
#13245=CARTESIAN_POINT ( 'NONE',  ( 11.99999999999999822, -18.89407956138310496, 75.16055320797023853 ) ) ;
#13248=FACE_OUTER_BOUND ( 'NONE', #43916, .T. ) ;
#13249=CARTESIAN_POINT ( 'NONE',  ( 0.000000000000000000, -36.73666225445845157, -65.58780272294114866 ) ) ;
#13252=EDGE_LOOP ( 'NONE', ( #35840, #8599, #14909, #36886 ) ) ;
#13253=CARTESIAN_POINT ( 'NONE',  ( 12.00000000000000000, 23.59884966291538433, 12.14883922797231186 ) ) ;
#13256=CARTESIAN_POINT ( 'NONE',  ( 0.000000000000000000, -41.76937507738745836, -62.50329211542482710 ) ) ;
#13264=CARTESIAN_POINT ( 'NONE',  ( 11.99999999999999822, -68.27212725128298132, 31.46837873494953541 ) ) ;
#13267=DIRECTION ( 'NONE',  ( 0.000000000000000000, 1.000000000000000000, 3.469446951953616555E-15 ) ) ;
#13270=VECTOR ( 'NONE', #19633, 1000.000000000000000 ) ;
#13283=ORIENTED_EDGE ( 'NONE', *, *, #43883, .F. ) ;
#13284=CARTESIAN_POINT ( 'NONE',  ( 12.00000000000000000, 22.07842321921492612, 8.187992925817123790 ) ) ;
#13287=CARTESIAN_POINT ( 'NONE',  ( 0.000000000000000000, 0.000000000000000000, 0.000000000000000000 ) ) ;
#13294=DIRECTION ( 'NONE',  ( 0.000000000000000000, 0.000000000000000000, 1.000000000000000000 ) ) ;
#13297=FACE_OUTER_BOUND ( 'NONE', #33300, .T. ) ;
#13300=ORIENTED_EDGE ( 'NONE', *, *, #16265, .T. ) ;
#13303=CARTESIAN_POINT ( 'NONE',  ( 11.99999999999999822, 71.21200624218795383, 40.65526001592638039 ) ) ;
#13304=CARTESIAN_POINT ( 'NONE',  ( 11.99999999999999822, 46.54456581323805153, 59.03342792756280488 ) ) ;
#13305=DIRECTION ( 'NONE',  ( -1.000000000000000000, 0.000000000000000000, 0.000000000000000000 ) ) ;
#13317=DIRECTION ( 'NONE',  ( 0.000000000000000000, 0.000000000000000000, 1.000000000000000000 ) ) ;
#13320=ORIENTED_EDGE ( 'NONE', *, *, #5732, .F. ) ;
#13328=CARTESIAN_POINT ( 'NONE',  ( 11.99999999999999822, -75.11725578898470701, 2.956366410620372864 ) ) ;
#13335=ORIENTED_EDGE ( 'NONE', *, *, #8363, .T. ) ;
#13341=VERTEX_POINT ( 'NONE', #3359 ) ;
#13343=AXIS2_PLACEMENT_3D ( 'NONE', #1484, #16411, #38940 ) ;
#13344=DIRECTION ( 'NONE',  ( -1.000000000000000000, -0.000000000000000000, 0.000000000000000000 ) ) ;
#13353=LINE ( 'NONE', #39788, #9771 ) ;
#13354=CARTESIAN_POINT ( 'NONE',  ( 6.000000000000000000, -34.94270380257585629, -74.18225833017926618 ) ) ;
#13356=EDGE_LOOP ( 'NONE', ( #44325, #11443, #26694, #16184 ) ) ;
#13357=DIRECTION ( 'NONE',  ( -1.000000000000000000, 0.000000000000000000, 0.000000000000000000 ) ) ;
#13361=AXIS2_PLACEMENT_3D ( 'NONE', #35319, #12106, #27030 ) ;
#13362=ADVANCED_FACE ( 'NONE', ( #4102 ), #19015, .T. ) ;
#13364=DIRECTION ( 'NONE',  ( 0.000000000000000000, 0.000000000000000000, 1.000000000000000000 ) ) ;
#13365=VECTOR ( 'NONE', #13390, 1000.000000000000000 ) ;
#13367=LINE ( 'NONE', #47132, #34780 ) ;
#13369=CIRCLE ( 'NONE', #38381, 31.99999999999998224 ) ;
#13373=LINE ( 'NONE', #20957, #8782 ) ;
#13376=CIRCLE ( 'NONE', #3221, 31.99999999999998579 ) ;
#13384=FACE_OUTER_BOUND ( 'NONE', #31814, .T. ) ;
#13390=DIRECTION ( 'NONE',  ( -1.000000000000000000, -0.000000000000000000, -0.000000000000000000 ) ) ;
#13397=CARTESIAN_POINT ( 'NONE',  ( 0.000000000000000000, 75.11764819372149304, -2.946379043146603482 ) ) ;
#13402=DIRECTION ( 'NONE',  ( -1.000000000000000000, -0.000000000000000000, 0.000000000000000000 ) ) ;
#13405=CYLINDRICAL_SURFACE ( 'NONE', #40887, 77.49899999999999523 ) ;
#13408=DIRECTION ( 'NONE',  ( 0.000000000000000000, 0.000000000000000000, 1.000000000000000000 ) ) ;
#13409=ORIENTED_EDGE ( 'NONE', *, *, #11887, .T. ) ;
#13411=CARTESIAN_POINT ( 'NONE',  ( 11.99999999999999822, 39.78640506895604290, 66.50666863322015843 ) ) ;
#13412=VERTEX_POINT ( 'NONE', #663 ) ;
#13413=CIRCLE ( 'NONE', #19642, 77.49900000000000944 ) ;
#13415=DIRECTION ( 'NONE',  ( -1.000000000000000000, 0.000000000000000000, 0.000000000000000000 ) ) ;
#13418=DIRECTION ( 'NONE',  ( -1.000000000000000000, -0.000000000000000000, 0.000000000000000000 ) ) ;
#13419=DIRECTION ( 'NONE',  ( 0.000000000000000000, -0.3826834323650772363, -0.9238795325112919565 ) ) ;
#13428=EDGE_CURVE ( 'NONE', #45301, #4301, #16325, .T. ) ;
#13430=VERTEX_POINT ( 'NONE', #30525 ) ;
#13440=ADVANCED_FACE ( 'NONE', ( #34416 ), #30773, .T. ) ;
#13442=EDGE_LOOP ( 'NONE', ( #14366, #15558, #22499, #47027 ) ) ;
#13443=EDGE_CURVE ( 'NONE', #22912, #21369, #37874, .T. ) ;
#13447=ORIENTED_EDGE ( 'NONE', *, *, #30051, .T. ) ;
#13449=VERTEX_POINT ( 'NONE', #16096 ) ;
#13456=DIRECTION ( 'NONE',  ( -1.000000000000000000, -0.000000000000000000, 0.000000000000000000 ) ) ;
#13459=FACE_OUTER_BOUND ( 'NONE', #26469, .T. ) ;
#13470=DIRECTION ( 'NONE',  ( -1.000000000000000000, -0.000000000000000000, 0.000000000000000000 ) ) ;
#13473=LINE ( 'NONE', #47007, #4436 ) ;
#13477=EDGE_CURVE ( 'NONE', #41663, #47844, #6453, .T. ) ;
#13478=DIRECTION ( 'NONE',  ( -1.000000000000000000, 0.000000000000000000, -0.000000000000000000 ) ) ;
#13479=CARTESIAN_POINT ( 'NONE',  ( 11.99999999999999822, 0.000000000000000000, 0.000000000000000000 ) ) ;
#13482=CARTESIAN_POINT ( 'NONE',  ( 15.00000000000000000, -25.60904388321925040, -6.976881207771165272 ) ) ;
#13483=EDGE_CURVE ( 'NONE', #32098, #46617, #31263, .T. ) ;
#13485=VERTEX_POINT ( 'NONE', #20228 ) ;
#13487=EDGE_CURVE ( 'NONE', #28808, #15783, #24408, .T. ) ;
#13490=CARTESIAN_POINT ( 'NONE',  ( 11.99999999999999822, 0.8261519478441983200, -77.49459641780885022 ) ) ;
#13491=ORIENTED_EDGE ( 'NONE', *, *, #30247, .F. ) ;
#13494=EDGE_LOOP ( 'NONE', ( #36611, #2282, #29401, #28543 ) ) ;
#13497=DIRECTION ( 'NONE',  ( -1.000000000000000000, -0.000000000000000000, 0.000000000000000000 ) ) ;
#13507=CARTESIAN_POINT ( 'NONE',  ( 0.000000000000000000, 0.000000000000000000, 0.000000000000000000 ) ) ;
#13514=CARTESIAN_POINT ( 'NONE',  ( 15.00000000000000000, 16.83928648764922542, -16.46020748918050458 ) ) ;
#13519=PLANE ( 'NONE',  #8398 ) ;
#13520=ORIENTED_EDGE ( 'NONE', *, *, #24569, .F. ) ;
#13522=DIRECTION ( 'NONE',  ( 0.000000000000000000, 0.3826834323650905589, -0.9238795325112864054 ) ) ;
#13527=CYLINDRICAL_SURFACE ( 'NONE', #23000, 31.99999999999998579 ) ;
#13528=VECTOR ( 'NONE', #13803, 1000.000000000000000 ) ;
#13529=CARTESIAN_POINT ( 'NONE',  ( 11.99999999999999822, -68.67312586194971402, -35.91791733033549860 ) ) ;
#13531=DIRECTION ( 'NONE',  ( 0.000000000000000000, 0.000000000000000000, 1.000000000000000000 ) ) ;
#13538=ADVANCED_FACE ( 'NONE', ( #2342 ), #13862, .T. ) ;
#13544=EDGE_CURVE ( 'NONE', #10193, #39901, #13373, .T. ) ;
#13545=ORIENTED_EDGE ( 'NONE', *, *, #12385, .T. ) ;
#13546=ORIENTED_EDGE ( 'NONE', *, *, #4426, .F. ) ;
#13548=AXIS2_PLACEMENT_3D ( 'NONE', #16007, #34577, #34111 ) ;
#13555=VERTEX_POINT ( 'NONE', #39807 ) ;
#13558=AXIS2_PLACEMENT_3D ( 'NONE', #22022, #26438, #11744 ) ;
#13563=FACE_OUTER_BOUND ( 'NONE', #33142, .T. ) ;
#13564=AXIS2_PLACEMENT_3D ( 'NONE', #24610, #47113, #47586 ) ;
#13568=LINE ( 'NONE', #32183, #46971 ) ;
#13578=ORIENTED_EDGE ( 'NONE', *, *, #10868, .F. ) ;
#13586=AXIS2_PLACEMENT_3D ( 'NONE', #35050, #5939, #42403 ) ;
#13594=EDGE_CURVE ( 'NONE', #44798, #1534, #32463, .T. ) ;
#13596=DIRECTION ( 'NONE',  ( -1.000000000000000000, 0.000000000000000000, -0.000000000000000000 ) ) ;
#13601=CARTESIAN_POINT ( 'NONE',  ( 11.99999999999999822, 81.90746397400387480, 3.894527615418187150 ) ) ;
#13606=DIRECTION ( 'NONE',  ( -1.000000000000000000, 0.000000000000000000, 0.000000000000000000 ) ) ;
#13609=EDGE_CURVE ( 'NONE', #27706, #24980, #1884, .T. ) ;
#13617=ORIENTED_EDGE ( 'NONE', *, *, #39649, .T. ) ;
#13618=AXIS2_PLACEMENT_3D ( 'NONE', #1580, #30308, #4112 ) ;
#13620=ORIENTED_EDGE ( 'NONE', *, *, #46906, .T. ) ;
#13621=AXIS2_PLACEMENT_3D ( 'NONE', #34008, #27166, #45767 ) ;
#13624=PLANE ( 'NONE',  #30846 ) ;
#13629=ORIENTED_EDGE ( 'NONE', *, *, #16817, .T. ) ;
#13630=DIRECTION ( 'NONE',  ( 0.000000000000000000, 0.000000000000000000, 1.000000000000000000 ) ) ;
#13631=DIRECTION ( 'NONE',  ( -1.000000000000000000, -0.000000000000000000, 0.000000000000000000 ) ) ;
#13634=CARTESIAN_POINT ( 'NONE',  ( 12.00000000000000000, 8.688484142253932063, -21.88630264137371029 ) ) ;
#13635=EDGE_CURVE ( 'NONE', #22127, #43691, #15057, .T. ) ;
#13636=VERTEX_POINT ( 'NONE', #28294 ) ;
#13637=ORIENTED_EDGE ( 'NONE', *, *, #25183, .T. ) ;
#13639=VERTEX_POINT ( 'NONE', #5796 ) ;
#13641=VECTOR ( 'NONE', #34609, 1000.000000000000227 ) ;
#13642=CARTESIAN_POINT ( 'NONE',  ( 0.000000000000000000, 0.000000000000000000, 0.000000000000000000 ) ) ;
#13643=VECTOR ( 'NONE', #48279, 1000.000000000000000 ) ;
#13644=ADVANCED_FACE ( 'NONE', ( #24632 ), #42995, .T. ) ;
#13648=DIRECTION ( 'NONE',  ( 0.000000000000000000, 0.5877852522924696954, -0.8090169943749498938 ) ) ;
#13652=AXIS2_PLACEMENT_3D ( 'NONE', #42463, #41500, #41747 ) ;
#13654=EDGE_LOOP ( 'NONE', ( #15330, #35152, #41147, #39676 ) ) ;
#13656=CARTESIAN_POINT ( 'NONE',  ( 0.000000000000000000, 17.28742895386084655, 75.54627589209950145 ) ) ;
#13660=AXIS2_PLACEMENT_3D ( 'NONE', #43572, #24012, #16902 ) ;
#13663=ORIENTED_EDGE ( 'NONE', *, *, #45758, .T. ) ;
#13670=LINE ( 'NONE', #35699, #41228 ) ;
#13672=LINE ( 'NONE', #29068, #3631 ) ;
#13678=EDGE_LOOP ( 'NONE', ( #45168, #28516, #5084, #25891 ) ) ;
#13683=CARTESIAN_POINT ( 'NONE',  ( 11.99999999999999822, 44.99326035066052754, 68.55367621811160461 ) ) ;
#13685=ORIENTED_EDGE ( 'NONE', *, *, #48236, .F. ) ;
#13686=VECTOR ( 'NONE', #24591, 1000.000000000000000 ) ;
#13687=AXIS2_PLACEMENT_3D ( 'NONE', #36115, #35645, #2825 ) ;
#13690=VERTEX_POINT ( 'NONE', #3552 ) ;
#13695=ADVANCED_FACE ( 'NONE', ( #22406 ), #26318, .T. ) ;
#13696=ORIENTED_EDGE ( 'NONE', *, *, #14085, .F. ) ;
#13698=ORIENTED_EDGE ( 'NONE', *, *, #11608, .T. ) ;
#13704=EDGE_CURVE ( 'NONE', #47811, #2023, #11401, .T. ) ;
#13707=EDGE_LOOP ( 'NONE', ( #22408, #43979, #2724, #6867, #7486, #33000, #7797, #45539, #11431, #4636, #11023, #37587, #9348, #16648, #12254, #7997, #35054, #9511, #2009, #47775, #841, #22779, #21272, #47623, #44090, #15913, #27885, #30327, #46365, #27411, #25549, #37043, #45791, #29875, #45069, #42110, #7412, #31358, #43597, #36495, #29634, #29285, #20237, #5034, #41505, #21755, #32859, #27170, #16769, #32855, #10753, #33480, #20373, #1335, #40875, #35940, #2206, #568, #39263, #13578, #21460, #40305, #23129, #42068, #1126, #933, #36876, #47164, #18227, #47698, #47378, #9283, #27364, #6585, #18213, #39918, #46378, #14928, #28103, #28187, #17055, #1403, #28699, #16225, #3080, #18682, #834, #6112, #21825, #10556, #20929, #7356, #20255, #30923, #30831, #5317, #12492, #42916, #12370, #30919, #32996, #47402, #16210, #25828, #34397, #5812, #36722, #24065, #7557, #44040, #21040, #6547, #37052, #30283, #504, #5382, #33160, #38376, #18393, #15405, #3476, #30986, #36707, #27111, #6933, #11837, #43891, #10691, #6173, #7767, #31994, #20396, #41269, #44130, #25714, #3703, #35610, #27910, #27857, #391, #11309, #37475, #30383, #48106, #23750, #11523, #43780, #42606, #12420, #4829, #40005, #42883, #30701, #30027, #41220, #20979, #22729, #21925, #2019, #13491, #48168, #44565, #45730, #14340, #45163, #29532, #48099, #11345, #2474, #40312, #46919, #31390, #37169, #43949, #4488, #34488, #34626, #16187, #7650, #5929, #47804, #43569, #384, #34141, #8457, #24704, #30313, #25007, #39575, #43565, #26619, #9399, #2364, #17420, #12985, #30813, #38910, #41827, #12320, #586, #35329, #21122, #35751, #7792, #34974, #15789, #45835, #39426, #29818, #22531, #39652, #47716, #35116, #5514, #17670, #9849, #5560, #34955, #16863, #6727, #12598, #16328, #20977, #17458, #32470, #15356, #35300, #41951, #13763, #25877, #11512, #5868, #18622, #43056, #12147, #37879, #46855, #46987, #40008, #18073, #2077, #46762, #35685, #4550, #44164, #39843, #7886, #11236, #48260, #41276, #21498, #48174, #42056, #36598, #12656, #3223, #39537, #42170, #31508, #47782, #43453, #47032, #31532, #34790, #41312, #4180, #39723, #36490, #45177, #42745, #8325, #3653, #2746, #10870, #9940, #527, #45698, #3309, #27862, #40606, #2008, #42245, #3100, #38586, #19330, #38061, #41633, #35482, #41678, #34225, #5381, #5489, #20205, #36131, #29231, #11626, #23149, #11824, #32914, #2887, #2387, #27777, #10571, #34125, #10730, #15911, #22878, #28437, #43607, #29862, #23555, #35949, #34827, #11952, #45802, #8991, #1483, #33038, #19213, #15700, #4335, #29927, #22100, #36673, #13685 ) ) ;
#13709=CARTESIAN_POINT ( 'NONE',  ( 0.000000000000000000, 17.28742895386189105, -75.54627589209924565 ) ) ;
#13720=CARTESIAN_POINT ( 'NONE',  ( 0.000000000000000000, 63.97538442413498672, -51.29473840253155004 ) ) ;
#13722=EDGE_CURVE ( 'NONE', #6056, #31411, #33642, .T. ) ;
#13724=CARTESIAN_POINT ( 'NONE',  ( 0.000000000000000000, 0.000000000000000000, 0.000000000000000000 ) ) ;
#13726=AXIS2_PLACEMENT_3D ( 'NONE', #6885, #22041, #14477 ) ;
#13727=CIRCLE ( 'NONE', #40284, 31.99999999999998579 ) ;
#13735=DIRECTION ( 'NONE',  ( 0.000000000000000000, -0.9238795325112906243, 0.3826834323650805114 ) ) ;
#13736=EDGE_LOOP ( 'NONE', ( #37970, #31153, #39733, #36174 ) ) ;
#13737=ORIENTED_EDGE ( 'NONE', *, *, #18529, .F. ) ;
#13754=VERTEX_POINT ( 'NONE', #33175 ) ;
#13755=CYLINDRICAL_SURFACE ( 'NONE', #18795, 77.49899999999999523 ) ;
#13762=CIRCLE ( 'NONE', #46615, 82.00000000000000000 ) ;
#13763=ORIENTED_EDGE ( 'NONE', *, *, #9650, .F. ) ;
#13764=DIRECTION ( 'NONE',  ( -1.000000000000000000, 0.000000000000000000, 0.000000000000000000 ) ) ;
#13776=ADVANCED_FACE ( 'NONE', ( #47843 ), #36597, .T. ) ;
#13780=VECTOR ( 'NONE', #32621, 1000.000000000000000 ) ;
#13781=DIRECTION ( 'NONE',  ( -1.000000000000000000, -0.000000000000000000, -0.000000000000000000 ) ) ;
#13782=CARTESIAN_POINT ( 'NONE',  ( -10.00000000000000000, 0.000000000000000000, 0.000000000000000000 ) ) ;
#13784=DIRECTION ( 'NONE',  ( -1.000000000000000000, 0.000000000000000000, 0.000000000000000000 ) ) ;
#13785=AXIS2_PLACEMENT_3D ( 'NONE', #30145, #7851, #33321 ) ;
#13788=ADVANCED_FACE ( 'NONE', ( #14817 ), #40756, .T. ) ;
#13789=CIRCLE ( 'NONE', #45049, 31.99999999999999289 ) ;
#13795=LINE ( 'NONE', #21611, #13780 ) ;
#13798=EDGE_CURVE ( 'NONE', #34257, #31329, #32994, .T. ) ;
#13800=AXIS2_PLACEMENT_3D ( 'NONE', #25650, #22713, #48183 ) ;
#13801=CYLINDRICAL_SURFACE ( 'NONE', #39437, 82.00000000000000000 ) ;
#13802=EDGE_LOOP ( 'NONE', ( #14284, #2491, #28785, #7315 ) ) ;
#13803=DIRECTION ( 'NONE',  ( -1.000000000000000000, -0.000000000000000000, 0.000000000000000000 ) ) ;
#13806=ORIENTED_EDGE ( 'NONE', *, *, #41138, .F. ) ;
#13807=VERTEX_POINT ( 'NONE', #37566 ) ;
#13808=EDGE_CURVE ( 'NONE', #12269, #28196, #29262, .T. ) ;
#13814=ORIENTED_EDGE ( 'NONE', *, *, #814, .T. ) ;
#13819=DIRECTION ( 'NONE',  ( 0.000000000000000000, -0.5000000000000039968, -0.8660254037844363761 ) ) ;
#13821=EDGE_LOOP ( 'NONE', ( #45514, #7615, #10711, #19056 ) ) ;
#13826=AXIS2_PLACEMENT_3D ( 'NONE', #25563, #47595, #25083 ) ;
#13843=LINE ( 'NONE', #35372, #41634 ) ;
#13852=LINE ( 'NONE', #9203, #40138 ) ;
#13857=LINE ( 'NONE', #39802, #11513 ) ;
#13858=DIRECTION ( 'NONE',  ( 1.000000000000000000, -0.000000000000000000, -0.000000000000000000 ) ) ;
#13862=CYLINDRICAL_SURFACE ( 'NONE', #21289, 77.49899999999999523 ) ;
#13863=ORIENTED_EDGE ( 'NONE', *, *, #31424, .T. ) ;
#13865=AXIS2_PLACEMENT_3D ( 'NONE', #3520, #40263, #43914 ) ;
#13866=ORIENTED_EDGE ( 'NONE', *, *, #34907, .T. ) ;
#13868=CIRCLE ( 'NONE', #47461, 82.00000000000000000 ) ;
#13876=ORIENTED_EDGE ( 'NONE', *, *, #22210, .T. ) ;
#13883=EDGE_LOOP ( 'NONE', ( #17664, #45388, #45652, #47715 ) ) ;
#13884=CYLINDRICAL_SURFACE ( 'NONE', #22390, 82.00000000000000000 ) ;
#13886=EDGE_CURVE ( 'NONE', #127, #45331, #31524, .T. ) ;
#13890=DIRECTION ( 'NONE',  ( 0.000000000000000000, 0.2079116908177641720, 0.9781476007338045786 ) ) ;
#13891=CARTESIAN_POINT ( 'NONE',  ( 0.000000000000000000, -60.67117009219096957, -55.16347631943106933 ) ) ;
#13894=AXIS2_PLACEMENT_3D ( 'NONE', #21, #19575, #34512 ) ;
#13898=CARTESIAN_POINT ( 'NONE',  ( -10.00000000000000000, 0.000000000000000000, 0.000000000000000000 ) ) ;
#13909=ORIENTED_EDGE ( 'NONE', *, *, #19721, .F. ) ;
#13912=EDGE_CURVE ( 'NONE', #37888, #3320, #26792, .T. ) ;
#13919=AXIS2_PLACEMENT_3D ( 'NONE', #12681, #23942, #31537 ) ;
#13925=EDGE_CURVE ( 'NONE', #20359, #35932, #8430, .T. ) ;
#13926=EDGE_CURVE ( 'NONE', #6721, #34257, #9582, .T. ) ;
#13930=ORIENTED_EDGE ( 'NONE', *, *, #16573, .T. ) ;
#13935=CARTESIAN_POINT ( 'NONE',  ( 0.000000000000000000, 14.66109333815460225, 73.73191006444577056 ) ) ;
#13940=DIRECTION ( 'NONE',  ( -1.000000000000000000, -0.000000000000000000, -0.000000000000000000 ) ) ;
#13942=VERTEX_POINT ( 'NONE', #5003 ) ;
#13944=CARTESIAN_POINT ( 'NONE',  ( 0.000000000000000000, -44.99326035066101781, 68.55367621811126355 ) ) ;
#13948=CARTESIAN_POINT ( 'NONE',  ( 11.99999999999999822, 72.35160999960844208, -20.41045688087747223 ) ) ;
#13957=VECTOR ( 'NONE', #35691, 1000.000000000000000 ) ;
#13959=CARTESIAN_POINT ( 'NONE',  ( 0.000000000000000000, 0.000000000000000000, 0.000000000000000000 ) ) ;
#13964=EDGE_LOOP ( 'NONE', ( #16721, #40354, #16017, #10489 ) ) ;
#13969=CARTESIAN_POINT ( 'NONE',  ( 6.000000000000000000, 8.966570791700705811, 81.50828551894228724 ) ) ;
#13977=ADVANCED_FACE ( 'NONE', ( #42700 ), #35589, .T. ) ;
#13982=CIRCLE ( 'NONE', #9304, 82.00000000000000000 ) ;
#13993=CARTESIAN_POINT ( 'NONE',  ( 11.99999999999999822, 0.000000000000000000, 0.000000000000000000 ) ) ;
#13996=CARTESIAN_POINT ( 'NONE',  ( 11.99999999999999822, 0.000000000000000000, 0.000000000000000000 ) ) ;
#13998=ORIENTED_EDGE ( 'NONE', *, *, #12220, .T. ) ;
#14001=ORIENTED_EDGE ( 'NONE', *, *, #3435, .T. ) ;
#14004=ORIENTED_EDGE ( 'NONE', *, *, #46551, .T. ) ;
#14012=DIRECTION ( 'NONE',  ( -1.000000000000000000, 0.000000000000000000, 0.000000000000000000 ) ) ;
#14020=FACE_OUTER_BOUND ( 'NONE', #12676, .T. ) ;
#14025=CIRCLE ( 'NONE', #26541, 77.49900000000000944 ) ;
#14027=CARTESIAN_POINT ( 'NONE',  ( 11.99999999999999822, 14.67089635893713684, 73.72996012237443608 ) ) ;
#14029=EDGE_LOOP ( 'NONE', ( #11540, #41423, #43828, #6601 ) ) ;
#14032=EDGE_CURVE ( 'NONE', #10055, #12035, #8052, .T. ) ;
#14038=DIRECTION ( 'NONE',  ( -1.000000000000000000, 0.000000000000000000, -0.000000000000000000 ) ) ;
#14039=VERTEX_POINT ( 'NONE', #36058 ) ;
#14046=DIRECTION ( 'NONE',  ( -1.000000000000000000, 0.000000000000000000, -0.000000000000000000 ) ) ;
#14048=DIRECTION ( 'NONE',  ( 1.000000000000000000, 0.000000000000000000, -0.000000000000000000 ) ) ;
#14054=VECTOR ( 'NONE', #23230, 1000.000000000000114 ) ;
#14059=ORIENTED_EDGE ( 'NONE', *, *, #6188, .F. ) ;
#14060=LINE ( 'NONE', #43681, #41094 ) ;
#14063=DIRECTION ( 'NONE',  ( -1.000000000000000000, -0.000000000000000000, -0.000000000000000000 ) ) ;
#14072=DIRECTION ( 'NONE',  ( 0.000000000000000000, 0.9945218953682730678, -0.1045284632676570929 ) ) ;
#14074=CIRCLE ( 'NONE', #21077, 82.00000000000000000 ) ;
#14075=ORIENTED_EDGE ( 'NONE', *, *, #5257, .T. ) ;
#14078=CARTESIAN_POINT ( 'NONE',  ( 11.99999999999999822, 68.55367621811141987, 44.99326035066078333 ) ) ;
#14084=EDGE_CURVE ( 'NONE', #48350, #20992, #35337, .T. ) ;
#14085=EDGE_CURVE ( 'NONE', #10568, #40057, #10120, .T. ) ;
#14086=DIRECTION ( 'NONE',  ( -1.000000000000000000, 0.000000000000000000, -0.000000000000000000 ) ) ;
#14091=EDGE_CURVE ( 'NONE', #4178, #43952, #30707, .T. ) ;
#14094=EDGE_CURVE ( 'NONE', #25033, #23062, #16981, .T. ) ;
#14098=ORIENTED_EDGE ( 'NONE', *, *, #24875, .T. ) ;
#14111=ORIENTED_EDGE ( 'NONE', *, *, #15588, .F. ) ;
#14113=DIRECTION ( 'NONE',  ( -1.000000000000000000, -0.000000000000000000, 0.000000000000000000 ) ) ;
#14114=ADVANCED_FACE ( 'NONE', ( #32632 ), #36307, .F. ) ;
#14122=CARTESIAN_POINT ( 'NONE',  ( 12.00000000000000000, -22.67460108101774452, 6.353146135318220367 ) ) ;
#14123=DIRECTION ( 'NONE',  ( -1.000000000000000000, -0.000000000000000000, -0.000000000000000000 ) ) ;
#14125=DIRECTION ( 'NONE',  ( -1.000000000000000000, -0.000000000000000000, 0.000000000000000000 ) ) ;
#14130=EDGE_CURVE ( 'NONE', #40856, #47874, #14766, .T. ) ;
#14141=DIRECTION ( 'NONE',  ( -1.000000000000000000, 0.000000000000000000, -0.000000000000000000 ) ) ;
#14151=EDGE_CURVE ( 'NONE', #15029, #38875, #17405, .T. ) ;
#14153=ADVANCED_FACE ( 'NONE', ( #40700 ), #11086, .T. ) ;
#14154=VERTEX_POINT ( 'NONE', #40953 ) ;
#14163=AXIS2_PLACEMENT_3D ( 'NONE', #43564, #10257, #32073 ) ;
#14166=ORIENTED_EDGE ( 'NONE', *, *, #3364, .T. ) ;
#14173=LINE ( 'NONE', #2660, #29083 ) ;
#14179=CARTESIAN_POINT ( 'NONE',  ( 5.999999999999999112, -59.75363087400035056, -56.15606465355020305 ) ) ;
#14181=DIRECTION ( 'NONE',  ( 0.000000000000000000, -0.8090169943749426773, 0.5877852522924797984 ) ) ;
#14188=CARTESIAN_POINT ( 'NONE',  ( 0.000000000000000000, 62.50884508063427347, 41.76106447765511831 ) ) ;
#14192=DIRECTION ( 'NONE',  ( -1.000000000000000000, 0.000000000000000000, -0.000000000000000000 ) ) ;
#14194=ADVANCED_FACE ( 'NONE', ( #40234 ), #26004, .T. ) ;
#14195=AXIS2_PLACEMENT_3D ( 'NONE', #23087, #19168, #3516 ) ;
#14199=AXIS2_PLACEMENT_3D ( 'NONE', #18125, #33066, #36976 ) ;
#14200=LINE ( 'NONE', #28403, #18190 ) ;
#14205=DIRECTION ( 'NONE',  ( -1.000000000000000000, -0.000000000000000000, 0.000000000000000000 ) ) ;
#14209=ORIENTED_EDGE ( 'NONE', *, *, #20727, .F. ) ;
#14213=EDGE_CURVE ( 'NONE', #22290, #35782, #20594, .T. ) ;
#14215=ORIENTED_EDGE ( 'NONE', *, *, #46299, .F. ) ;
#14219=CYLINDRICAL_SURFACE ( 'NONE', #10471, 82.00000000000000000 ) ;
#14224=VERTEX_POINT ( 'NONE', #25523 ) ;
#14227=ORIENTED_EDGE ( 'NONE', *, *, #29058, .T. ) ;
#14233=CARTESIAN_POINT ( 'NONE',  ( 0.000000000000000000, -68.27212725128254078, -31.46837873495049465 ) ) ;
#14236=DIRECTION ( 'NONE',  ( -1.000000000000000000, -0.000000000000000000, -0.000000000000000000 ) ) ;
#14240=DIRECTION ( 'NONE',  ( -1.000000000000000000, -0.000000000000000000, 0.000000000000000000 ) ) ;
#14241=ORIENTED_EDGE ( 'NONE', *, *, #27098, .F. ) ;
#14243=DIRECTION ( 'NONE',  ( -1.000000000000000000, -0.000000000000000000, -0.000000000000000000 ) ) ;
#14244=DIRECTION ( 'NONE',  ( -1.000000000000000000, -0.000000000000000000, 0.000000000000000000 ) ) ;
#14254=CARTESIAN_POINT ( 'NONE',  ( 11.99999999999999822, -77.32052557432845674, 5.256550761632577284 ) ) ;
#14262=CARTESIAN_POINT ( 'NONE',  ( -10.00000000000000000, 0.000000000000000000, 0.000000000000000000 ) ) ;
#14267=VERTEX_POINT ( 'NONE', #15255 ) ;
#14268=ADVANCED_FACE ( 'NONE', ( #8137 ), #19381, .T. ) ;
#14269=CIRCLE ( 'NONE', #11930, 31.99999999999999289 ) ;
#14271=DIRECTION ( 'NONE',  ( -1.000000000000000000, 0.000000000000000000, 0.000000000000000000 ) ) ;
#14279=VECTOR ( 'NONE', #6020, 1000.000000000000000 ) ;
#14280=VECTOR ( 'NONE', #6751, 1000.000000000000114 ) ;
#14283=CARTESIAN_POINT ( 'NONE',  ( 12.00000000000000000, -0.9646360437372099028, 23.52805723605590771 ) ) ;
#14284=ORIENTED_EDGE ( 'NONE', *, *, #34971, .F. ) ;
#14285=DIRECTION ( 'NONE',  ( -1.000000000000000000, 0.000000000000000000, 0.000000000000000000 ) ) ;
#14286=DIRECTION ( 'NONE',  ( 0.000000000000000000, 0.000000000000000000, 1.000000000000000000 ) ) ;
#14293=CYLINDRICAL_SURFACE ( 'NONE', #34478, 82.00000000000000000 ) ;
#14295=AXIS2_PLACEMENT_3D ( 'NONE', #26962, #8577, #7859 ) ;
#14297=ORIENTED_EDGE ( 'NONE', *, *, #42276, .T. ) ;
#14298=DIRECTION ( 'NONE',  ( -1.000000000000000000, 0.000000000000000000, 0.000000000000000000 ) ) ;
#14305=FACE_OUTER_BOUND ( 'NONE', #18613, .T. ) ;
#14308=PLANE ( 'NONE',  #47180 ) ;
#14310=CIRCLE ( 'NONE', #4152, 31.99999999999998579 ) ;
#14321=EDGE_CURVE ( 'NONE', #14957, #17765, #19021, .T. ) ;
#14322=LINE ( 'NONE', #18221, #12979 ) ;
#14323=DIRECTION ( 'NONE',  ( 0.000000000000000000, 0.000000000000000000, 1.000000000000000000 ) ) ;
#14328=DIRECTION ( 'NONE',  ( 0.000000000000000000, 0.000000000000000000, 1.000000000000000000 ) ) ;
#14332=EDGE_CURVE ( 'NONE', #11988, #30740, #38241, .T. ) ;
#14333=VERTEX_POINT ( 'NONE', #11811 ) ;
#14339=CYLINDRICAL_SURFACE ( 'NONE', #43726, 82.00000000000000000 ) ;
#14340=ORIENTED_EDGE ( 'NONE', *, *, #5937, .F. ) ;
#14341=VECTOR ( 'NONE', #42496, 1000.000000000000000 ) ;
#14345=AXIS2_PLACEMENT_3D ( 'NONE', #11787, #8107, #18403 ) ;
#14346=CYLINDRICAL_SURFACE ( 'NONE', #27343, 31.99999999999998579 ) ;
#14349=ORIENTED_EDGE ( 'NONE', *, *, #16829, .T. ) ;
#14355=DIRECTION ( 'NONE',  ( 0.000000000000000000, 0.000000000000000000, 1.000000000000000000 ) ) ;
#14357=CARTESIAN_POINT ( 'NONE',  ( 11.99999999999999822, 0.000000000000000000, 0.000000000000000000 ) ) ;
#14362=CARTESIAN_POINT ( 'NONE',  ( 11.99999999999999822, 0.000000000000000000, 0.000000000000000000 ) ) ;
#14366=ORIENTED_EDGE ( 'NONE', *, *, #26167, .F. ) ;
#14372=CIRCLE ( 'NONE', #20612, 77.49899999999999523 ) ;
#14376=ORIENTED_EDGE ( 'NONE', *, *, #16601, .F. ) ;
#14378=CARTESIAN_POINT ( 'NONE',  ( 15.00000000000000000, 5.835314593368470248, -22.81335362449854642 ) ) ;
#14380=AXIS2_PLACEMENT_3D ( 'NONE', #143, #1115, #15811 ) ;
#14382=CARTESIAN_POINT ( 'NONE',  ( 11.99999999999999822, 74.65491531819118620, -8.830959090342659579 ) ) ;
#14387=CARTESIAN_POINT ( 'NONE',  ( 12.00000000000000000, 20.85821328998741109, -10.92862929874522671 ) ) ;
#14390=LINE ( 'NONE', #18287, #18489 ) ;
#14391=CARTESIAN_POINT ( 'NONE',  ( 0.000000000000000000, 0.000000000000000000, 0.000000000000000000 ) ) ;
#14392=EDGE_CURVE ( 'NONE', #36067, #12155, #23714, .T. ) ;
#14393=AXIS2_PLACEMENT_3D ( 'NONE', #22025, #17870, #44313 ) ;
#14397=EDGE_LOOP ( 'NONE', ( #19749, #42831, #44348, #25186 ) ) ;
#14398=ORIENTED_EDGE ( 'NONE', *, *, #27290, .T. ) ;
#14399=ORIENTED_EDGE ( 'NONE', *, *, #17456, .T. ) ;
#14400=EDGE_CURVE ( 'NONE', #18807, #39592, #39329, .T. ) ;
#14402=DIRECTION ( 'NONE',  ( 0.000000000000000000, 0.8090169943749486725, -0.5877852522924713607 ) ) ;
#14405=EDGE_CURVE ( 'NONE', #26988, #30390, #28422, .T. ) ;
#14406=CIRCLE ( 'NONE', #30059, 31.99999999999998579 ) ;
#14407=DIRECTION ( 'NONE',  ( -1.000000000000000000, -0.000000000000000000, 0.000000000000000000 ) ) ;
#14408=CIRCLE ( 'NONE', #36274, 77.49899999999999523 ) ;
#14409=EDGE_LOOP ( 'NONE', ( #6690, #34277, #23572, #44193 ) ) ;
#14412=CARTESIAN_POINT ( 'NONE',  ( 11.99999999999999822, -69.42325613327466272, 34.44570377933573724 ) ) ;
#14413=VECTOR ( 'NONE', #16672, 999.9999999999998863 ) ;
#14414=ORIENTED_EDGE ( 'NONE', *, *, #28127, .T. ) ;
#14418=EDGE_CURVE ( 'NONE', #4565, #33667, #10429, .T. ) ;
#14427=VERTEX_POINT ( 'NONE', #31882 ) ;
#14434=DIRECTION ( 'NONE',  ( -1.000000000000000000, -0.000000000000000000, -0.000000000000000000 ) ) ;
#14436=VERTEX_POINT ( 'NONE', #13490 ) ;
#14439=DIRECTION ( 'NONE',  ( -1.000000000000000000, 0.000000000000000000, 0.000000000000000000 ) ) ;
#14443=AXIS2_PLACEMENT_3D ( 'NONE', #17309, #24905, #39847 ) ;
#14447=VECTOR ( 'NONE', #27296, 1000.000000000000000 ) ;
#14449=CARTESIAN_POINT ( 'NONE',  ( 0.000000000000000000, 0.000000000000000000, 0.000000000000000000 ) ) ;
#14455=VECTOR ( 'NONE', #33603, 1000.000000000000000 ) ;
#14456=AXIS2_PLACEMENT_3D ( 'NONE', #29734, #3550, #18710 ) ;
#14460=AXIS2_PLACEMENT_3D ( 'NONE', #29162, #25726, #44581 ) ;
#14463=ORIENTED_EDGE ( 'NONE', *, *, #38472, .T. ) ;
#14464=EDGE_CURVE ( 'NONE', #1147, #19053, #24484, .T. ) ;
#14472=VECTOR ( 'NONE', #12110, 1000.000000000000000 ) ;
#14475=EDGE_CURVE ( 'NONE', #34767, #9901, #8087, .T. ) ;
#14477=DIRECTION ( 'NONE',  ( 0.000000000000000000, 0.000000000000000000, 1.000000000000000000 ) ) ;
#14478=ORIENTED_EDGE ( 'NONE', *, *, #19317, .T. ) ;
#14484=CYLINDRICAL_SURFACE ( 'NONE', #13785, 31.99999999999998579 ) ;
#14486=EDGE_LOOP ( 'NONE', ( #27283, #11310, #10698, #3859 ) ) ;
#14487=DIRECTION ( 'NONE',  ( 0.000000000000000000, 0.000000000000000000, 1.000000000000000000 ) ) ;
#14494=ADVANCED_FACE ( 'NONE', ( #43116 ), #9335, .T. ) ;
#14495=DIRECTION ( 'NONE',  ( -1.000000000000000000, -0.000000000000000000, -0.000000000000000000 ) ) ;
#14497=ORIENTED_EDGE ( 'NONE', *, *, #40543, .T. ) ;
#14499=AXIS2_PLACEMENT_3D ( 'NONE', #29593, #22259, #25665 ) ;
#14500=EDGE_CURVE ( 'NONE', #39232, #20737, #40905, .T. ) ;
#14513=AXIS2_PLACEMENT_3D ( 'NONE', #28829, #36168, #21235 ) ;
#14528=EDGE_CURVE ( 'NONE', #48218, #48350, #3396, .T. ) ;
#14530=EDGE_CURVE ( 'NONE', #27089, #11938, #43293, .T. ) ;
#14531=CARTESIAN_POINT ( 'NONE',  ( 0.000000000000000000, 75.11764819372149304, -2.946379043146603482 ) ) ;
#14532=VECTOR ( 'NONE', #5775, 1000.000000000000000 ) ;
#14533=ORIENTED_EDGE ( 'NONE', *, *, #13064, .T. ) ;
#14537=DIRECTION ( 'NONE',  ( -1.000000000000000000, 0.000000000000000000, 0.000000000000000000 ) ) ;
#14539=DIRECTION ( 'NONE',  ( 0.000000000000000000, 0.000000000000000000, 1.000000000000000000 ) ) ;
#14542=LINE ( 'NONE', #40006, #30151 ) ;
#14545=ADVANCED_FACE ( 'NONE', ( #40412 ), #40168, .T. ) ;
#14551=DIRECTION ( 'NONE',  ( 0.000000000000000000, 0.000000000000000000, 1.000000000000000000 ) ) ;
#14556=DIRECTION ( 'NONE',  ( 0.000000000000000000, 0.2334453638558989796, 0.9723699203976782224 ) ) ;
#14561=ADVANCED_FACE ( 'NONE', ( #40881 ), #29129, .T. ) ;
#14563=CARTESIAN_POINT ( 'NONE',  ( 11.99999999999999822, -71.21200624218823805, 40.65526001592589722 ) ) ;
#14565=LINE ( 'NONE', #29713, #33889 ) ;
#14568=CARTESIAN_POINT ( 'NONE',  ( 0.000000000000000000, -39.47590169984898267, 71.87247863392400404 ) ) ;
#14572=CARTESIAN_POINT ( 'NONE',  ( 12.00000000000000000, -23.29833615347104470, 3.418703333116808629 ) ) ;
#14576=DIRECTION ( 'NONE',  ( -1.000000000000000000, -0.000000000000000000, 0.000000000000000000 ) ) ;
#14588=VERTEX_POINT ( 'NONE', #2946 ) ;
#14589=ADVANCED_FACE ( 'NONE', ( #28669 ), #36711, .T. ) ;
#14590=CIRCLE ( 'NONE', #5969, 77.49899999999999523 ) ;
#14591=EDGE_CURVE ( 'NONE', #24320, #28070, #36948, .T. ) ;
#14595=VERTEX_POINT ( 'NONE', #18362 ) ;
#14597=ORIENTED_EDGE ( 'NONE', *, *, #24819, .T. ) ;
#14599=CARTESIAN_POINT ( 'NONE',  ( 12.00000000000000000, 5.835314593368777558, 22.81335362449846471 ) ) ;
#14601=DIRECTION ( 'NONE',  ( -1.000000000000000000, -0.000000000000000000, 0.000000000000000000 ) ) ;
#14608=EDGE_CURVE ( 'NONE', #1470, #42776, #25939, .T. ) ;
#14609=EDGE_CURVE ( 'NONE', #39158, #37621, #31595, .T. ) ;
#14611=LINE ( 'NONE', #10922, #35221 ) ;
#14612=DIRECTION ( 'NONE',  ( 0.000000000000000000, 0.5877852522924780221, 0.8090169943749438985 ) ) ;
#14613=ORIENTED_EDGE ( 'NONE', *, *, #35588, .T. ) ;
#14617=VERTEX_POINT ( 'NONE', #33294 ) ;
#14618=CARTESIAN_POINT ( 'NONE',  ( 11.99999999999999822, -74.74816331893454446, 33.71516098798715433 ) ) ;
#14629=VERTEX_POINT ( 'NONE', #44546 ) ;
#14631=ORIENTED_EDGE ( 'NONE', *, *, #27827, .T. ) ;
#14632=DIRECTION ( 'NONE',  ( -1.000000000000000000, 0.000000000000000000, -0.000000000000000000 ) ) ;
#14636=CARTESIAN_POINT ( 'NONE',  ( 0.000000000000000000, -12.93880638057260590, -76.41127070299285151 ) ) ;
#14655=VERTEX_POINT ( 'NONE', #17640 ) ;
#14662=ADVANCED_FACE ( 'NONE', ( #41863 ), #30588, .T. ) ;
#14667=DIRECTION ( 'NONE',  ( 0.000000000000000000, -0.7071067811865536790, 0.7071067811865414665 ) ) ;
#14668=DIRECTION ( 'NONE',  ( 1.000000000000000000, -0.000000000000000000, -0.000000000000000000 ) ) ;
#14672=ADVANCED_FACE ( 'NONE', ( #23474 ), #37940, .T. ) ;
#14674=AXIS2_PLACEMENT_3D ( 'NONE', #41911, #40934, #45316 ) ;
#14675=ORIENTED_EDGE ( 'NONE', *, *, #32753, .T. ) ;
#14676=ORIENTED_EDGE ( 'NONE', *, *, #7013, .T. ) ;
#14698=DIRECTION ( 'NONE',  ( -1.000000000000000000, 0.000000000000000000, 0.000000000000000000 ) ) ;
#14710=ORIENTED_EDGE ( 'NONE', *, *, #41343, .T. ) ;
#14715=PRODUCT_DEFINITION_FORMATION_WITH_SPECIFIED_SOURCE ( 'ANY', '', #46831, .NOT_KNOWN. ) ;
#14716=AXIS2_PLACEMENT_3D ( 'NONE', #34474, #23467, #7589 ) ;
#14721=ORIENTED_EDGE ( 'NONE', *, *, #15638, .T. ) ;
#14723=CARTESIAN_POINT ( 'NONE',  ( 0.000000000000000000, 0.000000000000000000, 0.000000000000000000 ) ) ;
#14729=EDGE_CURVE ( 'NONE', #17607, #28640, #7320, .T. ) ;
#14733=ORIENTED_EDGE ( 'NONE', *, *, #22727, .F. ) ;
#14734=ORIENTED_EDGE ( 'NONE', *, *, #38760, .F. ) ;
#14742=AXIS2_PLACEMENT_3D ( 'NONE', #8450, #5276, #31721 ) ;
#14747=DIRECTION ( 'NONE',  ( -1.000000000000000000, -0.000000000000000000, 0.000000000000000000 ) ) ;
#14748=DIRECTION ( 'NONE',  ( -1.000000000000000000, 0.000000000000000000, 0.000000000000000000 ) ) ;
#14749=CARTESIAN_POINT ( 'NONE',  ( 0.000000000000000000, -16.65972982744991171, 80.28980883073752750 ) ) ;
#14752=DIRECTION ( 'NONE',  ( -1.000000000000000000, -0.000000000000000000, -0.000000000000000000 ) ) ;
#14753=VERTEX_POINT ( 'NONE', #44538 ) ;
#14754=LINE ( 'NONE', #22813, #16276 ) ;
#14763=DIRECTION ( 'NONE',  ( -1.000000000000000000, -0.000000000000000000, 0.000000000000000000 ) ) ;
#14765=EDGE_CURVE ( 'NONE', #11748, #27398, #9660, .T. ) ;
#14766=LINE ( 'NONE', #29449, #28359 ) ;
#14769=ADVANCED_FACE ( 'NONE', ( #14940 ), #8065, .F. ) ;
#14770=CYLINDRICAL_SURFACE ( 'NONE', #15242, 31.99999999999998579 ) ;
#14772=ORIENTED_EDGE ( 'NONE', *, *, #17370, .F. ) ;
#14776=CARTESIAN_POINT ( 'NONE',  ( 0.000000000000000000, 0.000000000000000000, 0.000000000000000000 ) ) ;
#14779=DIRECTION ( 'NONE',  ( -1.000000000000000000, 0.000000000000000000, 0.000000000000000000 ) ) ;
#14785=CARTESIAN_POINT ( 'NONE',  ( 11.99999999999999822, 14.67089635893713684, 73.72996012237443608 ) ) ;
#14790=CARTESIAN_POINT ( 'NONE',  ( 0.000000000000000000, 0.000000000000000000, 0.000000000000000000 ) ) ;
#14791=DIRECTION ( 'NONE',  ( 0.000000000000000000, 0.6494480483301793283, 0.7604059656000345946 ) ) ;
#14792=CARTESIAN_POINT ( 'NONE',  ( 11.99999999999999822, 23.16143007188530589, -73.95703589263951017 ) ) ;
#14801=CIRCLE ( 'NONE', #42149, 31.99999999999998579 ) ;
#14802=AXIS2_PLACEMENT_3D ( 'NONE', #36663, #14407, #21972 ) ;
#14804=CARTESIAN_POINT ( 'NONE',  ( 15.00000000000000000, 16.83928648764922542, -16.46020748918050458 ) ) ;
#14806=ADVANCED_FACE ( 'NONE', ( #496 ), #37689, .T. ) ;
#14808=DIRECTION ( 'NONE',  ( -1.000000000000000000, 0.000000000000000000, 0.000000000000000000 ) ) ;
#14813=CIRCLE ( 'NONE', #28120, 31.99999999999998579 ) ;
#14815=CARTESIAN_POINT ( 'NONE',  ( 11.99999999999999822, 74.65491531819118620, 23.16904090965732621 ) ) ;
#14817=FACE_OUTER_BOUND ( 'NONE', #18364, .T. ) ;
#14824=VERTEX_POINT ( 'NONE', #24447 ) ;
#14830=ORIENTED_EDGE ( 'NONE', *, *, #2535, .T. ) ;
#14832=DIRECTION ( 'NONE',  ( 0.000000000000000000, 0.000000000000000000, 1.000000000000000000 ) ) ;
#14834=ORIENTED_EDGE ( 'NONE', *, *, #35756, .T. ) ;
#14843=CYLINDRICAL_SURFACE ( 'NONE', #11089, 82.00000000000000000 ) ;
#14851=CARTESIAN_POINT ( 'NONE',  ( 15.00000000000000000, -1.278221433540507546, -26.51162292216071492 ) ) ;
#14852=DIRECTION ( 'NONE',  ( -1.000000000000000000, -0.000000000000000000, -0.000000000000000000 ) ) ;
#14857=VERTEX_POINT ( 'NONE', #42584 ) ;
#14860=ORIENTED_EDGE ( 'NONE', *, *, #9626, .F. ) ;
#14871=DIRECTION ( 'NONE',  ( 0.000000000000000000, 0.000000000000000000, 1.000000000000000000 ) ) ;
#14882=AXIS2_PLACEMENT_3D ( 'NONE', #32765, #25910, #25659 ) ;
#14890=FACE_OUTER_BOUND ( 'NONE', #28591, .T. ) ;
#14895=FACE_OUTER_BOUND ( 'NONE', #16104, .T. ) ;
#14901=CARTESIAN_POINT ( 'NONE',  ( 11.99999999999999822, -73.72996012237429397, -14.67089635893794508 ) ) ;
#14904=EDGE_LOOP ( 'NONE', ( #20458, #34140, #41389, #35011 ) ) ;
#14909=ORIENTED_EDGE ( 'NONE', *, *, #16265, .F. ) ;
#14913=ORIENTED_EDGE ( 'NONE', *, *, #14500, .F. ) ;
#14917=FACE_OUTER_BOUND ( 'NONE', #43422, .T. ) ;
#14926=DIRECTION ( 'NONE',  ( -1.000000000000000000, -0.000000000000000000, 0.000000000000000000 ) ) ;
#14928=ORIENTED_EDGE ( 'NONE', *, *, #14528, .F. ) ;
#14929=EDGE_CURVE ( 'NONE', #20943, #46617, #32395, .T. ) ;
#14931=ORIENTED_EDGE ( 'NONE', *, *, #31617, .F. ) ;
#14932=AXIS2_PLACEMENT_3D ( 'NONE', #1320, #23339, #16254 ) ;
#14936=DIRECTION ( 'NONE',  ( 0.000000000000000000, 0.000000000000000000, -1.000000000000000000 ) ) ;
#14939=CARTESIAN_POINT ( 'NONE',  ( 11.99999999999999822, 0.000000000000000000, 0.000000000000000000 ) ) ;
#14940=FACE_OUTER_BOUND ( 'NONE', #48296, .T. ) ;
#14950=VERTEX_POINT ( 'NONE', #21967 ) ;
#14951=ORIENTED_EDGE ( 'NONE', *, *, #22001, .T. ) ;
#14957=VERTEX_POINT ( 'NONE', #17330 ) ;
#14959=CYLINDRICAL_SURFACE ( 'NONE', #40820, 77.49899999999999523 ) ;
#14961=CARTESIAN_POINT ( 'NONE',  ( 11.99999999999999822, 0.000000000000000000, 0.000000000000000000 ) ) ;
#14962=FACE_OUTER_BOUND ( 'NONE', #17919, .T. ) ;
#14968=ORIENTED_EDGE ( 'NONE', *, *, #44378, .F. ) ;
#14971=ORIENTED_EDGE ( 'NONE', *, *, #31300, .F. ) ;
#14983=CARTESIAN_POINT ( 'NONE',  ( 0.000000000000000000, -31.47745569255092235, -68.26794271651296242 ) ) ;
#14984=EDGE_CURVE ( 'NONE', #29567, #19983, #7355, .T. ) ;
#14986=LINE ( 'NONE', #14254, #1651 ) ;
#14992=CIRCLE ( 'NONE', #42334, 31.99999999999999289 ) ;
#14993=CYLINDRICAL_SURFACE ( 'NONE', #30303, 82.00000000000000000 ) ;
#14994=CARTESIAN_POINT ( 'NONE',  ( -10.00000000000000000, 0.000000000000000000, 0.000000000000000000 ) ) ;
#14995=AXIS2_PLACEMENT_3D ( 'NONE', #33548, #37704, #15207 ) ;
#14997=CARTESIAN_POINT ( 'NONE',  ( 0.000000000000000000, 74.65374052328648702, 8.840884882375350529 ) ) ;
#14998=LINE ( 'NONE', #15477, #31136 ) ;
#15002=ORIENTED_EDGE ( 'NONE', *, *, #38127, .F. ) ;
#15003=EDGE_CURVE ( 'NONE', #4790, #15507, #10483, .T. ) ;
#15004=DIRECTION ( 'NONE',  ( 0.000000000000000000, -0.4067366430758009854, -0.9135454576426004225 ) ) ;
#15007=ORIENTED_EDGE ( 'NONE', *, *, #43427, .T. ) ;
#15010=VECTOR ( 'NONE', #26440, 1000.000000000000000 ) ;
#15012=LINE ( 'NONE', #22585, #31560 ) ;
#15013=ORIENTED_EDGE ( 'NONE', *, *, #26432, .F. ) ;
#15018=CARTESIAN_POINT ( 'NONE',  ( 0.000000000000000000, 62.20884554314085335, -46.21855187248562657 ) ) ;
#15019=EDGE_LOOP ( 'NONE', ( #45410, #39618, #41334, #4086 ) ) ;
#15021=ORIENTED_EDGE ( 'NONE', *, *, #21041, .T. ) ;
#15022=EDGE_LOOP ( 'NONE', ( #32589, #46963, #38011, #39110 ) ) ;
#15026=CARTESIAN_POINT ( 'NONE',  ( 0.000000000000000000, 40.65526001592713357, -71.21200624218752750 ) ) ;
#15029=VERTEX_POINT ( 'NONE', #13683 ) ;
#15031=EDGE_CURVE ( 'NONE', #41319, #48218, #26937, .T. ) ;
#15034=FACE_OUTER_BOUND ( 'NONE', #40012, .T. ) ;
#15035=CYLINDRICAL_SURFACE ( 'NONE', #806, 31.99999999999999289 ) ;
#15042=DIRECTION ( 'NONE',  ( 1.000000000000000000, -0.000000000000000000, -0.000000000000000000 ) ) ;
#15056=CARTESIAN_POINT ( 'NONE',  ( 11.99999999999999822, -74.65491531819124305, 8.830959090342128448 ) ) ;
#15057=CIRCLE ( 'NONE', #28323, 31.99999999999998579 ) ;
#15059=VERTEX_POINT ( 'NONE', #7042 ) ;
#15064=ORIENTED_EDGE ( 'NONE', *, *, #20704, .T. ) ;
#15067=FACE_OUTER_BOUND ( 'NONE', #47853, .T. ) ;
#15075=ORIENTED_EDGE ( 'NONE', *, *, #45712, .T. ) ;
#15076=VERTEX_POINT ( 'NONE', #43771 ) ;
#15078=ORIENTED_EDGE ( 'NONE', *, *, #8301, .T. ) ;
#15084=ORIENTED_EDGE ( 'NONE', *, *, #43315, .T. ) ;
#15086=LINE ( 'NONE', #37355, #11490 ) ;
#15089=CARTESIAN_POINT ( 'NONE',  ( 0.000000000000000000, 39.47590169984846398, 71.87247863392427405 ) ) ;
#15091=DIRECTION ( 'NONE',  ( 0.000000000000000000, 0.000000000000000000, -1.000000000000000000 ) ) ;
#15093=CARTESIAN_POINT ( 'NONE',  ( 0.000000000000000000, 8.840884882376133902, -74.65374052328640175 ) ) ;
#15098=LINE ( 'NONE', #7748, #48035 ) ;
#15103=EDGE_CURVE ( 'NONE', #18715, #23803, #18322, .T. ) ;
#15106=EDGE_CURVE ( 'NONE', #20488, #35390, #24590, .T. ) ;
#15113=FACE_OUTER_BOUND ( 'NONE', #18735, .T. ) ;
#15114=CYLINDRICAL_SURFACE ( 'NONE', #7351, 31.99999999999998579 ) ;
#15115=ORIENTED_EDGE ( 'NONE', *, *, #43894, .F. ) ;
#15119=VECTOR ( 'NONE', #26100, 1000.000000000000000 ) ;
#15126=AXIS2_PLACEMENT_3D ( 'NONE', #9627, #39517, #13317 ) ;
#15127=VECTOR ( 'NONE', #29971, 1000.000000000000000 ) ;
#15129=LINE ( 'NONE', #30307, #6218 ) ;
#15130=DIRECTION ( 'NONE',  ( 0.000000000000000000, 0.000000000000000000, 1.000000000000000000 ) ) ;
#15133=EDGE_CURVE ( 'NONE', #41271, #29872, #30823, .T. ) ;
#15135=ADVANCED_FACE ( 'NONE', ( #26865 ), #41804, .T. ) ;
#15141=CARTESIAN_POINT ( 'NONE',  ( 12.00000000000000000, -23.29833615347104470, 3.418703333116808629 ) ) ;
#15144=VERTEX_POINT ( 'NONE', #432 ) ;
#15146=ORIENTED_EDGE ( 'NONE', *, *, #12385, .F. ) ;
#15150=DIRECTION ( 'NONE',  ( -1.000000000000000000, -0.000000000000000000, -0.000000000000000000 ) ) ;
#15151=ADVANCED_FACE ( 'NONE', ( #11692 ), #18776, .T. ) ;
#15154=EDGE_CURVE ( 'NONE', #8878, #18839, #5018, .T. ) ;
#15161=ORIENTED_EDGE ( 'NONE', *, *, #37646, .F. ) ;
#15164=CARTESIAN_POINT ( 'NONE',  ( 11.99999999999999822, -8.840884882374576037, -74.65374052328658649 ) ) ;
#15165=ORIENTED_EDGE ( 'NONE', *, *, #30528, .F. ) ;
#15166=AXIS2_PLACEMENT_3D ( 'NONE', #23004, #4168, #19082 ) ;
#15169=DIRECTION ( 'NONE',  ( -1.000000000000000000, 0.000000000000000000, 0.000000000000000000 ) ) ;
#15172=DIRECTION ( 'NONE',  ( 0.000000000000000000, 0.000000000000000000, 1.000000000000000000 ) ) ;
#15178=CYLINDRICAL_SURFACE ( 'NONE', #26192, 31.99999999999998579 ) ;
#15179=( NAMED_UNIT ( * ) SI_UNIT ( $, .STERADIAN. ) SOLID_ANGLE_UNIT ( ) );
#15182=ORIENTED_EDGE ( 'NONE', *, *, #23272, .T. ) ;
#15183=AXIS2_PLACEMENT_3D ( 'NONE', #46825, #20375, #9134 ) ;
#15185=VECTOR ( 'NONE', #42917, 1000.000000000000000 ) ;
#15186=VECTOR ( 'NONE', #20951, 1000.000000000000000 ) ;
#15191=EDGE_CURVE ( 'NONE', #13412, #44059, #4589, .T. ) ;
#15194=LINE ( 'NONE', #22528, #18764 ) ;
#15195=CIRCLE ( 'NONE', #333, 82.00000000000000000 ) ;
#15198=ORIENTED_EDGE ( 'NONE', *, *, #2359, .T. ) ;
#15200=VERTEX_POINT ( 'NONE', #37636 ) ;
#15201=CARTESIAN_POINT ( 'NONE',  ( 11.99999999999999822, 0.000000000000000000, 0.000000000000000000 ) ) ;
#15202=EDGE_CURVE ( 'NONE', #59, #40154, #15195, .T. ) ;
#15207=DIRECTION ( 'NONE',  ( 0.000000000000000000, -0.8090169943749401238, -0.5877852522924831291 ) ) ;
#15208=EDGE_LOOP ( 'NONE', ( #30003, #35653, #21075, #31037 ) ) ;
#15213=EDGE_CURVE ( 'NONE', #925, #20327, #42561, .T. ) ;
#15232=CARTESIAN_POINT ( 'NONE',  ( 11.99999999999999822, -76.66974797899830207, -11.30684508768420571 ) ) ;
#15233=CARTESIAN_POINT ( 'NONE',  ( 12.00000000000000000, 16.83928648764922542, -16.46020748918050458 ) ) ;
#15236=CIRCLE ( 'NONE', #33967, 77.49900000000000944 ) ;
#15239=CARTESIAN_POINT ( 'NONE',  ( 11.99999999999999822, -46.54456581323762521, -59.03342792756313884 ) ) ;
#15241=AXIS2_PLACEMENT_3D ( 'NONE', #35920, #5594, #17311 ) ;
#15242=AXIS2_PLACEMENT_3D ( 'NONE', #43898, #29687, #47555 ) ;
#15250=VERTEX_POINT ( 'NONE', #47089 ) ;
#15251=CARTESIAN_POINT ( 'NONE',  ( 11.99999999999999822, 0.000000000000000000, 0.000000000000000000 ) ) ;
#15252=ORIENTED_EDGE ( 'NONE', *, *, #12334, .F. ) ;
#15253=LINE ( 'NONE', #11084, #4129 ) ;
#15255=CARTESIAN_POINT ( 'NONE',  ( 11.99999999999999822, 44.88180994100466847, -63.18004540532978552 ) ) ;
#15268=LINE ( 'NONE', #30199, #12168 ) ;
#15271=AXIS2_PLACEMENT_3D ( 'NONE', #7318, #29361, #21997 ) ;
#15273=AXIS2_PLACEMENT_3D ( 'NONE', #23999, #1718, #9778 ) ;
#15277=CARTESIAN_POINT ( 'NONE',  ( 11.99999999999999822, -71.27951684758005513, -30.41916302227188851 ) ) ;
#15278=CARTESIAN_POINT ( 'NONE',  ( 11.99999999999999822, 54.21277698773675979, 55.38113227695801299 ) ) ;
#15281=EDGE_LOOP ( 'NONE', ( #35708, #3642, #33351, #8935 ) ) ;
#15286=CIRCLE ( 'NONE', #42645, 77.49899999999999523 ) ;
#15290=FACE_OUTER_BOUND ( 'NONE', #29027, .T. ) ;
#15292=CYLINDRICAL_SURFACE ( 'NONE', #9436, 31.99999999999998579 ) ;
#15294=EDGE_CURVE ( 'NONE', #21018, #3559, #12781, .T. ) ;
#15295=VECTOR ( 'NONE', #46111, 1000.000000000000000 ) ;
#15297=DIRECTION ( 'NONE',  ( 0.000000000000000000, 0.000000000000000000, -1.000000000000000000 ) ) ;
#15304=AXIS2_PLACEMENT_3D ( 'NONE', #12319, #23552, #4957 ) ;
#15308=ORIENTED_EDGE ( 'NONE', *, *, #16904, .F. ) ;
#15315=EDGE_CURVE ( 'NONE', #6863, #32670, #19017, .T. ) ;
#15316=CIRCLE ( 'NONE', #19210, 31.99999999999998934 ) ;
#15318=PLANE ( 'NONE',  #28898 ) ;
#15324=EDGE_CURVE ( 'NONE', #8980, #1474, #17445, .T. ) ;
#15326=CARTESIAN_POINT ( 'NONE',  ( 15.00000000000000000, -25.60904388321925040, -6.976881207771165272 ) ) ;
#15330=ORIENTED_EDGE ( 'NONE', *, *, #29006, .T. ) ;
#15331=VERTEX_POINT ( 'NONE', #12843 ) ;
#15333=ORIENTED_EDGE ( 'NONE', *, *, #18228, .F. ) ;
#15335=CARTESIAN_POINT ( 'NONE',  ( 11.99999999999999822, -68.26794271651286294, 31.47745569255117104 ) ) ;
#15339=EDGE_LOOP ( 'NONE', ( #2207, #22034, #2412, #27564 ) ) ;
#15342=CARTESIAN_POINT ( 'NONE',  ( 0.000000000000000000, 0.000000000000000000, 0.000000000000000000 ) ) ;
#15346=FACE_OUTER_BOUND ( 'NONE', #10192, .T. ) ;
#15356=ORIENTED_EDGE ( 'NONE', *, *, #47765, .F. ) ;
#15360=AXIS2_PLACEMENT_3D ( 'NONE', #40685, #25255, #7155 ) ;
#15362=CARTESIAN_POINT ( 'NONE',  ( 11.99999999999999822, -65.58780272294100655, 36.73666225445870737 ) ) ;
#15363=ADVANCED_FACE ( 'NONE', ( #5734 ), #2073, .T. ) ;
#15373=VERTEX_POINT ( 'NONE', #28245 ) ;
#15375=EDGE_CURVE ( 'NONE', #22938, #28248, #31671, .T. ) ;
#15376=VERTEX_POINT ( 'NONE', #3248 ) ;
#15383=ADVANCED_FACE ( 'NONE', ( #36550 ), #17935, .T. ) ;
#15389=DIRECTION ( 'NONE',  ( -1.000000000000000000, 0.000000000000000000, 0.000000000000000000 ) ) ;
#15395=EDGE_LOOP ( 'NONE', ( #17992, #15333, #32931, #22658 ) ) ;
#15396=DIRECTION ( 'NONE',  ( -1.000000000000000000, 0.000000000000000000, -0.000000000000000000 ) ) ;
#15398=CARTESIAN_POINT ( 'NONE',  ( 11.99999999999999822, 8.966570791701867549, -81.50828551894218776 ) ) ;
#15401=SURFACE_SIDE_STYLE ('',( #4134 ) ) ;
#15404=ORIENTED_EDGE ( 'NONE', *, *, #23074, .F. ) ;
#15405=ORIENTED_EDGE ( 'NONE', *, *, #41408, .F. ) ;
#15407=EDGE_LOOP ( 'NONE', ( #43068, #2039, #14676, #17249 ) ) ;
#15410=AXIS2_PLACEMENT_3D ( 'NONE', #17566, #9029, #38900 ) ;
#15413=LINE ( 'NONE', #11500, #21284 ) ;
#15417=CARTESIAN_POINT ( 'NONE',  ( 11.99999999999999822, -8.966570791700153364, -81.50828551894235829 ) ) ;
#15419=ADVANCED_FACE ( 'NONE', ( #29929 ), #33365, .T. ) ;
#15426=CARTESIAN_POINT ( 'NONE',  ( 0.000000000000000000, -78.73519480814938731, -22.90783923731713045 ) ) ;
#15431=EDGE_CURVE ( 'NONE', #31692, #3151, #18174, .T. ) ;
#15436=AXIS2_PLACEMENT_3D ( 'NONE', #16084, #7758, #23177 ) ;
#15437=EDGE_LOOP ( 'NONE', ( #36895, #11962, #46931, #19368 ) ) ;
#15439=EDGE_CURVE ( 'NONE', #20016, #21863, #7425, .T. ) ;
#15440=VERTEX_POINT ( 'NONE', #33599 ) ;
#15446=ORIENTED_EDGE ( 'NONE', *, *, #3937, .T. ) ;
#15447=CYLINDRICAL_SURFACE ( 'NONE', #2750, 77.49899999999999523 ) ;
#15454=FACE_OUTER_BOUND ( 'NONE', #48012, .T. ) ;
#15456=LINE ( 'NONE', #41401, #39695 ) ;
#15464=DIRECTION ( 'NONE',  ( -1.000000000000000000, -0.000000000000000000, -0.000000000000000000 ) ) ;
#15465=CARTESIAN_POINT ( 'NONE',  ( 0.000000000000000000, 39.78640506895698081, -66.50666863321957578 ) ) ;
#15468=CARTESIAN_POINT ( 'NONE',  ( 11.99999999999999822, -77.32052557432837148, -5.256550761633681290 ) ) ;
#15469=EDGE_CURVE ( 'NONE', #38129, #44062, #43364, .T. ) ;
#15470=CARTESIAN_POINT ( 'NONE',  ( 12.00000000000000000, -18.13022148937262656, -15.02647892043543898 ) ) ;
#15471=PLANE ( 'NONE',  #14674 ) ;
#15474=CIRCLE ( 'NONE', #23320, 82.00000000000000000 ) ;
#15477=CARTESIAN_POINT ( 'NONE',  ( 11.99999999999999822, 11.30684508768450769, -76.66974797899825944 ) ) ;
#15478=CARTESIAN_POINT ( 'NONE',  ( 11.99999999999999822, 0.000000000000000000, 0.000000000000000000 ) ) ;
#15479=EDGE_CURVE ( 'NONE', #27749, #33199, #15012, .T. ) ;
#15483=DIRECTION ( 'NONE',  ( -1.000000000000000000, -0.000000000000000000, -0.000000000000000000 ) ) ;
#15488=ADVANCED_FACE ( 'NONE', ( #26010 ), #14770, .T. ) ;
#15493=ADVANCED_FACE ( 'NONE', ( #40240 ), #44619, .F. ) ;
#15495=DIRECTION ( 'NONE',  ( 0.000000000000000000, 0.000000000000000000, -1.000000000000000000 ) ) ;
#15498=DIRECTION ( 'NONE',  ( 1.000000000000000000, 0.000000000000000000, -0.000000000000000000 ) ) ;
#15501=CIRCLE ( 'NONE', #1460, 31.99999999999998934 ) ;
#15505=DIRECTION ( 'NONE',  ( -1.000000000000000000, 0.000000000000000000, 0.000000000000000000 ) ) ;
#15506=DIRECTION ( 'NONE',  ( -1.000000000000000000, 0.000000000000000000, 0.000000000000000000 ) ) ;
#15507=VERTEX_POINT ( 'NONE', #23543 ) ;
#15514=CARTESIAN_POINT ( 'NONE',  ( 11.99999999999999822, 24.73286445877705475, 73.44644590900068692 ) ) ;
#15515=ORIENTED_EDGE ( 'NONE', *, *, #31312, .T. ) ;
#15518=DIRECTION ( 'NONE',  ( -1.000000000000000000, 0.000000000000000000, 0.000000000000000000 ) ) ;
#15520=DIRECTION ( 'NONE',  ( -1.000000000000000000, 0.000000000000000000, -0.000000000000000000 ) ) ;
#15527=FACE_OUTER_BOUND ( 'NONE', #42038, .T. ) ;
#15529=EDGE_CURVE ( 'NONE', #35660, #12921, #37090, .T. ) ;
#15530=DIRECTION ( 'NONE',  ( 0.000000000000000000, 0.5877852522924684742, 0.8090169943749507819 ) ) ;
#15531=CARTESIAN_POINT ( 'NONE',  ( 11.99999999999999822, -20.40083707022829174, -72.35432306680507963 ) ) ;
#15545=EDGE_LOOP ( 'NONE', ( #43179, #41213, #10941, #17481 ) ) ;
#15548=LINE ( 'NONE', #4539, #37466 ) ;
#15549=CYLINDRICAL_SURFACE ( 'NONE', #48021, 77.49899999999999523 ) ;
#15552=CARTESIAN_POINT ( 'NONE',  ( 11.99999999999999822, 70.52718814184294160, -26.02418014898236720 ) ) ;
#15554=ORIENTED_EDGE ( 'NONE', *, *, #16234, .F. ) ;
#15556=CARTESIAN_POINT ( 'NONE',  ( 11.99999999999999822, 41.76937507738875155, -62.50329211542393892 ) ) ;
#15558=ORIENTED_EDGE ( 'NONE', *, *, #37565, .T. ) ;
#15562=EDGE_LOOP ( 'NONE', ( #33152, #28119, #47133, #8018 ) ) ;
#15566=CYLINDRICAL_SURFACE ( 'NONE', #18235, 31.99999999999997868 ) ;
#15568=DIRECTION ( 'NONE',  ( -1.000000000000000000, -0.000000000000000000, 0.000000000000000000 ) ) ;
#15570=CIRCLE ( 'NONE', #6176, 77.49899999999999523 ) ;
#15572=CYLINDRICAL_SURFACE ( 'NONE', #1676, 31.99999999999998579 ) ;
#15573=CARTESIAN_POINT ( 'NONE',  ( 11.99999999999999822, 0.000000000000000000, 0.000000000000000000 ) ) ;
#15574=EDGE_LOOP ( 'NONE', ( #42614, #5089, #19249, #17041 ) ) ;
#15580=ADVANCED_FACE ( 'NONE', ( #16224 ), #45844, .T. ) ;
#15583=DIRECTION ( 'NONE',  ( -1.000000000000000000, 0.000000000000000000, -0.000000000000000000 ) ) ;
#15584=EDGE_CURVE ( 'NONE', #29716, #36977, #41022, .T. ) ;
#15588=EDGE_CURVE ( 'NONE', #44874, #40000, #787, .T. ) ;
#15590=DIRECTION ( 'NONE',  ( 0.000000000000000000, 0.000000000000000000, 1.000000000000000000 ) ) ;
#15591=ADVANCED_FACE ( 'NONE', ( #304 ), #45111, .T. ) ;
#15595=ORIENTED_EDGE ( 'NONE', *, *, #16223, .T. ) ;
#15597=VERTEX_POINT ( 'NONE', #7891 ) ;
#15598=VECTOR ( 'NONE', #17276, 1000.000000000000000 ) ;
#15605=EDGE_CURVE ( 'NONE', #19547, #48421, #5677, .T. ) ;
#15614=EDGE_LOOP ( 'NONE', ( #16118, #9536, #8798, #48443 ) ) ;
#15616=LINE ( 'NONE', #30543, #41151 ) ;
#15631=DIRECTION ( 'NONE',  ( -0.000000000000000000, 0.2079116908177663092, 0.9781476007338041345 ) ) ;
#15638=EDGE_CURVE ( 'NONE', #31411, #17439, #47191, .T. ) ;
#15639=LINE ( 'NONE', #4867, #47148 ) ;
#15640=CARTESIAN_POINT ( 'NONE',  ( 11.99999999999999822, -20.41045688087772092, -72.35160999960838524 ) ) ;
#15645=AXIS2_PLACEMENT_3D ( 'NONE', #1543, #24064, #6180 ) ;
#15654=CARTESIAN_POINT ( 'NONE',  ( 0.000000000000000000, 0.000000000000000000, 0.000000000000000000 ) ) ;
#15661=AXIS2_PLACEMENT_3D ( 'NONE', #32196, #47112, #28523 ) ;
#15671=VERTEX_POINT ( 'NONE', #17159 ) ;
#15674=DIRECTION ( 'NONE',  ( -1.000000000000000000, 0.000000000000000000, 0.000000000000000000 ) ) ;
#15675=ORIENTED_EDGE ( 'NONE', *, *, #47127, .F. ) ;
#15676=CARTESIAN_POINT ( 'NONE',  ( 11.99999999999999822, 63.18004540533030422, 44.88180994100399346 ) ) ;
#15677=DIRECTION ( 'NONE',  ( 0.000000000000000000, 0.000000000000000000, 1.000000000000000000 ) ) ;
#15683=DIRECTION ( 'NONE',  ( 0.000000000000000000, 0.000000000000000000, -1.000000000000000000 ) ) ;
#15689=DIRECTION ( 'NONE',  ( -1.000000000000000000, -0.000000000000000000, -0.000000000000000000 ) ) ;
#15691=ORIENTED_EDGE ( 'NONE', *, *, #44235, .F. ) ;
#15695=EDGE_CURVE ( 'NONE', #47223, #5925, #27660, .T. ) ;
#15697=CARTESIAN_POINT ( 'NONE',  ( 11.99999999999999822, 2.946379043147425492, -75.11764819372145041 ) ) ;
#15700=ORIENTED_EDGE ( 'NONE', *, *, #27223, .F. ) ;
#15701=DIRECTION ( 'NONE',  ( -1.000000000000000000, 0.000000000000000000, 0.000000000000000000 ) ) ;
#15706=AXIS2_PLACEMENT_3D ( 'NONE', #17909, #10326, #47760 ) ;
#15707=AXIS2_PLACEMENT_3D ( 'NONE', #11223, #34209, #22241 ) ;
#15711=CARTESIAN_POINT ( 'NONE',  ( 0.000000000000000000, 65.58780272294076497, 36.73666225445916211 ) ) ;
#15716=DIRECTION ( 'NONE',  ( -1.000000000000000000, 0.000000000000000000, -0.000000000000000000 ) ) ;
#15717=VECTOR ( 'NONE', #38391, 1000.000000000000000 ) ;
#15724=EDGE_CURVE ( 'NONE', #29983, #17937, #38607, .T. ) ;
#15728=ADVANCED_FACE ( 'NONE', ( #16935 ), #24518, .T. ) ;
#15730=VECTOR ( 'NONE', #34380, 1000.000000000000227 ) ;
#15732=DIRECTION ( 'NONE',  ( -1.000000000000000000, -0.000000000000000000, -0.000000000000000000 ) ) ;
#15740=DIRECTION ( 'NONE',  ( -1.000000000000000000, 0.000000000000000000, -0.000000000000000000 ) ) ;
#15741=AXIS2_PLACEMENT_3D ( 'NONE', #45257, #10765, #3657 ) ;
#15744=ORIENTED_EDGE ( 'NONE', *, *, #13798, .F. ) ;
#15745=DIRECTION ( 'NONE',  ( -1.000000000000000000, 0.000000000000000000, 0.000000000000000000 ) ) ;
#15761=DIRECTION ( 'NONE',  ( -1.000000000000000000, -0.000000000000000000, 0.000000000000000000 ) ) ;
#15763=FACE_OUTER_BOUND ( 'NONE', #35101, .T. ) ;
#15764=DIRECTION ( 'NONE',  ( -1.000000000000000000, 0.000000000000000000, -0.000000000000000000 ) ) ;
#15768=DIRECTION ( 'NONE',  ( -0.000000000000000000, 0.1045284632676569680, 0.9945218953682730678 ) ) ;
#15769=EDGE_LOOP ( 'NONE', ( #16833, #40874, #41748, #38443 ) ) ;
#15770=DIRECTION ( 'NONE',  ( -1.000000000000000000, 0.000000000000000000, 0.000000000000000000 ) ) ;
#15773=EDGE_LOOP ( 'NONE', ( #17259, #2831, #12833, #1584 ) ) ;
#15777=VERTEX_POINT ( 'NONE', #18368 ) ;
#15782=AXIS2_PLACEMENT_3D ( 'NONE', #24671, #39617, #6078 ) ;
#15783=VERTEX_POINT ( 'NONE', #33301 ) ;
#15784=EDGE_LOOP ( 'NONE', ( #18567, #24826, #23410, #1679 ) ) ;
#15786=ORIENTED_EDGE ( 'NONE', *, *, #5867, .T. ) ;
#15788=ORIENTED_EDGE ( 'NONE', *, *, #31749, .F. ) ;
#15789=ORIENTED_EDGE ( 'NONE', *, *, #27886, .F. ) ;
#15795=VERTEX_POINT ( 'NONE', #47983 ) ;
#15796=DIRECTION ( 'NONE',  ( -1.000000000000000000, 0.000000000000000000, 0.000000000000000000 ) ) ;
#15802=AXIS2_PLACEMENT_3D ( 'NONE', #3781, #18702, #33633 ) ;
#15803=VERTEX_POINT ( 'NONE', #7357 ) ;
#15807=CIRCLE ( 'NONE', #23623, 77.49900000000000944 ) ;
#15808=CARTESIAN_POINT ( 'NONE',  ( 0.000000000000000000, 51.02545421589402252, -55.20638768913705263 ) ) ;
#15809=DIRECTION ( 'NONE',  ( 0.000000000000000000, 0.000000000000000000, 1.000000000000000000 ) ) ;
#15811=DIRECTION ( 'NONE',  ( 0.000000000000000000, -0.2334453638559126909, 0.9723699203976748917 ) ) ;
#15850=VECTOR ( 'NONE', #10356, 1000.000000000000000 ) ;
#15852=ADVANCED_FACE ( 'NONE', ( #17876 ), #14219, .T. ) ;
#15853=ORIENTED_EDGE ( 'NONE', *, *, #44791, .T. ) ;
#15857=DIRECTION ( 'NONE',  ( 0.000000000000000000, 0.5224985647159441360, 0.8526401643540952868 ) ) ;
#15860=EDGE_LOOP ( 'NONE', ( #3460, #42962, #30005, #35316 ) ) ;
#15861=DIRECTION ( 'NONE',  ( -1.000000000000000000, 0.000000000000000000, 0.000000000000000000 ) ) ;
#15864=VERTEX_POINT ( 'NONE', #39630 ) ;
#15868=DIRECTION ( 'NONE',  ( 0.000000000000000000, 0.000000000000000000, 1.000000000000000000 ) ) ;
#15870=FACE_OUTER_BOUND ( 'NONE', #13821, .T. ) ;
#15876=CIRCLE ( 'NONE', #14295, 31.99999999999998224 ) ;
#15878=EDGE_CURVE ( 'NONE', #35390, #33288, #44071, .T. ) ;
#15882=VECTOR ( 'NONE', #14123, 1000.000000000000000 ) ;
#15883=FACE_OUTER_BOUND ( 'NONE', #38032, .T. ) ;
#15887=AXIS2_PLACEMENT_3D ( 'NONE', #21721, #28338, #29062 ) ;
#15898=UNCERTAINTY_MEASURE_WITH_UNIT (LENGTH_MEASURE( 1.000000000000000082E-05 ), #23466, 'distance_accuracy_value', 'NONE');
#15902=DIRECTION ( 'NONE',  ( 0.000000000000000000, 0.000000000000000000, 1.000000000000000000 ) ) ;
#15903=EDGE_LOOP ( 'NONE', ( #172, #45559, #27855, #32802 ) ) ;
#15906=DIRECTION ( 'NONE',  ( -1.000000000000000000, 0.000000000000000000, -0.000000000000000000 ) ) ;
#15910=ORIENTED_EDGE ( 'NONE', *, *, #22674, .F. ) ;
#15911=ORIENTED_EDGE ( 'NONE', *, *, #6427, .F. ) ;
#15913=ORIENTED_EDGE ( 'NONE', *, *, #34315, .F. ) ;
#15914=ORIENTED_EDGE ( 'NONE', *, *, #27750, .F. ) ;
#15915=ORIENTED_EDGE ( 'NONE', *, *, #27879, .F. ) ;
#15931=VERTEX_POINT ( 'NONE', #32515 ) ;
#15938=VERTEX_POINT ( 'NONE', #40096 ) ;
#15943=DIRECTION ( 'NONE',  ( 0.000000000000000000, 0.9238795325112851842, 0.3826834323650937786 ) ) ;
#15944=CYLINDRICAL_SURFACE ( 'NONE', #44042, 31.99999999999998579 ) ;
#15959=CARTESIAN_POINT ( 'NONE',  ( 11.99999999999999822, 11.30684508768339569, 76.66974797899841576 ) ) ;
#15960=DIRECTION ( 'NONE',  ( 0.000000000000000000, -0.9876883405951359940, -0.1564344650402420545 ) ) ;
#15962=ORIENTED_EDGE ( 'NONE', *, *, #22166, .T. ) ;
#15964=FACE_BOUND ( 'NONE', #4667, .T. ) ;
#15965=AXIS2_PLACEMENT_3D ( 'NONE', #42928, #43644, #10110 ) ;
#15968=DIRECTION ( 'NONE',  ( 1.000000000000000000, -0.000000000000000000, 0.000000000000000000 ) ) ;
#15971=CARTESIAN_POINT ( 'NONE',  ( 11.99999999999999822, 55.19960302592066625, 51.03279382321107249 ) ) ;
#15977=AXIS2_PLACEMENT_3D ( 'NONE', #13003, #9310, #22000 ) ;
#15986=VERTEX_POINT ( 'NONE', #9501 ) ;
#15988=DIRECTION ( 'NONE',  ( -1.000000000000000000, 0.000000000000000000, -0.000000000000000000 ) ) ;
#15989=DIRECTION ( 'NONE',  ( -1.000000000000000000, 0.000000000000000000, -0.000000000000000000 ) ) ;
#15990=DIRECTION ( 'NONE',  ( 0.000000000000000000, 0.000000000000000000, -1.000000000000000000 ) ) ;
#15991=ORIENTED_EDGE ( 'NONE', *, *, #13064, .F. ) ;
#15993=VECTOR ( 'NONE', #2452, 1000.000000000000000 ) ;
#16000=AXIS2_PLACEMENT_3D ( 'NONE', #558, #8608, #19617 ) ;
#16005=CARTESIAN_POINT ( 'NONE',  ( 0.000000000000000000, -68.67312586195022561, 35.91791733033451806 ) ) ;
#16007=CARTESIAN_POINT ( 'NONE',  ( 11.99999999999999822, 0.000000000000000000, 0.000000000000000000 ) ) ;
#16010=DIRECTION ( 'NONE',  ( -1.000000000000000000, 0.000000000000000000, 0.000000000000000000 ) ) ;
#16017=ORIENTED_EDGE ( 'NONE', *, *, #33044, .T. ) ;
#16018=EDGE_LOOP ( 'NONE', ( #19478, #28689, #3991, #34497 ) ) ;
#16023=ORIENTED_EDGE ( 'NONE', *, *, #26424, .F. ) ;
#16025=VECTOR ( 'NONE', #19179, 1000.000000000000000 ) ;
#16034=ADVANCED_FACE ( 'NONE', ( #25872 ), #15114, .T. ) ;
#16038=AXIS2_PLACEMENT_3D ( 'NONE', #32588, #29410, #44568 ) ;
#16040=CYLINDRICAL_SURFACE ( 'NONE', #42581, 77.49899999999999523 ) ;
#16046=ADVANCED_FACE ( 'NONE', ( #47901 ), #7272, .T. ) ;
#16052=CIRCLE ( 'NONE', #4359, 31.99999999999998579 ) ;
#16058=AXIS2_PLACEMENT_3D ( 'NONE', #37726, #26, #3959 ) ;
#16060=FACE_OUTER_BOUND ( 'NONE', #13356, .T. ) ;
#16063=LINE ( 'NONE', #37601, #21973 ) ;
#16076=AXIS2_PLACEMENT_3D ( 'NONE', #41471, #33158, #591 ) ;
#16078=DIRECTION ( 'NONE',  ( 0.000000000000000000, 0.3090169943749461745, -0.9510565162951539753 ) ) ;
#16079=CARTESIAN_POINT ( 'NONE',  ( 0.000000000000000000, 77.19088730480532945, -6.903761155836932062 ) ) ;
#16080=AXIS2_PLACEMENT_3D ( 'NONE', #11898, #8220, #23151 ) ;
#16081=CIRCLE ( 'NONE', #43435, 31.99999999999998579 ) ;
#16084=CARTESIAN_POINT ( 'NONE',  ( 0.000000000000000000, 46.53671651293948486, 59.03961581697416250 ) ) ;
#16087=EDGE_CURVE ( 'NONE', #31329, #2031, #35480, .T. ) ;
#16096=CARTESIAN_POINT ( 'NONE',  ( 0.000000000000000000, -22.90783923731575200, -78.73519480814978522 ) ) ;
#16102=EDGE_CURVE ( 'NONE', #25704, #12511, #25391, .T. ) ;
#16104=EDGE_LOOP ( 'NONE', ( #2293, #38837, #7477, #35632 ) ) ;
#16106=CARTESIAN_POINT ( 'NONE',  ( 11.99999999999999822, 75.11764819372149304, -2.946379043146603482 ) ) ;
#16107=DIRECTION ( 'NONE',  ( 0.000000000000000000, 0.1564344650402244019, 0.9876883405951387696 ) ) ;
#16110=AXIS2_PLACEMENT_3D ( 'NONE', #29661, #22802, #32839 ) ;
#16116=VERTEX_POINT ( 'NONE', #40349 ) ;
#16118=ORIENTED_EDGE ( 'NONE', *, *, #39202, .T. ) ;
#16120=CARTESIAN_POINT ( 'NONE',  ( 15.00000000000000000, 22.07842321921480888, -8.187992925817425771 ) ) ;
#16123=CARTESIAN_POINT ( 'NONE',  ( 11.99999999999999822, -81.96053171279903893, 2.543863470248101333 ) ) ;
#16124=CARTESIAN_POINT ( 'NONE',  ( 11.99999999999999822, -46.11716303203136391, -67.80270845531939017 ) ) ;
#16125=ORIENTED_EDGE ( 'NONE', *, *, #33918, .F. ) ;
#16127=CARTESIAN_POINT ( 'NONE',  ( 11.99999999999999822, 0.000000000000000000, 0.000000000000000000 ) ) ;
#16129=DIRECTION ( 'NONE',  ( 0.000000000000000000, 0.6691306063588661202, 0.7431448254773871387 ) ) ;
#16130=AXIS2_PLACEMENT_3D ( 'NONE', #33408, #10660, #43937 ) ;
#16131=ORIENTED_EDGE ( 'NONE', *, *, #11398, .F. ) ;
#16132=DIRECTION ( 'NONE',  ( -1.000000000000000000, -0.000000000000000000, -0.000000000000000000 ) ) ;
#16135=ORIENTED_EDGE ( 'NONE', *, *, #27683, .T. ) ;
#16137=VERTEX_POINT ( 'NONE', #3801 ) ;
#16140=DIRECTION ( 'NONE',  ( -1.000000000000000000, -0.000000000000000000, -0.000000000000000000 ) ) ;
#16141=CARTESIAN_POINT ( 'NONE',  ( 11.99999999999999822, -0.8261519478436571973, 77.49459641780886443 ) ) ;
#16142=CARTESIAN_POINT ( 'NONE',  ( 11.99999999999999822, -73.72996012237429397, -14.67089635893794508 ) ) ;
#16143=DIRECTION ( 'NONE',  ( -1.000000000000000000, -0.000000000000000000, 0.000000000000000000 ) ) ;
#16146=FACE_OUTER_BOUND ( 'NONE', #45174, .T. ) ;
#16147=EDGE_CURVE ( 'NONE', #39227, #28808, #19853, .T. ) ;
#16156=CIRCLE ( 'NONE', #5994, 82.00000000000000000 ) ;
#16158=ORIENTED_EDGE ( 'NONE', *, *, #18157, .T. ) ;
#16161=AXIS2_PLACEMENT_3D ( 'NONE', #23179, #26375, #15590 ) ;
#16163=EDGE_CURVE ( 'NONE', #19053, #13639, #4259, .T. ) ;
#16168=ORIENTED_EDGE ( 'NONE', *, *, #38852, .F. ) ;
#16171=DIRECTION ( 'NONE',  ( 1.000000000000000000, 0.000000000000000000, 0.000000000000000000 ) ) ;
#16176=AXIS2_PLACEMENT_3D ( 'NONE', #39853, #24913, #13419 ) ;
#16184=ORIENTED_EDGE ( 'NONE', *, *, #39138, .T. ) ;
#16185=VECTOR ( 'NONE', #9612, 1000.000000000000000 ) ;
#16187=ORIENTED_EDGE ( 'NONE', *, *, #16686, .F. ) ;
#16200=CARTESIAN_POINT ( 'NONE',  ( 15.00000000000000000, -11.95096189432345746, -23.69967320028757030 ) ) ;
#16202=EDGE_CURVE ( 'NONE', #48350, #6120, #37866, .T. ) ;
#16205=CARTESIAN_POINT ( 'NONE',  ( 0.000000000000000000, 46.54456581323805153, 59.03342792756280488 ) ) ;
#16206=DIRECTION ( 'NONE',  ( -1.000000000000000000, 0.000000000000000000, 0.000000000000000000 ) ) ;
#16207=ADVANCED_FACE ( 'NONE', ( #27594 ), #33541, .T. ) ;
#16210=ORIENTED_EDGE ( 'NONE', *, *, #9448, .F. ) ;
#16214=EDGE_CURVE ( 'NONE', #40594, #15144, #26212, .T. ) ;
#16223=EDGE_CURVE ( 'NONE', #22722, #28723, #11276, .T. ) ;
#16224=FACE_OUTER_BOUND ( 'NONE', #13883, .T. ) ;
#16225=ORIENTED_EDGE ( 'NONE', *, *, #15724, .F. ) ;
#16227=EDGE_CURVE ( 'NONE', #13807, #21898, #22970, .T. ) ;
#16230=VERTEX_POINT ( 'NONE', #44559 ) ;
#16231=CARTESIAN_POINT ( 'NONE',  ( 15.00000000000000000, -10.45096189432344502, -21.10159698893425784 ) ) ;
#16234=EDGE_CURVE ( 'NONE', #33766, #9506, #23673, .T. ) ;
#16237=DIRECTION ( 'NONE',  ( 1.000000000000000000, 0.000000000000000000, -0.000000000000000000 ) ) ;
#16240=AXIS2_PLACEMENT_3D ( 'NONE', #8345, #23278, #33791 ) ;
#16242=VERTEX_POINT ( 'NONE', #8495 ) ;
#16252=DIRECTION ( 'NONE',  ( -1.000000000000000000, -0.000000000000000000, 0.000000000000000000 ) ) ;
#16254=DIRECTION ( 'NONE',  ( 0.000000000000000000, 0.000000000000000000, 1.000000000000000000 ) ) ;
#16258=AXIS2_PLACEMENT_3D ( 'NONE', #19480, #45695, #8713 ) ;
#16259=LINE ( 'NONE', #45616, #14472 ) ;
#16260=CARTESIAN_POINT ( 'NONE',  ( 0.000000000000000000, -24.73286445877757345, 73.44644590900053061 ) ) ;
#16261=DIRECTION ( 'NONE',  ( 0.000000000000000000, 0.000000000000000000, 1.000000000000000000 ) ) ;
#16262=EDGE_CURVE ( 'NONE', #46617, #9384, #37048, .T. ) ;
#16264=FACE_OUTER_BOUND ( 'NONE', #24418, .T. ) ;
#16265=EDGE_CURVE ( 'NONE', #37023, #23034, #35889, .T. ) ;
#16267=VECTOR ( 'NONE', #37444, 1000.000000000000227 ) ;
#16268=VERTEX_POINT ( 'NONE', #20733 ) ;
#16271=ORIENTED_EDGE ( 'NONE', *, *, #24823, .T. ) ;
#16273=CARTESIAN_POINT ( 'NONE',  ( 0.000000000000000000, 0.000000000000000000, 0.000000000000000000 ) ) ;
#16275=ORIENTED_EDGE ( 'NONE', *, *, #16227, .F. ) ;
#16276=VECTOR ( 'NONE', #3232, 1000.000000000000000 ) ;
#16280=CARTESIAN_POINT ( 'NONE',  ( 11.99999999999999822, 2.946379043146343246, 75.11764819372150725 ) ) ;
#16285=ORIENTED_EDGE ( 'NONE', *, *, #4685, .T. ) ;
#16289=DIRECTION ( 'NONE',  ( 0.000000000000000000, -0.7431448254773862505, 0.6691306063588672304 ) ) ;
#16295=ORIENTED_EDGE ( 'NONE', *, *, #30622, .T. ) ;
#16312=DIRECTION ( 'NONE',  ( -1.000000000000000000, 0.000000000000000000, 0.000000000000000000 ) ) ;
#16313=ADVANCED_FACE ( 'NONE', ( #42772 ), #13624, .F. ) ;
#16320=EDGE_LOOP ( 'NONE', ( #14733, #44083, #36982, #7497 ) ) ;
#16324=DIRECTION ( 'NONE',  ( 0.000000000000000000, 0.000000000000000000, 1.000000000000000000 ) ) ;
#16325=LINE ( 'NONE', #27339, #30770 ) ;
#16328=ORIENTED_EDGE ( 'NONE', *, *, #17008, .F. ) ;
#16335=CIRCLE ( 'NONE', #38215, 82.00000000000000000 ) ;
#16338=AXIS2_PLACEMENT_3D ( 'NONE', #18994, #8237, #23168 ) ;
#16343=DIRECTION ( 'NONE',  ( -1.000000000000000000, 0.000000000000000000, 0.000000000000000000 ) ) ;
#16344=EDGE_CURVE ( 'NONE', #1582, #7124, #28561, .T. ) ;
#16346=ORIENTED_EDGE ( 'NONE', *, *, #27366, .F. ) ;
#16352=EDGE_CURVE ( 'NONE', #43548, #47535, #31525, .T. ) ;
#16356=CYLINDRICAL_SURFACE ( 'NONE', #17393, 77.49899999999999523 ) ;
#16357=EDGE_CURVE ( 'NONE', #21831, #37286, #11323, .T. ) ;
#16360=CARTESIAN_POINT ( 'NONE',  ( 11.99999999999999822, -77.49459641780886443, -0.8261519478439277586 ) ) ;
#16364=VERTEX_POINT ( 'NONE', #40055 ) ;
#16367=CARTESIAN_POINT ( 'NONE',  ( -10.00000000000000000, 0.000000000000000000, 0.000000000000000000 ) ) ;
#16369=ADVANCED_FACE ( 'NONE', ( #13384 ), #16823, .T. ) ;
#16371=DIRECTION ( 'NONE',  ( -1.000000000000000000, 0.000000000000000000, -0.000000000000000000 ) ) ;
#16373=VECTOR ( 'NONE', #16422, 1000.000000000000000 ) ;
#16384=CARTESIAN_POINT ( 'NONE',  ( 11.99999999999999822, 68.26794271651307611, -31.47745569255064169 ) ) ;
#16386=ORIENTED_EDGE ( 'NONE', *, *, #26424, .T. ) ;
#16391=ORIENTED_EDGE ( 'NONE', *, *, #48145, .T. ) ;
#16392=VERTEX_POINT ( 'NONE', #5556 ) ;
#16397=AXIS2_PLACEMENT_3D ( 'NONE', #16991, #41991, #46861 ) ;
#16398=ORIENTED_EDGE ( 'NONE', *, *, #20842, .T. ) ;
#16407=ORIENTED_EDGE ( 'NONE', *, *, #36234, .F. ) ;
#16408=VECTOR ( 'NONE', #26355, 1000.000000000000000 ) ;
#16409=CARTESIAN_POINT ( 'NONE',  ( 0.000000000000000000, 0.000000000000000000, 0.000000000000000000 ) ) ;
#16411=DIRECTION ( 'NONE',  ( -1.000000000000000000, -0.000000000000000000, -0.000000000000000000 ) ) ;
#16417=LINE ( 'NONE', #46279, #8788 ) ;
#16418=LINE ( 'NONE', #45304, #9084 ) ;
#16419=LINE ( 'NONE', #12514, #31650 ) ;
#16421=LINE ( 'NONE', #31369, #5763 ) ;
#16422=DIRECTION ( 'NONE',  ( -1.000000000000000000, -0.000000000000000000, 0.000000000000000000 ) ) ;
#16427=ORIENTED_EDGE ( 'NONE', *, *, #11999, .F. ) ;
#16429=CARTESIAN_POINT ( 'NONE',  ( 15.00000000000000000, 6.762365576493647445, 25.66652317338391498 ) ) ;
#16431=CARTESIAN_POINT ( 'NONE',  ( 11.99999999999999822, 2.543863470248389103, 81.96053171279902472 ) ) ;
#16433=DIRECTION ( 'NONE',  ( -1.000000000000000000, -0.000000000000000000, -0.000000000000000000 ) ) ;
#16438=CARTESIAN_POINT ( 'NONE',  ( 11.99999999999999822, 59.03342792756328095, -46.54456581323744757 ) ) ;
#16444=DIRECTION ( 'NONE',  ( -1.000000000000000000, -0.000000000000000000, 0.000000000000000000 ) ) ;
#16446=AXIS2_PLACEMENT_3D ( 'NONE', #8859, #5439, #35048 ) ;
#16449=DIRECTION ( 'NONE',  ( 0.000000000000000000, -6.938893903907231533E-15, 1.000000000000000000 ) ) ;
#16451=LINE ( 'NONE', #31400, #42221 ) ;
#16452=CARTESIAN_POINT ( 'NONE',  ( 0.000000000000000000, 0.000000000000000000, 0.000000000000000000 ) ) ;
#16461=DIRECTION ( 'NONE',  ( -1.000000000000000000, -0.000000000000000000, 0.000000000000000000 ) ) ;
#16471=ORIENTED_EDGE ( 'NONE', *, *, #33237, .T. ) ;
#16476=ORIENTED_EDGE ( 'NONE', *, *, #17990, .T. ) ;
#16478=DIRECTION ( 'NONE',  ( 0.000000000000000000, -0.7071067811865535679, 0.7071067811865414665 ) ) ;
#16480=CYLINDRICAL_SURFACE ( 'NONE', #839, 82.00000000000000000 ) ;
#16483=DIRECTION ( 'NONE',  ( -1.000000000000000000, 0.000000000000000000, -0.000000000000000000 ) ) ;
#16485=CARTESIAN_POINT ( 'NONE',  ( 0.000000000000000000, 0.000000000000000000, 0.000000000000000000 ) ) ;
#16489=DIRECTION ( 'NONE',  ( -1.000000000000000000, 0.000000000000000000, 0.000000000000000000 ) ) ;
#16490=VECTOR ( 'NONE', #29051, 1000.000000000000000 ) ;
#16491=CARTESIAN_POINT ( 'NONE',  ( 0.000000000000000000, 69.42325613327489009, -34.44570377933524696 ) ) ;
#16494=DIRECTION ( 'NONE',  ( 0.000000000000000000, -0.9510565162951499785, -0.3090169943749582204 ) ) ;
#16505=ADVANCED_FACE ( 'NONE', ( #36607 ), #11417, .T. ) ;
#16512=DIRECTION ( 'NONE',  ( 0.000000000000000000, -0.9510565162951544194, -0.3090169943749450643 ) ) ;
#16516=DIRECTION ( 'NONE',  ( 0.000000000000000000, -0.9876883405951359940, -0.1564344650402420545 ) ) ;
#16517=VERTEX_POINT ( 'NONE', #43959 ) ;
#16519=CARTESIAN_POINT ( 'NONE',  ( 0.000000000000000000, 0.000000000000000000, 0.000000000000000000 ) ) ;
#16521=EDGE_CURVE ( 'NONE', #38433, #23803, #21918, .T. ) ;
#16526=EDGE_LOOP ( 'NONE', ( #27596, #31762, #38264, #39139 ) ) ;
#16527=ORIENTED_EDGE ( 'NONE', *, *, #34084, .F. ) ;
#16529=DIRECTION ( 'NONE',  ( -1.000000000000000000, 0.000000000000000000, 0.000000000000000000 ) ) ;
#16530=ORIENTED_EDGE ( 'NONE', *, *, #36367, .F. ) ;
#16531=EDGE_CURVE ( 'NONE', #6004, #38691, #15236, .T. ) ;
#16532=CYLINDRICAL_SURFACE ( 'NONE', #41864, 31.99999999999999289 ) ;
#16533=DIRECTION ( 'NONE',  ( -1.000000000000000000, -0.000000000000000000, -0.000000000000000000 ) ) ;
#16538=DIRECTION ( 'NONE',  ( 0.000000000000000000, 0.000000000000000000, 1.000000000000000000 ) ) ;
#16543=CYLINDRICAL_SURFACE ( 'NONE', #40290, 31.99999999999998579 ) ;
#16548=AXIS2_PLACEMENT_3D ( 'NONE', #32706, #2145, #9711 ) ;
#16551=AXIS2_PLACEMENT_3D ( 'NONE', #19964, #38101, #5295 ) ;
#16560=CARTESIAN_POINT ( 'NONE',  ( 11.99999999999999822, -62.50884508063395373, -41.76106447765554464 ) ) ;
#16561=ORIENTED_EDGE ( 'NONE', *, *, #42374, .F. ) ;
#16562=ADVANCED_FACE ( 'NONE', ( #27535 ), #46137, .T. ) ;
#16568=DIRECTION ( 'NONE',  ( 0.000000000000000000, 0.000000000000000000, -1.000000000000000000 ) ) ;
#16570=DIRECTION ( 'NONE',  ( 0.000000000000000000, -0.5877852522924802425, 0.8090169943749422332 ) ) ;
#16572=ORIENTED_EDGE ( 'NONE', *, *, #28014, .F. ) ;
#16573=EDGE_CURVE ( 'NONE', #14427, #1582, #12142, .T. ) ;
#16574=ORIENTED_EDGE ( 'NONE', *, *, #33376, .F. ) ;
#16577=DIRECTION ( 'NONE',  ( -1.000000000000000000, 0.000000000000000000, 0.000000000000000000 ) ) ;
#16580=CYLINDRICAL_SURFACE ( 'NONE', #6763, 82.00000000000000000 ) ;
#16582=ORIENTED_EDGE ( 'NONE', *, *, #25823, .F. ) ;
#16583=EDGE_CURVE ( 'NONE', #5172, #20943, #27062, .T. ) ;
#16587=ORIENTED_EDGE ( 'NONE', *, *, #35081, .F. ) ;
#16591=CARTESIAN_POINT ( 'NONE',  ( 11.99999999999999822, -74.74816331893404708, -33.71516098798819172 ) ) ;
#16601=EDGE_CURVE ( 'NONE', #42647, #15803, #42215, .T. ) ;
#16602=CARTESIAN_POINT ( 'NONE',  ( 11.99999999999999822, -40.65526001592663619, 71.21200624218782593 ) ) ;
#16604=CARTESIAN_POINT ( 'NONE',  ( 6.000000000000000000, 39.47590169984846398, 71.87247863392427405 ) ) ;
#16605=DIRECTION ( 'NONE',  ( -1.000000000000000000, 0.000000000000000000, -0.000000000000000000 ) ) ;
#16609=CARTESIAN_POINT ( 'NONE',  ( 0.000000000000000000, -74.74816331893453025, 33.71516098798714722 ) ) ;
#16618=ORIENTED_EDGE ( 'NONE', *, *, #4103, .T. ) ;
#16620=AXIS2_PLACEMENT_3D ( 'NONE', #8465, #8950, #8227 ) ;
#16622=ADVANCED_FACE ( 'NONE', ( #33898 ), #15549, .T. ) ;
#16629=VECTOR ( 'NONE', #38947, 1000.000000000000000 ) ;
#16634=ADVANCED_FACE ( 'NONE', ( #23137 ), #11639, .T. ) ;
#16636=EDGE_CURVE ( 'NONE', #39485, #34540, #22242, .T. ) ;
#16639=EDGE_LOOP ( 'NONE', ( #20409, #9075, #36050, #9067 ) ) ;
#16642=DIRECTION ( 'NONE',  ( -1.000000000000000000, 0.000000000000000000, 0.000000000000000000 ) ) ;
#16644=CIRCLE ( 'NONE', #18964, 82.00000000000000000 ) ;
#16648=ORIENTED_EDGE ( 'NONE', *, *, #33692, .F. ) ;
#16655=EDGE_LOOP ( 'NONE', ( #11935, #43035, #5643, #42228 ) ) ;
#16661=FACE_OUTER_BOUND ( 'NONE', #15614, .T. ) ;
#16663=CARTESIAN_POINT ( 'NONE',  ( 11.99999999999999822, -77.49459641780886443, 0.8261519478428549501 ) ) ;
#16671=DIRECTION ( 'NONE',  ( 0.000000000000000000, -0.7431448254773953543, -0.6691306063588570163 ) ) ;
#16672=DIRECTION ( 'NONE',  ( 0.000000000000000000, -0.8660254037844363761, 0.5000000000000039968 ) ) ;
#16681=LINE ( 'NONE', #8843, #26850 ) ;
#16686=EDGE_CURVE ( 'NONE', #24474, #6004, #35592, .T. ) ;
#16687=CIRCLE ( 'NONE', #29184, 31.99999999999999289 ) ;
#16688=CARTESIAN_POINT ( 'NONE',  ( 0.000000000000000000, 0.000000000000000000, 0.000000000000000000 ) ) ;
#16690=AXIS2_PLACEMENT_3D ( 'NONE', #34905, #45686, #46171 ) ;
#16697=EDGE_LOOP ( 'NONE', ( #24331, #33776, #1015, #26023 ) ) ;
#16698=CARTESIAN_POINT ( 'NONE',  ( 11.99999999999999822, 71.27951684758069462, -30.41916302227037150 ) ) ;
#16703=ORIENTED_EDGE ( 'NONE', *, *, #40951, .T. ) ;
#16708=CARTESIAN_POINT ( 'NONE',  ( 0.000000000000000000, 11.30684508768450591, -76.66974797899824523 ) ) ;
#16709=CARTESIAN_POINT ( 'NONE',  ( 11.99999999999999822, 71.91182617369230456, -28.89263327155667938 ) ) ;
#16711=DIRECTION ( 'NONE',  ( 0.000000000000000000, 0.9510565162951543083, 0.3090169943749449533 ) ) ;
#16715=ORIENTED_EDGE ( 'NONE', *, *, #23252, .T. ) ;
#16719=DIRECTION ( 'NONE',  ( -1.000000000000000000, -0.000000000000000000, -0.000000000000000000 ) ) ;
#16721=ORIENTED_EDGE ( 'NONE', *, *, #30605, .T. ) ;
#16722=AXIS2_PLACEMENT_3D ( 'NONE', #33945, #9815, #40576 ) ;
#16729=DIRECTION ( 'NONE',  ( -1.000000000000000000, -0.000000000000000000, 0.000000000000000000 ) ) ;
#16730=CARTESIAN_POINT ( 'NONE',  ( 6.000000000000000000, 81.50828551894240093, -8.966570791699810528 ) ) ;
#16734=AXIS2_PLACEMENT_3D ( 'NONE', #25260, #26254, #22076 ) ;
#16737=DIRECTION ( 'NONE',  ( 0.000000000000000000, 0.4539904997395478037, -0.8910065241883673437 ) ) ;
#16739=AXIS2_PLACEMENT_3D ( 'NONE', #24508, #39452, #5927 ) ;
#16740=DIRECTION ( 'NONE',  ( 0.000000000000000000, -0.1564344650402170744, -0.9876883405951399908 ) ) ;
#16741=DIRECTION ( 'NONE',  ( -1.000000000000000000, 0.000000000000000000, 0.000000000000000000 ) ) ;
#16742=AXIS2_PLACEMENT_3D ( 'NONE', #19156, #23314, #19389 ) ;
#16744=CARTESIAN_POINT ( 'NONE',  ( 11.99999999999999822, -17.28742895386137945, 75.54627589209938776 ) ) ;
#16748=DIRECTION ( 'NONE',  ( -1.000000000000000000, -0.000000000000000000, -0.000000000000000000 ) ) ;
#16757=ORIENTED_EDGE ( 'NONE', *, *, #13704, .T. ) ;
#16765=CARTESIAN_POINT ( 'NONE',  ( 11.99999999999999822, 0.000000000000000000, 0.000000000000000000 ) ) ;
#16769=ORIENTED_EDGE ( 'NONE', *, *, #15529, .F. ) ;
#16775=ORIENTED_EDGE ( 'NONE', *, *, #28398, .T. ) ;
#16780=LINE ( 'NONE', #40266, #33249 ) ;
#16782=CARTESIAN_POINT ( 'NONE',  ( 11.99999999999999822, -15.33399622253540606, 80.55351364060582853 ) ) ;
#16784=CARTESIAN_POINT ( 'NONE',  ( 12.00000000000000000, 24.81905959214260804, -9.408202855044828894 ) ) ;
#16785=CARTESIAN_POINT ( 'NONE',  ( 11.99999999999999822, -26.02418014898260878, -70.52718814184285634 ) ) ;
#16787=ORIENTED_EDGE ( 'NONE', *, *, #6096, .F. ) ;
#16788=FACE_OUTER_BOUND ( 'NONE', #18500, .T. ) ;
#16790=EDGE_CURVE ( 'NONE', #22095, #36859, #34005, .T. ) ;
#16796=VECTOR ( 'NONE', #29749, 1000.000000000000000 ) ;
#16797=VECTOR ( 'NONE', #10351, 1000.000000000000114 ) ;
#16798=CYLINDRICAL_SURFACE ( 'NONE', #18090, 31.99999999999998579 ) ;
#16800=FACE_OUTER_BOUND ( 'NONE', #36316, .T. ) ;
#16801=CARTESIAN_POINT ( 'NONE',  ( 11.99999999999999822, 0.000000000000000000, 0.000000000000000000 ) ) ;
#16807=EDGE_CURVE ( 'NONE', #18388, #10792, #5498, .T. ) ;
#16810=VECTOR ( 'NONE', #14244, 1000.000000000000000 ) ;
#16813=EDGE_CURVE ( 'NONE', #37423, #13942, #25403, .T. ) ;
#16815=VERTEX_POINT ( 'NONE', #35605 ) ;
#16817=EDGE_CURVE ( 'NONE', #32670, #40177, #16992, .T. ) ;
#16821=VECTOR ( 'NONE', #26303, 1000.000000000000000 ) ;
#16823=CYLINDRICAL_SURFACE ( 'NONE', #19884, 82.00000000000000000 ) ;
#16829=EDGE_CURVE ( 'NONE', #40361, #35892, #23850, .T. ) ;
#16833=ORIENTED_EDGE ( 'NONE', *, *, #15638, .F. ) ;
#16841=DIRECTION ( 'NONE',  ( 0.000000000000000000, 0.000000000000000000, 1.000000000000000000 ) ) ;
#16843=CARTESIAN_POINT ( 'NONE',  ( 11.99999999999999822, 0.000000000000000000, 0.000000000000000000 ) ) ;
#16846=ORIENTED_EDGE ( 'NONE', *, *, #27919, .T. ) ;
#16850=EDGE_CURVE ( 'NONE', #32306, #19020, #48051, .T. ) ;
#16851=CARTESIAN_POINT ( 'NONE',  ( 0.000000000000000000, -73.44644590900077219, 24.73286445877677764 ) ) ;
#16857=FACE_OUTER_BOUND ( 'NONE', #3626, .T. ) ;
#16863=ORIENTED_EDGE ( 'NONE', *, *, #1287, .F. ) ;
#16872=EDGE_CURVE ( 'NONE', #23277, #25392, #37285, .T. ) ;
#16874=DIRECTION ( 'NONE',  ( 0.000000000000000000, 1.000000000000000000, 3.491481338843133355E-15 ) ) ;
#16876=AXIS2_PLACEMENT_3D ( 'NONE', #43395, #35311, #32138 ) ;
#16879=DIRECTION ( 'NONE',  ( 0.000000000000000000, 0.000000000000000000, 1.000000000000000000 ) ) ;
#16880=ORIENTED_EDGE ( 'NONE', *, *, #18107, .T. ) ;
#16881=VERTEX_POINT ( 'NONE', #3748 ) ;
#16886=FACE_OUTER_BOUND ( 'NONE', #22778, .T. ) ;
#16892=ORIENTED_EDGE ( 'NONE', *, *, #41234, .T. ) ;
#16896=LINE ( 'NONE', #20809, #21183 ) ;
#16897=AXIS2_PLACEMENT_3D ( 'NONE', #35675, #2148, #17781 ) ;
#16902=DIRECTION ( 'NONE',  ( 0.000000000000000000, 0.8910065241883691201, -0.4539904997395446951 ) ) ;
#16903=ORIENTED_EDGE ( 'NONE', *, *, #27385, .F. ) ;
#16904=EDGE_CURVE ( 'NONE', #40015, #19091, #21859, .T. ) ;
#16905=FACE_OUTER_BOUND ( 'NONE', #13206, .T. ) ;
#16908=FACE_OUTER_BOUND ( 'NONE', #18595, .T. ) ;
#16916=CARTESIAN_POINT ( 'NONE',  ( 6.000000000000000000, 71.87247863392471459, -39.47590169984771080 ) ) ;
#16917=EDGE_CURVE ( 'NONE', #11391, #42540, #26191, .T. ) ;
#16921=ADVANCED_FACE ( 'NONE', ( #48057 ), #26018, .T. ) ;
#16922=ORIENTED_EDGE ( 'NONE', *, *, #5255, .F. ) ;
#16924=ORIENTED_EDGE ( 'NONE', *, *, #16531, .T. ) ;
#16928=EDGE_CURVE ( 'NONE', #1474, #6091, #18674, .T. ) ;
#16934=CARTESIAN_POINT ( 'NONE',  ( 11.99999999999999822, -78.73519480814969995, 22.90783923731599359 ) ) ;
#16935=FACE_OUTER_BOUND ( 'NONE', #4840, .T. ) ;
#16939=AXIS2_PLACEMENT_3D ( 'NONE', #23455, #20031, #5355 ) ;
#16940=LINE ( 'NONE', #31895, #32841 ) ;
#16941=VERTEX_POINT ( 'NONE', #15018 ) ;
#16942=CARTESIAN_POINT ( 'NONE',  ( 12.00000000000000000, 22.07842321921480533, -8.187992925817425771 ) ) ;
#16962=CARTESIAN_POINT ( 'NONE',  ( 15.00000000000000000, -4.261787119645322974, -26.19803753235774835 ) ) ;
#16963=ADVANCED_FACE ( 'NONE', ( #32641 ), #3019, .T. ) ;
#16965=CARTESIAN_POINT ( 'NONE',  ( 15.00000000000000000, -23.29833615347109088, -3.418703333116486665 ) ) ;
#16967=DIRECTION ( 'NONE',  ( 1.000000000000000000, 0.000000000000000000, 0.000000000000000000 ) ) ;
#16968=VECTOR ( 'NONE', #15745, 1000.000000000000000 ) ;
#16972=AXIS2_PLACEMENT_3D ( 'NONE', #18814, #18344, #26180 ) ;
#16973=LINE ( 'NONE', #25029, #47103 ) ;
#16974=LINE ( 'NONE', #31931, #40980 ) ;
#16976=EDGE_CURVE ( 'NONE', #9769, #28195, #25535, .T. ) ;
#16981=LINE ( 'NONE', #18167, #15850 ) ;
#16982=ORIENTED_EDGE ( 'NONE', *, *, #30067, .T. ) ;
#16983=EDGE_CURVE ( 'NONE', #26733, #30959, #19624, .T. ) ;
#16988=ORIENTED_EDGE ( 'NONE', *, *, #38930, .F. ) ;
#16991=CARTESIAN_POINT ( 'NONE',  ( 0.000000000000000000, 59.03961581697465277, -46.53671651293886669 ) ) ;
#16992=LINE ( 'NONE', #31948, #13686 ) ;
#16998=DIRECTION ( 'NONE',  ( 1.000000000000000000, -0.000000000000000000, 0.000000000000000000 ) ) ;
#16999=CARTESIAN_POINT ( 'NONE',  ( 11.99999999999999822, 75.16055320797030959, 18.89407956138283851 ) ) ;
#17008=EDGE_CURVE ( 'NONE', #28298, #34997, #21507, .T. ) ;
#17009=CARTESIAN_POINT ( 'NONE',  ( 12.00000000000000000, 8.688484142253932063, -21.88630264137371384 ) ) ;
#17011=DIRECTION ( 'NONE',  ( 0.000000000000000000, 0.000000000000000000, -1.000000000000000000 ) ) ;
#17017=DIRECTION ( 'NONE',  ( -1.000000000000000000, 0.000000000000000000, 0.000000000000000000 ) ) ;
#17024=EDGE_CURVE ( 'NONE', #10193, #32354, #47335, .T. ) ;
#17027=CARTESIAN_POINT ( 'NONE',  ( 15.00000000000000000, -3.948201729842355068, -23.21447184625292692 ) ) ;
#17036=AXIS2_PLACEMENT_3D ( 'NONE', #25356, #40063, #13630 ) ;
#17037=DIRECTION ( 'NONE',  ( 0.000000000000000000, -0.8090169943749497827, -0.5877852522924698064 ) ) ;
#17041=ORIENTED_EDGE ( 'NONE', *, *, #40122, .T. ) ;
#17047=ORIENTED_EDGE ( 'NONE', *, *, #19045, .T. ) ;
#17053=CARTESIAN_POINT ( 'NONE',  ( 12.00000000000000000, -0.9646360437375368635, -23.52805723605589705 ) ) ;
#17055=ORIENTED_EDGE ( 'NONE', *, *, #31414, .F. ) ;
#17059=DIRECTION ( 'NONE',  ( 0.000000000000000000, 0.000000000000000000, 1.000000000000000000 ) ) ;
#17060=EDGE_LOOP ( 'NONE', ( #34937, #3438, #45350, #9053 ) ) ;
#17065=DIRECTION ( 'NONE',  ( -1.000000000000000000, -0.000000000000000000, -0.000000000000000000 ) ) ;
#17067=FACE_OUTER_BOUND ( 'NONE', #8789, .T. ) ;
#17069=AXIS2_PLACEMENT_3D ( 'NONE', #6470, #32186, #17720 ) ;
#17079=CARTESIAN_POINT ( 'NONE',  ( 0.000000000000000000, 51.29473840253223216, 63.97538442413444670 ) ) ;
#17082=ORIENTED_EDGE ( 'NONE', *, *, #5301, .F. ) ;
#17084=CARTESIAN_POINT ( 'NONE',  ( 11.99999999999999822, 77.32052557432841411, 5.256550761633121738 ) ) ;
#17085=ADVANCED_FACE ( 'NONE', ( #4716 ), #37521, .T. ) ;
#17088=ORIENTED_EDGE ( 'NONE', *, *, #1215, .T. ) ;
#17097=EDGE_CURVE ( 'NONE', #35782, #4856, #15268, .T. ) ;
#17098=VECTOR ( 'NONE', #1227, 1000.000000000000000 ) ;
#17099=ORIENTED_EDGE ( 'NONE', *, *, #24428, .T. ) ;
#17108=ORIENTED_EDGE ( 'NONE', *, *, #3596, .T. ) ;
#17110=ORIENTED_EDGE ( 'NONE', *, *, #27257, .F. ) ;
#17116=ORIENTED_EDGE ( 'NONE', *, *, #10228, .T. ) ;
#17118=DIRECTION ( 'NONE',  ( 0.000000000000000000, -0.6494480483301739993, -0.7604059656000390355 ) ) ;
#17129=ORIENTED_EDGE ( 'NONE', *, *, #34471, .T. ) ;
#17134=EDGE_LOOP ( 'NONE', ( #15165, #39846, #624, #1907 ) ) ;
#17138=CARTESIAN_POINT ( 'NONE',  ( 6.000000000000000000, -15.33399622253424432, -80.55351364060604169 ) ) ;
#17139=LINE ( 'NONE', #28397, #33586 ) ;
#17144=DIRECTION ( 'NONE',  ( -1.000000000000000000, 0.000000000000000000, 0.000000000000000000 ) ) ;
#17149=VERTEX_POINT ( 'NONE', #16942 ) ;
#17159=CARTESIAN_POINT ( 'NONE',  ( 11.99999999999999822, 69.42325613327440692, 34.44570377933622041 ) ) ;
#17161=VERTEX_POINT ( 'NONE', #39217 ) ;
#17169=EDGE_CURVE ( 'NONE', #38560, #7173, #31407, .T. ) ;
#17170=CARTESIAN_POINT ( 'NONE',  ( 11.99999999999999822, 79.10210256391397365, -21.60688246758502729 ) ) ;
#17173=CYLINDRICAL_SURFACE ( 'NONE', #37512, 82.00000000000000000 ) ;
#17175=EDGE_LOOP ( 'NONE', ( #19568, #26734, #32125, #16386 ) ) ;
#17180=CARTESIAN_POINT ( 'NONE',  ( 0.000000000000000000, 0.000000000000000000, 0.000000000000000000 ) ) ;
#17181=CARTESIAN_POINT ( 'NONE',  ( 11.99999999999999822, 77.32052557432841411, 5.256550761633121738 ) ) ;
#17191=AXIS2_PLACEMENT_3D ( 'NONE', #15640, #41841, #15172 ) ;
#17193=AXIS2_PLACEMENT_3D ( 'NONE', #6709, #21380, #32640 ) ;
#17209=EDGE_CURVE ( 'NONE', #12329, #24320, #40320, .T. ) ;
#17211=ORIENTED_EDGE ( 'NONE', *, *, #9629, .F. ) ;
#17215=DIRECTION ( 'NONE',  ( 0.000000000000000000, -0.1564344650402168801, -0.9876883405951399908 ) ) ;
#17220=VECTOR ( 'NONE', #27811, 999.9999999999998863 ) ;
#17222=ORIENTED_EDGE ( 'NONE', *, *, #29086, .T. ) ;
#17223=DIRECTION ( 'NONE',  ( -1.000000000000000000, 0.000000000000000000, 0.000000000000000000 ) ) ;
#17224=EDGE_CURVE ( 'NONE', #32354, #35720, #41857, .T. ) ;
#17225=EDGE_LOOP ( 'NONE', ( #18899, #6210, #38431, #10051 ) ) ;
#17226=AXIS2_PLACEMENT_3D ( 'NONE', #22550, #36983, #11776 ) ;
#17227=EDGE_CURVE ( 'NONE', #29462, #48127, #35548, .T. ) ;
#17243=DIRECTION ( 'NONE',  ( 0.000000000000000000, 0.000000000000000000, 1.000000000000000000 ) ) ;
#17244=CARTESIAN_POINT ( 'NONE',  ( 11.99999999999999822, 68.67312586194995561, 35.91791733033500122 ) ) ;
#17246=CARTESIAN_POINT ( 'NONE',  ( 11.99999999999999822, -12.93880638057369659, 76.41127070299266677 ) ) ;
#17247=LINE ( 'NONE', #32444, #39563 ) ;
#17249=ORIENTED_EDGE ( 'NONE', *, *, #46752, .T. ) ;
#17250=CYLINDRICAL_SURFACE ( 'NONE', #27066, 31.99999999999998579 ) ;
#17254=VECTOR ( 'NONE', #7201, 1000.000000000000000 ) ;
#17255=ORIENTED_EDGE ( 'NONE', *, *, #27919, .F. ) ;
#17256=CARTESIAN_POINT ( 'NONE',  ( 5.999999999999999112, 50.23322058963348979, 64.81221759200361987 ) ) ;
#17257=CARTESIAN_POINT ( 'NONE',  ( 0.000000000000000000, 0.000000000000000000, 0.000000000000000000 ) ) ;
#17259=ORIENTED_EDGE ( 'NONE', *, *, #8053, .F. ) ;
#17261=AXIS2_PLACEMENT_3D ( 'NONE', #44891, #18459, #11844 ) ;
#17263=ORIENTED_EDGE ( 'NONE', *, *, #33531, .T. ) ;
#17265=VECTOR ( 'NONE', #2204, 1000.000000000000000 ) ;
#17269=AXIS2_PLACEMENT_3D ( 'NONE', #2156, #31302, #39615 ) ;
#17270=VERTEX_POINT ( 'NONE', #7120 ) ;
#17273=VERTEX_POINT ( 'NONE', #37221 ) ;
#17274=ADVANCED_FACE ( 'NONE', ( #36256 ), #43611, .T. ) ;
#17276=DIRECTION ( 'NONE',  ( -1.000000000000000000, -0.000000000000000000, 0.000000000000000000 ) ) ;
#17277=DIRECTION ( 'NONE',  ( -1.000000000000000000, -0.000000000000000000, -0.000000000000000000 ) ) ;
#17285=DIRECTION ( 'NONE',  ( 1.000000000000000000, 0.000000000000000000, 0.000000000000000000 ) ) ;
#17288=CIRCLE ( 'NONE', #23549, 31.99999999999999289 ) ;
#17293=DIRECTION ( 'NONE',  ( -1.000000000000000000, 0.000000000000000000, -0.000000000000000000 ) ) ;
#17294=ORIENTED_EDGE ( 'NONE', *, *, #19001, .F. ) ;
#17301=DIRECTION ( 'NONE',  ( 0.000000000000000000, 0.9238795325112877377, -0.3826834323650873948 ) ) ;
#17303=DIRECTION ( 'NONE',  ( -1.000000000000000000, 0.000000000000000000, -0.000000000000000000 ) ) ;
#17306=CARTESIAN_POINT ( 'NONE',  ( 11.99999999999999822, 14.67089635893819377, -73.72996012237423713 ) ) ;
#17309=CARTESIAN_POINT ( 'NONE',  ( 0.000000000000000000, 0.000000000000000000, 0.000000000000000000 ) ) ;
#17311=DIRECTION ( 'NONE',  ( 0.000000000000000000, 0.000000000000000000, 1.000000000000000000 ) ) ;
#17312=DIRECTION ( 'NONE',  ( 1.000000000000000000, -0.000000000000000000, 0.000000000000000000 ) ) ;
#17313=CARTESIAN_POINT ( 'NONE',  ( 0.000000000000000000, 68.26794271651262136, 31.47745569255165066 ) ) ;
#17318=CARTESIAN_POINT ( 'NONE',  ( 11.99999999999999822, 8.830959090342393125, 74.65491531819122883 ) ) ;
#17319=CARTESIAN_POINT ( 'NONE',  ( 12.00000000000000000, -0.9646360437375368635, -23.52805723605589705 ) ) ;
#17321=VERTEX_POINT ( 'NONE', #47286 ) ;
#17322=ORIENTED_EDGE ( 'NONE', *, *, #34310, .T. ) ;
#17330=CARTESIAN_POINT ( 'NONE',  ( 11.99999999999999822, 39.47590169984846398, 71.87247863392425984 ) ) ;
#17331=ORIENTED_EDGE ( 'NONE', *, *, #33257, .T. ) ;
#17343=DIRECTION ( 'NONE',  ( 0.000000000000000000, 0.000000000000000000, 1.000000000000000000 ) ) ;
#17347=VECTOR ( 'NONE', #12692, 1000.000000000000000 ) ;
#17348=DIRECTION ( 'NONE',  ( 0.000000000000000000, 0.000000000000000000, 1.000000000000000000 ) ) ;
#17357=EDGE_LOOP ( 'NONE', ( #29037, #43784, #26473, #43725 ) ) ;
#17364=DIRECTION ( 'NONE',  ( 1.000000000000000000, 0.000000000000000000, 0.000000000000000000 ) ) ;
#17366=DIRECTION ( 'NONE',  ( -1.000000000000000000, -0.000000000000000000, 0.000000000000000000 ) ) ;
#17369=FACE_OUTER_BOUND ( 'NONE', #15339, .T. ) ;
#17370=EDGE_CURVE ( 'NONE', #12813, #20184, #10304, .T. ) ;
#17373=LINE ( 'NONE', #39910, #5120 ) ;
#17374=AXIS2_PLACEMENT_3D ( 'NONE', #22150, #37081, #14328 ) ;
#17381=VERTEX_POINT ( 'NONE', #42109 ) ;
#17382=EDGE_CURVE ( 'NONE', #7173, #24762, #26217, .T. ) ;
#17383=CARTESIAN_POINT ( 'NONE',  ( 0.000000000000000000, 0.000000000000000000, 0.000000000000000000 ) ) ;
#17393=AXIS2_PLACEMENT_3D ( 'NONE', #16843, #27611, #42549 ) ;
#17396=ORIENTED_EDGE ( 'NONE', *, *, #32174, .F. ) ;
#17397=CIRCLE ( 'NONE', #19779, 82.00000000000000000 ) ;
#17400=FACE_OUTER_BOUND ( 'NONE', #3437, .T. ) ;
#17402=CARTESIAN_POINT ( 'NONE',  ( 12.00000000000000000, 22.07842321921492612, 8.187992925817123790 ) ) ;
#17405=CIRCLE ( 'NONE', #36972, 82.00000000000000000 ) ;
#17412=ORIENTED_EDGE ( 'NONE', *, *, #23038, .F. ) ;
#17416=DIRECTION ( 'NONE',  ( 1.000000000000000000, -0.000000000000000000, -0.000000000000000000 ) ) ;
#17420=ORIENTED_EDGE ( 'NONE', *, *, #6306, .F. ) ;
#17421=DIRECTION ( 'NONE',  ( -1.000000000000000000, 0.000000000000000000, 0.000000000000000000 ) ) ;
#17422=DIRECTION ( 'NONE',  ( -1.000000000000000000, 0.000000000000000000, 0.000000000000000000 ) ) ;
#17423=CARTESIAN_POINT ( 'NONE',  ( 0.000000000000000000, -2.956366410621191765, 75.11725578898467859 ) ) ;
#17426=AXIS2_PLACEMENT_3D ( 'NONE', #26737, #15483, #18427 ) ;
#17428=DIRECTION ( 'NONE',  ( 0.000000000000000000, 0.4539904997395477482, -0.8910065241883674547 ) ) ;
#17429=AXIS2_PLACEMENT_3D ( 'NONE', #38961, #5418, #1271 ) ;
#17433=LINE ( 'NONE', #35083, #33238 ) ;
#17439=VERTEX_POINT ( 'NONE', #45792 ) ;
#17443=ORIENTED_EDGE ( 'NONE', *, *, #30844, .F. ) ;
#17445=CIRCLE ( 'NONE', #4302, 31.99999999999998579 ) ;
#17451=AXIS2_PLACEMENT_3D ( 'NONE', #30418, #554, #4944 ) ;
#17456=EDGE_CURVE ( 'NONE', #12155, #17273, #735, .T. ) ;
#17458=ORIENTED_EDGE ( 'NONE', *, *, #6695, .F. ) ;
#17459=EDGE_CURVE ( 'NONE', #14267, #40188, #5591, .T. ) ;
#17462=CARTESIAN_POINT ( 'NONE',  ( 11.99999999999999822, -54.21277698773713638, 55.38113227695764351 ) ) ;
#17465=VECTOR ( 'NONE', #6540, 1000.000000000000000 ) ;
#17466=DIRECTION ( 'NONE',  ( 0.000000000000000000, 0.000000000000000000, 1.000000000000000000 ) ) ;
#17475=DIRECTION ( 'NONE',  ( -1.000000000000000000, -0.000000000000000000, -0.000000000000000000 ) ) ;
#17477=CIRCLE ( 'NONE', #46387, 82.00000000000000000 ) ;
#17479=FACE_OUTER_BOUND ( 'NONE', #41847, .T. ) ;
#17480=ORIENTED_EDGE ( 'NONE', *, *, #4613, .F. ) ;
#17481=ORIENTED_EDGE ( 'NONE', *, *, #11694, .T. ) ;
#17484=AXIS2_PLACEMENT_3D ( 'NONE', #40632, #32796, #47723 ) ;
#17488=CARTESIAN_POINT ( 'NONE',  ( 11.99999999999999822, -55.38113227695745167, -54.21277698773732823 ) ) ;
#17493=DIRECTION ( 'NONE',  ( 0.000000000000000000, -0.9969173337331271867, -0.07845909572785571273 ) ) ;
#17497=FACE_OUTER_BOUND ( 'NONE', #13736, .T. ) ;
#17498=EDGE_CURVE ( 'NONE', #31053, #26390, #7611, .T. ) ;
#17500=CARTESIAN_POINT ( 'NONE',  ( 11.99999999999999822, -76.66974797899830207, -11.30684508768420571 ) ) ;
#17503=CIRCLE ( 'NONE', #24533, 82.00000000000000000 ) ;
#17507=ORIENTED_EDGE ( 'NONE', *, *, #30550, .F. ) ;
#17509=DIRECTION ( 'NONE',  ( -1.000000000000000000, -0.000000000000000000, -0.000000000000000000 ) ) ;
#17511=CIRCLE ( 'NONE', #46457, 82.00000000000000000 ) ;
#17519=VECTOR ( 'NONE', #19776, 1000.000000000000000 ) ;
#17531=EDGE_LOOP ( 'NONE', ( #23819, #38118, #20627, #32646 ) ) ;
#17535=DIRECTION ( 'NONE',  ( 0.000000000000000000, 0.000000000000000000, -1.000000000000000000 ) ) ;
#17538=ORIENTED_EDGE ( 'NONE', *, *, #37952, .T. ) ;
#17548=EDGE_CURVE ( 'NONE', #42392, #46674, #118, .T. ) ;
#17549=CARTESIAN_POINT ( 'NONE',  ( 0.000000000000000000, -65.58780272294048075, -36.73666225445966660 ) ) ;
#17560=DIRECTION ( 'NONE',  ( -1.000000000000000000, -0.000000000000000000, 0.000000000000000000 ) ) ;
#17563=EDGE_CURVE ( 'NONE', #15597, #10015, #13413, .T. ) ;
#17566=CARTESIAN_POINT ( 'NONE',  ( 11.99999999999999822, -75.11764819372145041, -2.946379043147127064 ) ) ;
#17571=DIRECTION ( 'NONE',  ( 0.000000000000000000, 0.000000000000000000, -1.000000000000000000 ) ) ;
#17578=ORIENTED_EDGE ( 'NONE', *, *, #1441, .F. ) ;
#17579=CARTESIAN_POINT ( 'NONE',  ( 0.000000000000000000, 81.96053171279902472, -2.543863470248677316 ) ) ;
#17582=EDGE_CURVE ( 'NONE', #29949, #15931, #20415, .T. ) ;
#17583=AXIS2_PLACEMENT_3D ( 'NONE', #18182, #25770, #40709 ) ;
#17586=ORIENTED_EDGE ( 'NONE', *, *, #41664, .T. ) ;
#17588=AXIS2_PLACEMENT_3D ( 'NONE', #12166, #46656, #34898 ) ;
#17595=CARTESIAN_POINT ( 'NONE',  ( 5.999999999999999112, 55.16347631943131802, -60.67117009219074930 ) ) ;
#17596=CIRCLE ( 'NONE', #22298, 77.49899999999999523 ) ;
#17598=LINE ( 'NONE', #21265, #20474 ) ;
#17603=CARTESIAN_POINT ( 'NONE',  ( 11.99999999999999822, 68.27212725128275395, 31.46837873495001503 ) ) ;
#17604=AXIS2_PLACEMENT_3D ( 'NONE', #48269, #14747, #47540 ) ;
#17607=VERTEX_POINT ( 'NONE', #28375 ) ;
#17611=ORIENTED_EDGE ( 'NONE', *, *, #16976, .T. ) ;
#17616=CARTESIAN_POINT ( 'NONE',  ( 15.00000000000000000, 23.59884966291538078, 12.14883922797231008 ) ) ;
#17632=EDGE_CURVE ( 'NONE', #3822, #12857, #47024, .T. ) ;
#17633=EDGE_CURVE ( 'NONE', #8125, #9625, #25902, .T. ) ;
#17634=ORIENTED_EDGE ( 'NONE', *, *, #17692, .T. ) ;
#17640=CARTESIAN_POINT ( 'NONE',  ( 11.99999999999999822, 59.46389618801966037, 49.70050353004911159 ) ) ;
#17643=AXIS2_PLACEMENT_3D ( 'NONE', #21051, #9802, #20099 ) ;
#17644=ORIENTED_EDGE ( 'NONE', *, *, #36480, .T. ) ;
#17648=ORIENTED_EDGE ( 'NONE', *, *, #17563, .T. ) ;
#17652=CARTESIAN_POINT ( 'NONE',  ( 11.99999999999999822, 69.42325613327489009, -34.44570377933524696 ) ) ;
#17657=CARTESIAN_POINT ( 'NONE',  ( 11.99999999999999822, 40.65526001592713357, -71.21200624218752750 ) ) ;
#17658=EDGE_LOOP ( 'NONE', ( #37267, #20679, #19666, #47617 ) ) ;
#17661=DIRECTION ( 'NONE',  ( 0.000000000000000000, -0.2079116908177532363, 0.9781476007338069101 ) ) ;
#17664=ORIENTED_EDGE ( 'NONE', *, *, #2125, .T. ) ;
#17665=CYLINDRICAL_SURFACE ( 'NONE', #41089, 82.00000000000000000 ) ;
#17670=ORIENTED_EDGE ( 'NONE', *, *, #26627, .F. ) ;
#17676=CARTESIAN_POINT ( 'NONE',  ( 11.99999999999999822, 74.65374052328648702, 8.840884882375350529 ) ) ;
#17679=CARTESIAN_POINT ( 'NONE',  ( 11.99999999999999822, -50.95692526931372157, 58.39081064771733054 ) ) ;
#17681=EDGE_CURVE ( 'NONE', #5353, #14154, #24942, .T. ) ;
#17686=EDGE_CURVE ( 'NONE', #33006, #2837, #47460, .T. ) ;
#17688=ORIENTED_EDGE ( 'NONE', *, *, #2453, .F. ) ;
#17691=CARTESIAN_POINT ( 'NONE',  ( 11.99999999999999822, 62.20884554314020676, 46.21855187248652896 ) ) ;
#17692=EDGE_CURVE ( 'NONE', #5492, #897, #14173, .T. ) ;
#17694=CARTESIAN_POINT ( 'NONE',  ( 0.000000000000000000, -63.18004540533059554, 44.88180994100355292 ) ) ;
#17696=DIRECTION ( 'NONE',  ( -1.000000000000000000, 0.000000000000000000, 0.000000000000000000 ) ) ;
#17699=DIRECTION ( 'NONE',  ( -1.000000000000000000, 0.000000000000000000, 0.000000000000000000 ) ) ;
#17710=VECTOR ( 'NONE', #3847, 1000.000000000000000 ) ;
#17712=EDGE_CURVE ( 'NONE', #39648, #18873, #40042, .T. ) ;
#17718=CARTESIAN_POINT ( 'NONE',  ( 0.000000000000000000, 81.90746397400387480, 3.894527615418180044 ) ) ;
#17720=DIRECTION ( 'NONE',  ( 0.000000000000000000, -0.8910065241883722287, 0.4539904997395382558 ) ) ;
#17721=DIRECTION ( 'NONE',  ( 0.000000000000000000, -0.5877852522924691403, 0.8090169943749504489 ) ) ;
#17729=EDGE_CURVE ( 'NONE', #33736, #24721, #7057, .T. ) ;
#17731=CIRCLE ( 'NONE', #21650, 77.49899999999999523 ) ;
#17733=DIRECTION ( 'NONE',  ( 0.000000000000000000, 0.9876883405951383255, -0.1564344650402277048 ) ) ;
#17738=LINE ( 'NONE', #46401, #35488 ) ;
#17751=DIRECTION ( 'NONE',  ( 0.000000000000000000, 0.4539904997395478037, -0.8910065241883673437 ) ) ;
#17755=DIRECTION ( 'NONE',  ( 0.000000000000000000, 0.3090169943749411785, 0.9510565162951556406 ) ) ;
#17756=DIRECTION ( 'NONE',  ( -1.000000000000000000, -0.000000000000000000, 0.000000000000000000 ) ) ;
#17763=CARTESIAN_POINT ( 'NONE',  ( 0.000000000000000000, 66.50666863322000211, 39.78640506895628448 ) ) ;
#17765=VERTEX_POINT ( 'NONE', #47227 ) ;
#17767=LINE ( 'NONE', #25591, #21068 ) ;
#17769=EDGE_LOOP ( 'NONE', ( #35719, #22019, #41380, #22120 ) ) ;
#17773=ORIENTED_EDGE ( 'NONE', *, *, #1767, .F. ) ;
#17776=CIRCLE ( 'NONE', #31892, 31.99999999999998934 ) ;
#17781=DIRECTION ( 'NONE',  ( 0.000000000000000000, 0.000000000000000000, 1.000000000000000000 ) ) ;
#17784=CARTESIAN_POINT ( 'NONE',  ( 0.000000000000000000, 76.66974797899852945, -11.30684508768257679 ) ) ;
#17788=CARTESIAN_POINT ( 'NONE',  ( 11.99999999999999822, 72.35432306680485226, -20.40083707022909110 ) ) ;
#17797=ADVANCED_FACE ( 'NONE', ( #48417 ), #19038, .T. ) ;
#17800=AXIS2_PLACEMENT_3D ( 'NONE', #41812, #19031, #41328 ) ;
#17804=DIRECTION ( 'NONE',  ( 0.000000000000000000, 0.000000000000000000, 1.000000000000000000 ) ) ;
#17807=CARTESIAN_POINT ( 'NONE',  ( 11.99999999999999822, 49.70050353004975818, -59.46389618801909904 ) ) ;
#17810=LINE ( 'NONE', #18294, #28443 ) ;
#17814=VERTEX_POINT ( 'NONE', #37653 ) ;
#17817=VERTEX_POINT ( 'NONE', #23207 ) ;
#17829=ORIENTED_EDGE ( 'NONE', *, *, #29319, .T. ) ;
#17831=ORIENTED_EDGE ( 'NONE', *, *, #3190, .T. ) ;
#17833=DIRECTION ( 'NONE',  ( -1.000000000000000000, 0.000000000000000000, 0.000000000000000000 ) ) ;
#17835=EDGE_CURVE ( 'NONE', #675, #40605, #3638, .T. ) ;
#17839=CARTESIAN_POINT ( 'NONE',  ( 0.000000000000000000, -58.39081064771713869, -50.95692526931392052 ) ) ;
#17841=ORIENTED_EDGE ( 'NONE', *, *, #22080, .T. ) ;
#17843=LINE ( 'NONE', #14179, #35972 ) ;
#17844=DIRECTION ( 'NONE',  ( 1.000000000000000000, 0.000000000000000000, 0.000000000000000000 ) ) ;
#17846=ORIENTED_EDGE ( 'NONE', *, *, #45335, .T. ) ;
#17850=VERTEX_POINT ( 'NONE', #29820 ) ;
#17851=CYLINDRICAL_SURFACE ( 'NONE', #5819, 31.99999999999998579 ) ;
#17858=CARTESIAN_POINT ( 'NONE',  ( 0.000000000000000000, -79.10210256391383155, 21.60688246758558506 ) ) ;
#17860=DIRECTION ( 'NONE',  ( 0.000000000000000000, 0.000000000000000000, 1.000000000000000000 ) ) ;
#17862=DIRECTION ( 'NONE',  ( -1.000000000000000000, 0.000000000000000000, 0.000000000000000000 ) ) ;
#17869=DIRECTION ( 'NONE',  ( -1.000000000000000000, 0.000000000000000000, 0.000000000000000000 ) ) ;
#17870=DIRECTION ( 'NONE',  ( -1.000000000000000000, -0.000000000000000000, -0.000000000000000000 ) ) ;
#17871=ORIENTED_EDGE ( 'NONE', *, *, #16807, .F. ) ;
#17876=FACE_OUTER_BOUND ( 'NONE', #35484, .T. ) ;
#17879=CARTESIAN_POINT ( 'NONE',  ( 11.99999999999999822, -77.32052557432837148, -5.256550761633681290 ) ) ;
#17880=EDGE_CURVE ( 'NONE', #33388, #6346, #26406, .T. ) ;
#17881=CARTESIAN_POINT ( 'NONE',  ( 11.99999999999999822, -68.27212725128254078, -31.46837873495049465 ) ) ;
#17882=AXIS2_PLACEMENT_3D ( 'NONE', #47212, #7291, #44501 ) ;
#17884=EDGE_LOOP ( 'NONE', ( #10596, #28845, #6844, #19741 ) ) ;
#17886=EDGE_CURVE ( 'NONE', #897, #28171, #22960, .T. ) ;
#17889=CIRCLE ( 'NONE', #45270, 82.00000000000000000 ) ;
#17892=CYLINDRICAL_SURFACE ( 'NONE', #14199, 77.49899999999999523 ) ;
#17898=DIRECTION ( 'NONE',  ( -1.000000000000000000, -0.000000000000000000, 0.000000000000000000 ) ) ;
#17899=VERTEX_POINT ( 'NONE', #31536 ) ;
#17900=DIRECTION ( 'NONE',  ( -1.000000000000000000, -0.000000000000000000, -0.000000000000000000 ) ) ;
#17901=ORIENTED_EDGE ( 'NONE', *, *, #30550, .T. ) ;
#17902=FACE_OUTER_BOUND ( 'NONE', #46657, .T. ) ;
#17903=ORIENTED_EDGE ( 'NONE', *, *, #13443, .F. ) ;
#17905=DIRECTION ( 'NONE',  ( 0.000000000000000000, 0.000000000000000000, 1.000000000000000000 ) ) ;
#17909=CARTESIAN_POINT ( 'NONE',  ( 0.000000000000000000, 0.000000000000000000, 0.000000000000000000 ) ) ;
#17912=CARTESIAN_POINT ( 'NONE',  ( 11.99999999999999822, -71.27951684758005513, -30.41916302227188851 ) ) ;
#17914=CARTESIAN_POINT ( 'NONE',  ( 11.99999999999999822, 36.73666225445894185, 65.58780272294090707 ) ) ;
#17919=EDGE_LOOP ( 'NONE', ( #47947, #7787, #26740, #24939 ) ) ;
#17920=CYLINDRICAL_SURFACE ( 'NONE', #38519, 31.99999999999998579 ) ;
#17925=ORIENTED_EDGE ( 'NONE', *, *, #9286, .F. ) ;
#17926=CIRCLE ( 'NONE', #21843, 82.00000000000000000 ) ;
#17933=VERTEX_POINT ( 'NONE', #34944 ) ;
#17935=CYLINDRICAL_SURFACE ( 'NONE', #11206, 31.99999999999998579 ) ;
#17937=VERTEX_POINT ( 'NONE', #16123 ) ;
#17940=CARTESIAN_POINT ( 'NONE',  ( 11.99999999999999822, 46.11716303203283474, -67.80270845531838120 ) ) ;
#17944=ORIENTED_EDGE ( 'NONE', *, *, #1164, .T. ) ;
#17948=DIRECTION ( 'NONE',  ( 0.000000000000000000, 0.000000000000000000, 1.000000000000000000 ) ) ;
#17949=EDGE_CURVE ( 'NONE', #33272, #35412, #20748, .T. ) ;
#17950=LINE ( 'NONE', #40493, #40028 ) ;
#17952=ORIENTED_EDGE ( 'NONE', *, *, #19323, .T. ) ;
#17953=VECTOR ( 'NONE', #11585, 1000.000000000000000 ) ;
#17954=CARTESIAN_POINT ( 'NONE',  ( 0.000000000000000000, 36.73666225445894185, 65.58780272294090707 ) ) ;
#17956=ORIENTED_EDGE ( 'NONE', *, *, #32448, .T. ) ;
#17957=ADVANCED_FACE ( 'NONE', ( #1175 ), #42788, .T. ) ;
#17959=CIRCLE ( 'NONE', #38307, 77.49899999999999523 ) ;
#17960=DIRECTION ( 'NONE',  ( -1.000000000000000000, 0.000000000000000000, 0.000000000000000000 ) ) ;
#17963=VERTEX_POINT ( 'NONE', #24406 ) ;
#17966=AXIS2_PLACEMENT_3D ( 'NONE', #17549, #45197, #41291 ) ;
#17968=DIRECTION ( 'NONE',  ( -1.000000000000000000, 0.000000000000000000, -0.000000000000000000 ) ) ;
#17973=CARTESIAN_POINT ( 'NONE',  ( 11.99999999999999822, -51.03279382321125723, 55.19960302592048862 ) ) ;
#17976=DIRECTION ( 'NONE',  ( -1.000000000000000000, 0.000000000000000000, -0.000000000000000000 ) ) ;
#17979=DIRECTION ( 'NONE',  ( 0.000000000000000000, 0.000000000000000000, 1.000000000000000000 ) ) ;
#17983=ORIENTED_EDGE ( 'NONE', *, *, #39391, .F. ) ;
#17986=AXIS2_PLACEMENT_3D ( 'NONE', #44082, #36254, #21078 ) ;
#17988=EDGE_LOOP ( 'NONE', ( #27292, #40822, #2801, #297 ) ) ;
#17990=EDGE_CURVE ( 'NONE', #31583, #24639, #27367, .T. ) ;
#17991=DIRECTION ( 'NONE',  ( 0.000000000000000000, -0.3826834323650969427, 0.9238795325112837409 ) ) ;
#17992=ORIENTED_EDGE ( 'NONE', *, *, #35922, .F. ) ;
#17993=EDGE_CURVE ( 'NONE', #38319, #39373, #23398, .T. ) ;
#17996=VERTEX_POINT ( 'NONE', #12680 ) ;
#18002=ORIENTED_EDGE ( 'NONE', *, *, #17224, .T. ) ;
#18004=CARTESIAN_POINT ( 'NONE',  ( 11.99999999999999822, 65.64334221924964652, -41.19522573413665611 ) ) ;
#18011=EDGE_LOOP ( 'NONE', ( #12221, #13320, #43861, #19512 ) ) ;
#18020=DIRECTION ( 'NONE',  ( 0.000000000000000000, -0.3090169943749349613, -0.9510565162951576390 ) ) ;
#18031=CIRCLE ( 'NONE', #3176, 82.00000000000000000 ) ;
#18032=DIRECTION ( 'NONE',  ( -1.000000000000000000, 0.000000000000000000, -0.000000000000000000 ) ) ;
#18035=DIRECTION ( 'NONE',  ( 0.000000000000000000, -0.7071067811865389130, -0.7071067811865561215 ) ) ;
#18038=PLANE ( 'NONE',  #38115 ) ;
#18041=DIRECTION ( 'NONE',  ( -1.000000000000000000, 0.000000000000000000, -0.000000000000000000 ) ) ;
#18042=CARTESIAN_POINT ( 'NONE',  ( 0.000000000000000000, 0.000000000000000000, 0.000000000000000000 ) ) ;
#18046=ADVANCED_FACE ( 'NONE', ( #26029 ), #28575, .T. ) ;
#18047=ADVANCED_FACE ( 'NONE', ( #29945 ), #7188, .T. ) ;
#18049=LINE ( 'NONE', #39642, #3012 ) ;
#18051=CARTESIAN_POINT ( 'NONE',  ( 0.000000000000000000, 0.000000000000000000, 0.000000000000000000 ) ) ;
#18057=VECTOR ( 'NONE', #5889, 1000.000000000000000 ) ;
#18060=ADVANCED_FACE ( 'NONE', ( #28321 ), #24890, .T. ) ;
#18069=VECTOR ( 'NONE', #18621, 1000.000000000000000 ) ;
#18073=ORIENTED_EDGE ( 'NONE', *, *, #38676, .F. ) ;
#18074=ORIENTED_EDGE ( 'NONE', *, *, #22996, .T. ) ;
#18075=DIRECTION ( 'NONE',  ( -1.000000000000000000, -0.000000000000000000, 0.000000000000000000 ) ) ;
#18076=AXIS2_PLACEMENT_3D ( 'NONE', #3970, #16371, #7870 ) ;
#18077=FACE_OUTER_BOUND ( 'NONE', #47363, .T. ) ;
#18084=DIRECTION ( 'NONE',  ( 0.000000000000000000, 0.000000000000000000, -1.000000000000000000 ) ) ;
#18090=AXIS2_PLACEMENT_3D ( 'NONE', #8707, #13357, #23642 ) ;
#18098=CIRCLE ( 'NONE', #43786, 77.49899999999999523 ) ;
#18107=EDGE_CURVE ( 'NONE', #38875, #15373, #33564, .T. ) ;
#18112=DIRECTION ( 'NONE',  ( -1.000000000000000000, -0.000000000000000000, -0.000000000000000000 ) ) ;
#18113=ORIENTED_EDGE ( 'NONE', *, *, #11770, .F. ) ;
#18122=CIRCLE ( 'NONE', #22042, 77.49899999999999523 ) ;
#18123=ORIENTED_EDGE ( 'NONE', *, *, #45043, .T. ) ;
#18125=CARTESIAN_POINT ( 'NONE',  ( 11.99999999999999822, 0.000000000000000000, 0.000000000000000000 ) ) ;
#18126=ORIENTED_EDGE ( 'NONE', *, *, #18278, .T. ) ;
#18129=DIRECTION ( 'NONE',  ( 0.000000000000000000, -0.9238795325112821866, -0.3826834323651006065 ) ) ;
#18133=VERTEX_POINT ( 'NONE', #15026 ) ;
#18135=CARTESIAN_POINT ( 'NONE',  ( 15.00000000000000000, -20.55727247249726020, 16.78983467731313084 ) ) ;
#18137=VECTOR ( 'NONE', #11685, 999.9999999999998863 ) ;
#18138=CARTESIAN_POINT ( 'NONE',  ( 11.99999999999999822, 0.000000000000000000, 0.000000000000000000 ) ) ;
#18139=CYLINDRICAL_SURFACE ( 'NONE', #46954, 31.99999999999998579 ) ;
#18145=ORIENTED_EDGE ( 'NONE', *, *, #18230, .T. ) ;
#18147=DIRECTION ( 'NONE',  ( -0.000000000000000000, 0.1045284632676437703, -0.9945218953682742891 ) ) ;
#18153=DIRECTION ( 'NONE',  ( -1.000000000000000000, -0.000000000000000000, -0.000000000000000000 ) ) ;
#18157=EDGE_CURVE ( 'NONE', #20008, #31521, #42169, .T. ) ;
#18160=AXIS2_PLACEMENT_3D ( 'NONE', #31478, #38325, #4793 ) ;
#18167=CARTESIAN_POINT ( 'NONE',  ( 15.00000000000000000, 20.85821328998756385, 10.92862929874494249 ) ) ;
#18174=LINE ( 'NONE', #33119, #44923 ) ;
#18177=ORIENTED_EDGE ( 'NONE', *, *, #4049, .T. ) ;
#18179=CARTESIAN_POINT ( 'NONE',  ( 11.99999999999999822, -39.47590169984896846, 71.87247863392398983 ) ) ;
#18182=CARTESIAN_POINT ( 'NONE',  ( 0.000000000000000000, -31.47745569255189224, 68.26794271651249346 ) ) ;
#18190=VECTOR ( 'NONE', #9552, 999.9999999999998863 ) ;
#18192=VERTEX_POINT ( 'NONE', #4965 ) ;
#18199=CIRCLE ( 'NONE', #24464, 77.49899999999998101 ) ;
#18203=AXIS2_PLACEMENT_3D ( 'NONE', #457, #15150, #27138 ) ;
#18205=CARTESIAN_POINT ( 'NONE',  ( 0.000000000000000000, 0.000000000000000000, 0.000000000000000000 ) ) ;
#18206=ORIENTED_EDGE ( 'NONE', *, *, #47482, .F. ) ;
#18208=VECTOR ( 'NONE', #39624, 1000.000000000000000 ) ;
#18210=DIRECTION ( 'NONE',  ( -1.000000000000000000, -0.000000000000000000, -0.000000000000000000 ) ) ;
#18211=CARTESIAN_POINT ( 'NONE',  ( 11.99999999999999822, 50.95692526931414790, -58.39081064771693974 ) ) ;
#18212=DIRECTION ( 'NONE',  ( 0.000000000000000000, 0.000000000000000000, 1.000000000000000000 ) ) ;
#18213=ORIENTED_EDGE ( 'NONE', *, *, #19225, .F. ) ;
#18215=DIRECTION ( 'NONE',  ( 0.000000000000000000, 0.000000000000000000, 1.000000000000000000 ) ) ;
#18220=EDGE_CURVE ( 'NONE', #10015, #19091, #35900, .T. ) ;
#18221=CARTESIAN_POINT ( 'NONE',  ( 11.99999999999999822, 71.91182617369230456, -28.89263327155667938 ) ) ;
#18225=DIRECTION ( 'NONE',  ( -1.000000000000000000, 0.000000000000000000, 0.000000000000000000 ) ) ;
#18226=CARTESIAN_POINT ( 'NONE',  ( 15.00000000000000000, 8.688484142253932063, -21.88630264137371029 ) ) ;
#18227=ORIENTED_EDGE ( 'NONE', *, *, #3912, .F. ) ;
#18228=EDGE_CURVE ( 'NONE', #36977, #26066, #23812, .T. ) ;
#18229=CIRCLE ( 'NONE', #30764, 31.99999999999998579 ) ;
#18230=EDGE_CURVE ( 'NONE', #8878, #42578, #14813, .T. ) ;
#18231=ORIENTED_EDGE ( 'NONE', *, *, #48360, .F. ) ;
#18233=AXIS2_PLACEMENT_3D ( 'NONE', #31540, #1429, #9477 ) ;
#18235=AXIS2_PLACEMENT_3D ( 'NONE', #3830, #12159, #30496 ) ;
#18238=VECTOR ( 'NONE', #36644, 1000.000000000000000 ) ;
#18239=ORIENTED_EDGE ( 'NONE', *, *, #23172, .T. ) ;
#18241=AXIS2_PLACEMENT_3D ( 'NONE', #13264, #1525, #16449 ) ;
#18245=CARTESIAN_POINT ( 'NONE',  ( 11.99999999999999822, 22.90783923731629201, 78.73519480814962890 ) ) ;
#18246=AXIS2_PLACEMENT_3D ( 'NONE', #5670, #39700, #35531 ) ;
#18255=DIRECTION ( 'NONE',  ( 1.000000000000000000, -0.000000000000000000, -0.000000000000000000 ) ) ;
#18258=ORIENTED_EDGE ( 'NONE', *, *, #7567, .F. ) ;
#18266=DIRECTION ( 'NONE',  ( 0.000000000000000000, 0.9969173337331281859, -0.07845909572784182107 ) ) ;
#18272=EDGE_CURVE ( 'NONE', #9873, #45638, #21052, .T. ) ;
#18274=ORIENTED_EDGE ( 'NONE', *, *, #45578, .T. ) ;
#18276=AXIS2_PLACEMENT_3D ( 'NONE', #19460, #37600, #22439 ) ;
#18277=VECTOR ( 'NONE', #10663, 1000.000000000000000 ) ;
#18278=EDGE_CURVE ( 'NONE', #21831, #15376, #37773, .T. ) ;
#18279=CARTESIAN_POINT ( 'NONE',  ( 11.99999999999999822, 55.19960302592066625, 51.03279382321107249 ) ) ;
#18282=DIRECTION ( 'NONE',  ( 0.000000000000000000, 0.8090169943749445647, 0.5877852522924770229 ) ) ;
#18284=CARTESIAN_POINT ( 'NONE',  ( 11.99999999999999822, 0.000000000000000000, 0.000000000000000000 ) ) ;
#18287=CARTESIAN_POINT ( 'NONE',  ( 11.99999999999999822, -69.42325613327415113, -34.44570377933671779 ) ) ;
#18292=AXIS2_PLACEMENT_3D ( 'NONE', #47273, #3178, #37207 ) ;
#18294=CARTESIAN_POINT ( 'NONE',  ( 6.000000000000000000, 22.90783923731629201, 78.73519480814962890 ) ) ;
#18297=AXIS2_PLACEMENT_3D ( 'NONE', #23799, #13037, #31894 ) ;
#18303=EDGE_LOOP ( 'NONE', ( #38270, #5798, #15691, #36475 ) ) ;
#18310=VECTOR ( 'NONE', #47049, 1000.000000000000000 ) ;
#18314=DIRECTION ( 'NONE',  ( -1.000000000000000000, -0.000000000000000000, 0.000000000000000000 ) ) ;
#18322=CIRCLE ( 'NONE', #13618, 77.49899999999998101 ) ;
#18333=EDGE_CURVE ( 'NONE', #29949, #5918, #46078, .T. ) ;
#18337=CARTESIAN_POINT ( 'NONE',  ( 11.99999999999999822, 20.41045688087824317, 72.35160999960824313 ) ) ;
#18339=CARTESIAN_POINT ( 'NONE',  ( 11.99999999999999822, 59.03342792756328095, -46.54456581323744757 ) ) ;
#18342=LINE ( 'NONE', #37920, #6450 ) ;
#18344=DIRECTION ( 'NONE',  ( -1.000000000000000000, -0.000000000000000000, -0.000000000000000000 ) ) ;
#18345=AXIS2_PLACEMENT_3D ( 'NONE', #45990, #28104, #23454 ) ;
#18348=ADVANCED_FACE ( 'NONE', ( #24781 ), #17173, .T. ) ;
#18350=AXIS2_PLACEMENT_3D ( 'NONE', #15251, #26498, #27225 ) ;
#18351=CYLINDRICAL_SURFACE ( 'NONE', #37745, 77.49899999999999523 ) ;
#18358=VECTOR ( 'NONE', #15732, 1000.000000000000000 ) ;
#18359=VECTOR ( 'NONE', #6270, 1000.000000000000000 ) ;
#18362=CARTESIAN_POINT ( 'NONE',  ( 11.99999999999999822, -54.21277698773636899, -55.38113227695839669 ) ) ;
#18363=CIRCLE ( 'NONE', #35570, 31.99999999999998579 ) ;
#18364=EDGE_LOOP ( 'NONE', ( #31767, #79, #31462, #11775 ) ) ;
#18365=VECTOR ( 'NONE', #22044, 1000.000000000000114 ) ;
#18368=CARTESIAN_POINT ( 'NONE',  ( 11.99999999999999822, -3.894527615418461153, 81.90746397400387480 ) ) ;
#18386=CARTESIAN_POINT ( 'NONE',  ( 0.000000000000000000, -55.38113227695745167, -54.21277698773732823 ) ) ;
#18387=CARTESIAN_POINT ( 'NONE',  ( 11.99999999999999822, 71.87247863392470038, -39.47590169984768949 ) ) ;
#18388=VERTEX_POINT ( 'NONE', #25001 ) ;
#18393=ORIENTED_EDGE ( 'NONE', *, *, #21373, .F. ) ;
#18403=DIRECTION ( 'NONE',  ( 0.000000000000000000, -0.9723699203976789995, 0.2334453638558957322 ) ) ;
#18405=EDGE_CURVE ( 'NONE', #9566, #17161, #9127, .T. ) ;
#18407=DIRECTION ( 'NONE',  ( -1.000000000000000000, -0.000000000000000000, -0.000000000000000000 ) ) ;
#18409=ADVANCED_FACE ( 'NONE', ( #5951 ), #39478, .T. ) ;
#18410=CARTESIAN_POINT ( 'NONE',  ( 0.000000000000000000, -71.27951684758005513, -30.41916302227188851 ) ) ;
#18416=DIRECTION ( 'NONE',  ( 0.000000000000000000, 0.7431448254773939111, 0.6691306063588584596 ) ) ;
#18427=DIRECTION ( 'NONE',  ( 0.000000000000000000, 0.000000000000000000, 1.000000000000000000 ) ) ;
#18436=EDGE_CURVE ( 'NONE', #1080, #11405, #6259, .T. ) ;
#18443=DIRECTION ( 'NONE',  ( -1.000000000000000000, 0.000000000000000000, 0.000000000000000000 ) ) ;
#18449=CARTESIAN_POINT ( 'NONE',  ( 0.000000000000000000, -21.60688246758530084, -79.10210256391388839 ) ) ;
#18450=VECTOR ( 'NONE', #4154, 1000.000000000000114 ) ;
#18456=CARTESIAN_POINT ( 'NONE',  ( 11.99999999999999822, -14.66109333815410487, -73.73191006444587003 ) ) ;
#18459=DIRECTION ( 'NONE',  ( -1.000000000000000000, -0.000000000000000000, -0.000000000000000000 ) ) ;
#18469=CARTESIAN_POINT ( 'NONE',  ( 11.99999999999999822, -75.11764819372149304, 2.946379043146075905 ) ) ;
#18472=DIRECTION ( 'NONE',  ( 0.000000000000000000, 0.4067366430758009854, 0.9135454576426004225 ) ) ;
#18473=CIRCLE ( 'NONE', #19237, 31.99999999999998579 ) ;
#18474=CARTESIAN_POINT ( 'NONE',  ( 15.00000000000000000, 20.85821328998756385, 10.92862929874494249 ) ) ;
#18480=CARTESIAN_POINT ( 'NONE',  ( 0.000000000000000000, -77.19088730480518734, -6.903761155838607166 ) ) ;
#18483=CARTESIAN_POINT ( 'NONE',  ( 11.99999999999999822, 34.94270380257741238, -74.18225833017854143 ) ) ;
#18484=CIRCLE ( 'NONE', #5992, 31.99999999999998934 ) ;
#18485=VECTOR ( 'NONE', #26224, 999.9999999999998863 ) ;
#18486=DIRECTION ( 'NONE',  ( -1.000000000000000000, -0.000000000000000000, 0.000000000000000000 ) ) ;
#18489=VECTOR ( 'NONE', #3352, 1000.000000000000000 ) ;
#18491=ORIENTED_EDGE ( 'NONE', *, *, #11997, .T. ) ;
#18494=AXIS2_PLACEMENT_3D ( 'NONE', #9185, #39280, #9655 ) ;
#18495=EDGE_CURVE ( 'NONE', #44863, #33047, #12510, .T. ) ;
#18496=LINE ( 'NONE', #21913, #16796 ) ;
#18499=EDGE_CURVE ( 'NONE', #40483, #6863, #19531, .T. ) ;
#18500=EDGE_LOOP ( 'NONE', ( #13876, #24291, #41856, #20705 ) ) ;
#18501=AXIS2_PLACEMENT_3D ( 'NONE', #20822, #31864, #46781 ) ;
#18504=ORIENTED_EDGE ( 'NONE', *, *, #6010, .F. ) ;
#18505=EDGE_CURVE ( 'NONE', #5920, #13159, #25718, .T. ) ;
#18506=ORIENTED_EDGE ( 'NONE', *, *, #1767, .T. ) ;
#18510=VERTEX_POINT ( 'NONE', #36264 ) ;
#18511=AXIS2_PLACEMENT_3D ( 'NONE', #46839, #27765, #16261 ) ;
#18512=VERTEX_POINT ( 'NONE', #29886 ) ;
#18514=ORIENTED_EDGE ( 'NONE', *, *, #16102, .F. ) ;
#18515=DIRECTION ( 'NONE',  ( -1.000000000000000000, -0.000000000000000000, -0.000000000000000000 ) ) ;
#18517=CARTESIAN_POINT ( 'NONE',  ( 15.00000000000000000, 8.688484142253932063, -21.88630264137371029 ) ) ;
#18518=CARTESIAN_POINT ( 'NONE',  ( 0.000000000000000000, 26.01480285779837232, 70.53064760720326376 ) ) ;
#18521=CARTESIAN_POINT ( 'NONE',  ( 11.99999999999999822, 49.70050353004889132, 59.46389618801982380 ) ) ;
#18525=CARTESIAN_POINT ( 'NONE',  ( 11.99999999999999822, 70.53064760720278059, 26.01480285779964774 ) ) ;
#18528=ORIENTED_EDGE ( 'NONE', *, *, #37134, .T. ) ;
#18529=EDGE_CURVE ( 'NONE', #8637, #33006, #43768, .T. ) ;
#18535=LINE ( 'NONE', #10716, #41181 ) ;
#18542=CARTESIAN_POINT ( 'NONE',  ( 15.00000000000000000, 8.688484142254226938, 21.88630264137359305 ) ) ;
#18545=ORIENTED_EDGE ( 'NONE', *, *, #34204, .T. ) ;
#18547=AXIS2_PLACEMENT_3D ( 'NONE', #38596, #30293, #31258 ) ;
#18550=DIRECTION ( 'NONE',  ( 0.000000000000000000, 0.000000000000000000, -1.000000000000000000 ) ) ;
#18558=ORIENTED_EDGE ( 'NONE', *, *, #4344, .T. ) ;
#18559=EDGE_CURVE ( 'NONE', #4757, #2290, #28904, .T. ) ;
#18562=AXIS2_PLACEMENT_3D ( 'NONE', #42121, #18632, #8100 ) ;
#18564=ORIENTED_EDGE ( 'NONE', *, *, #7224, .F. ) ;
#18565=FACE_OUTER_BOUND ( 'NONE', #41800, .T. ) ;
#18567=ORIENTED_EDGE ( 'NONE', *, *, #19438, .T. ) ;
#18572=EDGE_LOOP ( 'NONE', ( #19445, #24434, #6042, #11222 ) ) ;
#18574=EDGE_CURVE ( 'NONE', #45301, #24474, #14074, .T. ) ;
#18576=CARTESIAN_POINT ( 'NONE',  ( 15.00000000000000000, 23.49999999999999645, 1.499999999999995337 ) ) ;
#18577=VECTOR ( 'NONE', #1139, 1000.000000000000114 ) ;
#18578=ORIENTED_EDGE ( 'NONE', *, *, #48184, .F. ) ;
#18579=VERTEX_POINT ( 'NONE', #3453 ) ;
#18580=ADVANCED_FACE ( 'NONE', ( #25232 ), #26226, .T. ) ;
#18583=ORIENTED_EDGE ( 'NONE', *, *, #4344, .F. ) ;
#18590=VECTOR ( 'NONE', #42007, 1000.000000000000000 ) ;
#18593=DIRECTION ( 'NONE',  ( -1.000000000000000000, 0.000000000000000000, 0.000000000000000000 ) ) ;
#18595=EDGE_LOOP ( 'NONE', ( #42739, #47747, #29740, #27118 ) ) ;
#18601=ORIENTED_EDGE ( 'NONE', *, *, #9455, .F. ) ;
#18611=ORIENTED_EDGE ( 'NONE', *, *, #24756, .F. ) ;
#18613=EDGE_LOOP ( 'NONE', ( #17611, #31725, #27578, #26499 ) ) ;
#18621=DIRECTION ( 'NONE',  ( -1.000000000000000000, -0.000000000000000000, 0.000000000000000000 ) ) ;
#18622=ORIENTED_EDGE ( 'NONE', *, *, #19042, .F. ) ;
#18628=DIRECTION ( 'NONE',  ( -1.000000000000000000, -0.000000000000000000, -0.000000000000000000 ) ) ;
#18629=ORIENTED_EDGE ( 'NONE', *, *, #21753, .T. ) ;
#18630=CYLINDRICAL_SURFACE ( 'NONE', #37576, 31.99999999999998579 ) ;
#18632=DIRECTION ( 'NONE',  ( -1.000000000000000000, -0.000000000000000000, -0.000000000000000000 ) ) ;
#18634=CARTESIAN_POINT ( 'NONE',  ( -10.00000000000000000, 0.000000000000000000, 0.000000000000000000 ) ) ;
#18636=EDGE_LOOP ( 'NONE', ( #39771, #34439, #14166, #44503 ) ) ;
#18637=AXIS2_PLACEMENT_3D ( 'NONE', #15711, #26985, #8370 ) ;
#18644=CARTESIAN_POINT ( 'NONE',  ( 6.000000000000000000, -80.55351364060578589, -15.33399622253569383 ) ) ;
#18648=DIRECTION ( 'NONE',  ( 1.000000000000000000, 0.000000000000000000, 0.000000000000000000 ) ) ;
#18649=FACE_OUTER_BOUND ( 'NONE', #25588, .T. ) ;
#18652=CARTESIAN_POINT ( 'NONE',  ( 11.99999999999999822, 55.38113227695783536, 54.21277698773694453 ) ) ;
#18664=CIRCLE ( 'NONE', #32740, 82.00000000000000000 ) ;
#18668=ORIENTED_EDGE ( 'NONE', *, *, #34145, .T. ) ;
#18674=LINE ( 'NONE', #33373, #14455 ) ;
#18681=CARTESIAN_POINT ( 'NONE',  ( 11.99999999999999822, 65.59268652807210742, 36.72794159290264560 ) ) ;
#18682=ORIENTED_EDGE ( 'NONE', *, *, #12220, .F. ) ;
#18686=DIRECTION ( 'NONE',  ( -1.000000000000000000, -0.000000000000000000, 0.000000000000000000 ) ) ;
#18689=CARTESIAN_POINT ( 'NONE',  ( -10.00000000000000000, 0.000000000000000000, 0.000000000000000000 ) ) ;
#18690=DIRECTION ( 'NONE',  ( 1.000000000000000000, 0.000000000000000000, -0.000000000000000000 ) ) ;
#18691=VERTEX_POINT ( 'NONE', #4196 ) ;
#18695=LINE ( 'NONE', #47825, #28314 ) ;
#18699=DIRECTION ( 'NONE',  ( 1.000000000000000000, 0.000000000000000000, 0.000000000000000000 ) ) ;
#18702=DIRECTION ( 'NONE',  ( -1.000000000000000000, 0.000000000000000000, 0.000000000000000000 ) ) ;
#18704=DIRECTION ( 'NONE',  ( -1.000000000000000000, -0.000000000000000000, 0.000000000000000000 ) ) ;
#18710=DIRECTION ( 'NONE',  ( 0.000000000000000000, 0.9969173337331276308, 0.07845909572784874608 ) ) ;
#18715=VERTEX_POINT ( 'NONE', #12505 ) ;
#18724=DIRECTION ( 'NONE',  ( 0.000000000000000000, -0.8090169943749402348, -0.5877852522924830181 ) ) ;
#18730=EDGE_LOOP ( 'NONE', ( #4195, #8984, #29625, #21621 ) ) ;
#18733=LINE ( 'NONE', #387, #15730 ) ;
#18735=EDGE_LOOP ( 'NONE', ( #26436, #36082, #32938, #27186 ) ) ;
#18740=DIRECTION ( 'NONE',  ( 0.000000000000000000, -0.5877852522924689183, 0.8090169943749504489 ) ) ;
#18742=CARTESIAN_POINT ( 'NONE',  ( 0.000000000000000000, -36.72794159290288718, 65.59268652807197952 ) ) ;
#18751=CARTESIAN_POINT ( 'NONE',  ( 0.000000000000000000, -68.55367621811110723, -44.99326035066126650 ) ) ;
#18753=DIRECTION ( 'NONE',  ( 0.000000000000000000, 0.6494480483301849905, -0.7604059656000298206 ) ) ;
#18756=CARTESIAN_POINT ( 'NONE',  ( 6.000000000000000000, 16.65972982744933972, 80.28980883073764119 ) ) ;
#18759=VECTOR ( 'NONE', #30730, 1000.000000000000000 ) ;
#18764=VECTOR ( 'NONE', #26445, 1000.000000000000000 ) ;
#18776=CYLINDRICAL_SURFACE ( 'NONE', #47228, 31.99999999999997868 ) ;
#18779=EDGE_CURVE ( 'NONE', #3340, #40727, #9532, .T. ) ;
#18784=ADVANCED_FACE ( 'NONE', ( #20808 ), #35245, .F. ) ;
#18787=CARTESIAN_POINT ( 'NONE',  ( 0.000000000000000000, -31.46837873494930093, -68.27212725128309501 ) ) ;
#18788=AXIS2_PLACEMENT_3D ( 'NONE', #4486, #19390, #14539 ) ;
#18794=VECTOR ( 'NONE', #585, 1000.000000000000000 ) ;
#18795=AXIS2_PLACEMENT_3D ( 'NONE', #22038, #47509, #40183 ) ;
#18801=AXIS2_PLACEMENT_3D ( 'NONE', #1553, #17422, #2262 ) ;
#18804=CIRCLE ( 'NONE', #41498, 82.00000000000000000 ) ;
#18806=DIRECTION ( 'NONE',  ( -1.000000000000000000, 0.000000000000000000, 0.000000000000000000 ) ) ;
#18807=VERTEX_POINT ( 'NONE', #39669 ) ;
#18812=FACE_OUTER_BOUND ( 'NONE', #26763, .T. ) ;
#18814=CARTESIAN_POINT ( 'NONE',  ( -10.00000000000000000, 0.000000000000000000, 0.000000000000000000 ) ) ;
#18819=CARTESIAN_POINT ( 'NONE',  ( 11.99999999999999822, 2.946379043146343246, 75.11764819372150725 ) ) ;
#18820=SURFACE_STYLE_USAGE ( .BOTH. , #3909 ) ;
#18822=EDGE_CURVE ( 'NONE', #188, #46211, #25038, .T. ) ;
#18823=ORIENTED_EDGE ( 'NONE', *, *, #35475, .F. ) ;
#18828=CARTESIAN_POINT ( 'NONE',  ( 0.000000000000000000, -46.21855187248673502, 62.20884554314003623 ) ) ;
#18829=AXIS2_PLACEMENT_3D ( 'NONE', #46269, #38202, #46519 ) ;
#18833=VECTOR ( 'NONE', #38392, 1000.000000000000000 ) ;
#18835=CIRCLE ( 'NONE', #4774, 77.49899999999999523 ) ;
#18837=DIRECTION ( 'NONE',  ( 0.000000000000000000, 0.6494480483301849905, -0.7604059656000298206 ) ) ;
#18838=VERTEX_POINT ( 'NONE', #5891 ) ;
#18839=VERTEX_POINT ( 'NONE', #23748 ) ;
#18840=ORIENTED_EDGE ( 'NONE', *, *, #44791, .F. ) ;
#18848=DIRECTION ( 'NONE',  ( -1.000000000000000000, -0.000000000000000000, -0.000000000000000000 ) ) ;
#18854=CARTESIAN_POINT ( 'NONE',  ( 0.000000000000000000, -33.71516098798793593, 74.74816331893418919 ) ) ;
#18865=VECTOR ( 'NONE', #5768, 1000.000000000000000 ) ;
#18867=CARTESIAN_POINT ( 'NONE',  ( 50.00005079999999680, 2.571758278209441661E-15, -21.00000000000000000 ) ) ;
#18869=CYLINDRICAL_SURFACE ( 'NONE', #25269, 77.49899999999999523 ) ;
#18870=LINE ( 'NONE', #15232, #27308 ) ;
#18871=DIRECTION ( 'NONE',  ( -1.000000000000000000, 0.000000000000000000, 0.000000000000000000 ) ) ;
#18873=VERTEX_POINT ( 'NONE', #43332 ) ;
#18875=DIRECTION ( 'NONE',  ( -1.000000000000000000, -0.000000000000000000, 0.000000000000000000 ) ) ;
#18881=CARTESIAN_POINT ( 'NONE',  ( 0.000000000000000000, -26.02418014898260878, -70.52718814184285634 ) ) ;
#18884=LINE ( 'NONE', #32851, #42104 ) ;
#18885=EDGE_CURVE ( 'NONE', #37023, #35068, #19560, .T. ) ;
#18888=LINE ( 'NONE', #26735, #48046 ) ;
#18890=EDGE_CURVE ( 'NONE', #17899, #46621, #33629, .T. ) ;
#18899=ORIENTED_EDGE ( 'NONE', *, *, #32863, .F. ) ;
#18902=FACE_OUTER_BOUND ( 'NONE', #27058, .T. ) ;
#18903=CARTESIAN_POINT ( 'NONE',  ( 11.99999999999999822, 0.000000000000000000, 0.000000000000000000 ) ) ;
#18907=ORIENTED_EDGE ( 'NONE', *, *, #44755, .F. ) ;
#18910=CARTESIAN_POINT ( 'NONE',  ( 0.000000000000000000, 0.000000000000000000, 0.000000000000000000 ) ) ;
#18925=DIRECTION ( 'NONE',  ( 0.000000000000000000, 0.000000000000000000, 1.000000000000000000 ) ) ;
#18929=FACE_OUTER_BOUND ( 'NONE', #40494, .T. ) ;
#18931=FACE_OUTER_BOUND ( 'NONE', #29916, .T. ) ;
#18936=DIRECTION ( 'NONE',  ( -1.000000000000000000, 0.000000000000000000, 0.000000000000000000 ) ) ;
#18943=FACE_OUTER_BOUND ( 'NONE', #8867, .T. ) ;
#18946=VECTOR ( 'NONE', #41252, 1000.000000000000000 ) ;
#18948=CARTESIAN_POINT ( 'NONE',  ( 11.99999999999999822, 63.18004540533092239, -44.88180994100307686 ) ) ;
#18949=ORIENTED_EDGE ( 'NONE', *, *, #21316, .T. ) ;
#18952=AXIS2_PLACEMENT_3D ( 'NONE', #25184, #7317, #21533 ) ;
#18961=DIRECTION ( 'NONE',  ( 0.000000000000000000, -0.9723699203976740035, -0.2334453638559160216 ) ) ;
#18964=AXIS2_PLACEMENT_3D ( 'NONE', #16127, #17065, #16841 ) ;
#18965=VERTEX_POINT ( 'NONE', #29098 ) ;
#18967=CIRCLE ( 'NONE', #46351, 77.49899999999999523 ) ;
#18969=CARTESIAN_POINT ( 'NONE',  ( 0.000000000000000000, 75.11764819372142199, 2.946379043147685728 ) ) ;
#18978=CARTESIAN_POINT ( 'NONE',  ( 11.99999999999999822, 0.000000000000000000, 0.000000000000000000 ) ) ;
#18982=LINE ( 'NONE', #29767, #15119 ) ;
#18984=DIRECTION ( 'NONE',  ( 0.000000000000000000, 0.9969173337331281859, -0.07845909572784182107 ) ) ;
#18989=FACE_OUTER_BOUND ( 'NONE', #7604, .T. ) ;
#18993=EDGE_LOOP ( 'NONE', ( #6025, #36568, #6103, #13637 ) ) ;
#18994=CARTESIAN_POINT ( 'NONE',  ( 15.00000000000000000, 0.000000000000000000, 0.000000000000000000 ) ) ;
#18995=ORIENTED_EDGE ( 'NONE', *, *, #39174, .T. ) ;
#19001=EDGE_CURVE ( 'NONE', #19294, #38298, #17843, .T. ) ;
#19002=EDGE_CURVE ( 'NONE', #37684, #2082, #39132, .T. ) ;
#19005=FACE_OUTER_BOUND ( 'NONE', #40182, .T. ) ;
#19006=CARTESIAN_POINT ( 'NONE',  ( 12.00000000000000000, 8.688484142253932063, -21.88630264137371029 ) ) ;
#19007=EDGE_CURVE ( 'NONE', #39954, #11520, #47936, .T. ) ;
#19015=CYLINDRICAL_SURFACE ( 'NONE', #16722, 82.00000000000000000 ) ;
#19016=ORIENTED_EDGE ( 'NONE', *, *, #32285, .T. ) ;
#19017=CIRCLE ( 'NONE', #26160, 31.99999999999998934 ) ;
#19019=VECTOR ( 'NONE', #17366, 1000.000000000000000 ) ;
#19020=VERTEX_POINT ( 'NONE', #6363 ) ;
#19021=CIRCLE ( 'NONE', #17451, 82.00000000000000000 ) ;
#19030=AXIS2_PLACEMENT_3D ( 'NONE', #945, #41849, #8308 ) ;
#19031=DIRECTION ( 'NONE',  ( -1.000000000000000000, 0.000000000000000000, -0.000000000000000000 ) ) ;
#19032=CARTESIAN_POINT ( 'NONE',  ( 11.99999999999999822, 46.11716303203186840, 67.80270845531904911 ) ) ;
#19034=EDGE_CURVE ( 'NONE', #6091, #15795, #848, .T. ) ;
#19037=VERTEX_POINT ( 'NONE', #33264 ) ;
#19038=CYLINDRICAL_SURFACE ( 'NONE', #43943, 77.49899999999999523 ) ;
#19042=EDGE_CURVE ( 'NONE', #23167, #23653, #1637, .T. ) ;
#19045=EDGE_CURVE ( 'NONE', #24460, #1914, #18804, .T. ) ;
#19050=AXIS2_PLACEMENT_3D ( 'NONE', #12312, #23792, #38245 ) ;
#19053=VERTEX_POINT ( 'NONE', #13709 ) ;
#19055=CARTESIAN_POINT ( 'NONE',  ( 11.99999999999999822, 2.956366410621684260, -75.11725578898465017 ) ) ;
#19056=ORIENTED_EDGE ( 'NONE', *, *, #7535, .T. ) ;
#19059=DIRECTION ( 'NONE',  ( 0.000000000000000000, 0.000000000000000000, -1.000000000000000000 ) ) ;
#19065=AXIS2_PLACEMENT_3D ( 'NONE', #41937, #37762, #4245 ) ;
#19068=DIRECTION ( 'NONE',  ( 0.000000000000000000, 0.000000000000000000, -1.000000000000000000 ) ) ;
#19077=CIRCLE ( 'NONE', #33925, 31.99999999999998579 ) ;
#19080=AXIS2_PLACEMENT_3D ( 'NONE', #18910, #34321, #26283 ) ;
#19082=DIRECTION ( 'NONE',  ( 0.000000000000000000, 0.000000000000000000, 1.000000000000000000 ) ) ;
#19088=EDGE_LOOP ( 'NONE', ( #42889, #26892, #42727, #27302 ) ) ;
#19089=ORIENTED_EDGE ( 'NONE', *, *, #11887, .F. ) ;
#19090=ORIENTED_EDGE ( 'NONE', *, *, #32325, .F. ) ;
#19091=VERTEX_POINT ( 'NONE', #45480 ) ;
#19098=CARTESIAN_POINT ( 'NONE',  ( 6.000000000000000000, 78.73519480814955784, 22.90783923731656557 ) ) ;
#19101=DIRECTION ( 'NONE',  ( -1.000000000000000000, 0.000000000000000000, 0.000000000000000000 ) ) ;
#19105=MANIFOLD_SOLID_BREP ( 'CirPattern1', #10664 ) ;
#19109=AXIS2_PLACEMENT_3D ( 'NONE', #8821, #5900, #5405 ) ;
#19114=ORIENTED_EDGE ( 'NONE', *, *, #28071, .F. ) ;
#19115=CARTESIAN_POINT ( 'NONE',  ( 12.00000000000000000, -14.54903810567644484, 22.19967320028775504 ) ) ;
#19120=CARTESIAN_POINT ( 'NONE',  ( 11.99999999999999822, 11.30684508768339569, 76.66974797899841576 ) ) ;
#19132=DIRECTION ( 'NONE',  ( 0.000000000000000000, -0.4539904997395541875, 0.8910065241883641241 ) ) ;
#19134=VECTOR ( 'NONE', #24563, 1000.000000000000000 ) ;
#19136=DIRECTION ( 'NONE',  ( -1.000000000000000000, 0.000000000000000000, 0.000000000000000000 ) ) ;
#19140=AXIS2_PLACEMENT_3D ( 'NONE', #7736, #18515, #4071 ) ;
#19144=FACE_BOUND ( 'NONE', #8507, .T. ) ;
#19149=EDGE_LOOP ( 'NONE', ( #9704, #10013, #25581, #18995 ) ) ;
#19150=VECTOR ( 'NONE', #44654, 1000.000000000000000 ) ;
#19156=CARTESIAN_POINT ( 'NONE',  ( 0.000000000000000000, -65.59268652807183742, -36.72794159290312166 ) ) ;
#19163=EDGE_CURVE ( 'NONE', #3559, #10015, #45247, .T. ) ;
#19168=DIRECTION ( 'NONE',  ( -1.000000000000000000, 0.000000000000000000, 0.000000000000000000 ) ) ;
#19172=ORIENTED_EDGE ( 'NONE', *, *, #17712, .T. ) ;
#19174=CARTESIAN_POINT ( 'NONE',  ( 15.00000000000000000, 16.61724383029390140, 20.69703378468902955 ) ) ;
#19176=ORIENTED_EDGE ( 'NONE', *, *, #3861, .T. ) ;
#19179=DIRECTION ( 'NONE',  ( -1.000000000000000000, -0.000000000000000000, -0.000000000000000000 ) ) ;
#19184=FACE_OUTER_BOUND ( 'NONE', #29761, .T. ) ;
#19188=AXIS2_PLACEMENT_3D ( 'NONE', #6203, #39008, #5470 ) ;
#19189=CARTESIAN_POINT ( 'NONE',  ( 11.99999999999999822, -46.54456581323762521, -59.03342792756313884 ) ) ;
#19192=DIRECTION ( 'NONE',  ( 0.000000000000000000, -0.8090169943749433434, 0.5877852522924787992 ) ) ;
#19196=CARTESIAN_POINT ( 'NONE',  ( 11.99999999999999822, -36.73666225445940370, 65.58780272294062286 ) ) ;
#19197=EDGE_CURVE ( 'NONE', #9076, #42556, #35433, .T. ) ;
#19199=AXIS2_PLACEMENT_3D ( 'NONE', #24773, #20357, #24525 ) ;
#19205=AXIS2_PLACEMENT_3D ( 'NONE', #28275, #20942, #9671 ) ;
#19206=DIRECTION ( 'NONE',  ( 0.000000000000000000, 0.000000000000000000, -1.000000000000000000 ) ) ;
#19210=AXIS2_PLACEMENT_3D ( 'NONE', #20420, #12861, #46382 ) ;
#19212=VECTOR ( 'NONE', #18704, 1000.000000000000000 ) ;
#19213=ORIENTED_EDGE ( 'NONE', *, *, #3408, .F. ) ;
#19216=DIRECTION ( 'NONE',  ( 0.000000000000000000, 0.000000000000000000, 1.000000000000000000 ) ) ;
#19217=EDGE_CURVE ( 'NONE', #25968, #46297, #12689, .T. ) ;
#19219=CARTESIAN_POINT ( 'NONE',  ( 11.99999999999999822, -71.27951684758045303, 30.41916302227090085 ) ) ;
#19220=ORIENTED_EDGE ( 'NONE', *, *, #35819, .T. ) ;
#19225=EDGE_CURVE ( 'NONE', #4472, #20356, #36001, .T. ) ;
#19227=CARTESIAN_POINT ( 'NONE',  ( 11.99999999999999822, 72.35432306680455383, 20.40083707023012494 ) ) ;
#19231=VERTEX_POINT ( 'NONE', #20500 ) ;
#19234=ORIENTED_EDGE ( 'NONE', *, *, #12546, .T. ) ;
#19237=AXIS2_PLACEMENT_3D ( 'NONE', #11851, #26775, #41707 ) ;
#19239=FACE_OUTER_BOUND ( 'NONE', #15784, .T. ) ;
#19241=DIRECTION ( 'NONE',  ( 0.000000000000000000, -0.8526401643540860720, -0.5224985647159589019 ) ) ;
#19248=EDGE_LOOP ( 'NONE', ( #22757, #4288, #12896, #20874 ) ) ;
#19249=ORIENTED_EDGE ( 'NONE', *, *, #43215, .F. ) ;
#19255=DIRECTION ( 'NONE',  ( 0.000000000000000000, -0.07845909572783056618, -0.9969173337331290741 ) ) ;
#19261=ORIENTED_EDGE ( 'NONE', *, *, #25279, .F. ) ;
#19264=ORIENTED_EDGE ( 'NONE', *, *, #39972, .T. ) ;
#19265=AXIS2_PLACEMENT_3D ( 'NONE', #46288, #8360, #4460 ) ;
#19273=ORIENTED_EDGE ( 'NONE', *, *, #800, .F. ) ;
#19274=ORIENTED_EDGE ( 'NONE', *, *, #25529, .T. ) ;
#19276=ADVANCED_FACE ( 'NONE', ( #5348 ), #31797, .T. ) ;
#19283=DIRECTION ( 'NONE',  ( 0.000000000000000000, 0.4539904997395478037, -0.8910065241883673437 ) ) ;
#19293=ORIENTED_EDGE ( 'NONE', *, *, #26197, .T. ) ;
#19294=VERTEX_POINT ( 'NONE', #48140 ) ;
#19298=FACE_OUTER_BOUND ( 'NONE', #19788, .T. ) ;
#19299=ORIENTED_EDGE ( 'NONE', *, *, #46664, .F. ) ;
#19304=DIRECTION ( 'NONE',  ( 0.000000000000000000, 0.000000000000000000, 1.000000000000000000 ) ) ;
#19305=DIRECTION ( 'NONE',  ( 1.000000000000000000, 0.000000000000000000, -0.000000000000000000 ) ) ;
#19309=DIRECTION ( 'NONE',  ( -1.000000000000000000, 0.000000000000000000, -0.000000000000000000 ) ) ;
#19313=SHAPE_REPRESENTATION_RELATIONSHIP ( 'NONE' , 'NONE' ,  #37520, #20448 ) ;
#19314=CARTESIAN_POINT ( 'NONE',  ( 11.99999999999999822, 73.73191006444572793, -14.66109333815486515 ) ) ;
#19317=EDGE_CURVE ( 'NONE', #44556, #39373, #9971, .T. ) ;
#19323=EDGE_CURVE ( 'NONE', #42306, #24639, #11735, .T. ) ;
#19328=CARTESIAN_POINT ( 'NONE',  ( 15.00000000000000000, 0.000000000000000000, 0.000000000000000000 ) ) ;
#19330=ORIENTED_EDGE ( 'NONE', *, *, #62, .F. ) ;
#19335=CARTESIAN_POINT ( 'NONE',  ( 0.000000000000000000, -81.90746397400386059, -3.894527615418766242 ) ) ;
#19339=ORIENTED_EDGE ( 'NONE', *, *, #35044, .T. ) ;
#19340=CARTESIAN_POINT ( 'NONE',  ( 15.00000000000000000, 5.835314593368777558, 22.81335362449846471 ) ) ;
#19342=FACE_OUTER_BOUND ( 'NONE', #12716, .T. ) ;
#19347=EDGE_CURVE ( 'NONE', #8722, #15986, #28901, .T. ) ;
#19351=FACE_OUTER_BOUND ( 'NONE', #5455, .T. ) ;
#19363=FACE_OUTER_BOUND ( 'NONE', #4923, .T. ) ;
#19364=VERTEX_POINT ( 'NONE', #10206 ) ;
#19368=ORIENTED_EDGE ( 'NONE', *, *, #30974, .T. ) ;
#19371=CARTESIAN_POINT ( 'NONE',  ( 5.999999999999999112, -55.16347631942998930, -60.67117009219195722 ) ) ;
#19376=FACE_BOUND ( 'NONE', #37507, .T. ) ;
#19381=CYLINDRICAL_SURFACE ( 'NONE', #45575, 31.99999999999998579 ) ;
#19387=EDGE_CURVE ( 'NONE', #23803, #23034, #6253, .T. ) ;
#19389=DIRECTION ( 'NONE',  ( 0.000000000000000000, 0.000000000000000000, -1.000000000000000000 ) ) ;
#19390=DIRECTION ( 'NONE',  ( -1.000000000000000000, -0.000000000000000000, -0.000000000000000000 ) ) ;
#19398=DIRECTION ( 'NONE',  ( 0.000000000000000000, 0.000000000000000000, 1.000000000000000000 ) ) ;
#19401=ORIENTED_EDGE ( 'NONE', *, *, #29513, .F. ) ;
#19404=ORIENTED_EDGE ( 'NONE', *, *, #330, .T. ) ;
#19416=CARTESIAN_POINT ( 'NONE',  ( 15.00000000000000000, -0.9646360437375368635, -23.52805723605589705 ) ) ;
#19417=DIRECTION ( 'NONE',  ( 0.000000000000000000, 0.000000000000000000, 1.000000000000000000 ) ) ;
#19419=FACE_OUTER_BOUND ( 'NONE', #30729, .T. ) ;
#19425=CARTESIAN_POINT ( 'NONE',  ( 0.000000000000000000, 49.70050353004889132, 59.46389618801982380 ) ) ;
#19428=EDGE_CURVE ( 'NONE', #6106, #31086, #46118, .T. ) ;
#19431=ADVANCED_FACE ( 'NONE', ( #11906 ), #15572, .T. ) ;
#19434=ORIENTED_EDGE ( 'NONE', *, *, #21143, .F. ) ;
#19438=EDGE_CURVE ( 'NONE', #37652, #45656, #44956, .T. ) ;
#19439=AXIS2_PLACEMENT_3D ( 'NONE', #43354, #38964, #6144 ) ;
#19445=ORIENTED_EDGE ( 'NONE', *, *, #37094, .F. ) ;
#19446=CARTESIAN_POINT ( 'NONE',  ( 11.99999999999999822, 18.89407956138257205, 75.16055320797038064 ) ) ;
#19449=CARTESIAN_POINT ( 'NONE',  ( 11.99999999999999822, -71.21200624218766961, -40.65526001592688488 ) ) ;
#19452=EDGE_LOOP ( 'NONE', ( #2732, #36308, #2464, #40139 ) ) ;
#19456=CARTESIAN_POINT ( 'NONE',  ( 11.99999999999999822, 68.26794271651262136, 31.47745569255165066 ) ) ;
#19460=CARTESIAN_POINT ( 'NONE',  ( 11.99999999999999822, -55.20638768913797634, 51.02545421589302777 ) ) ;
#19461=CARTESIAN_POINT ( 'NONE',  ( 0.000000000000000000, 0.000000000000000000, 0.000000000000000000 ) ) ;
#19468=LINE ( 'NONE', #4801, #4043 ) ;
#19478=ORIENTED_EDGE ( 'NONE', *, *, #30462, .T. ) ;
#19480=CARTESIAN_POINT ( 'NONE',  ( -10.00000000000000000, 0.000000000000000000, 0.000000000000000000 ) ) ;
#19481=ADVANCED_FACE ( 'NONE', ( #41766 ), #8229, .F. ) ;
#19496=DIRECTION ( 'NONE',  ( -1.000000000000000000, -0.000000000000000000, -0.000000000000000000 ) ) ;
#19499=LINE ( 'NONE', #34433, #27287 ) ;
#19500=CARTESIAN_POINT ( 'NONE',  ( 11.99999999999999822, 0.000000000000000000, 0.000000000000000000 ) ) ;
#19501=ADVANCED_FACE ( 'NONE', ( #16788 ), #22192, .T. ) ;
#19503=VERTEX_POINT ( 'NONE', #8694 ) ;
#19504=CARTESIAN_POINT ( 'NONE',  ( 11.99999999999999822, 10.30890764327382136, 81.34940948281339956 ) ) ;
#19508=DIRECTION ( 'NONE',  ( -1.000000000000000000, -0.000000000000000000, -0.000000000000000000 ) ) ;
#19509=VERTEX_POINT ( 'NONE', #24129 ) ;
#19512=ORIENTED_EDGE ( 'NONE', *, *, #41658, .T. ) ;
#19513=ORIENTED_EDGE ( 'NONE', *, *, #25412, .T. ) ;
#19526=CYLINDRICAL_SURFACE ( 'NONE', #17191, 31.99999999999998579 ) ;
#19527=CIRCLE ( 'NONE', #7838, 77.49899999999999523 ) ;
#19531=CIRCLE ( 'NONE', #34383, 77.49900000000000944 ) ;
#19532=LINE ( 'NONE', #31817, #20724 ) ;
#19533=EDGE_CURVE ( 'NONE', #18873, #22722, #4798, .T. ) ;
#19538=DIRECTION ( 'NONE',  ( 0.000000000000000000, 0.2334453638559060851, -0.9723699203976764460 ) ) ;
#19543=ORIENTED_EDGE ( 'NONE', *, *, #19751, .T. ) ;
#19547=VERTEX_POINT ( 'NONE', #27559 ) ;
#19550=PLANE ( 'NONE',  #32804 ) ;
#19556=ORIENTED_EDGE ( 'NONE', *, *, #33368, .T. ) ;
#19560=CIRCLE ( 'NONE', #13343, 82.00000000000000000 ) ;
#19565=VERTEX_POINT ( 'NONE', #24355 ) ;
#19568=ORIENTED_EDGE ( 'NONE', *, *, #17582, .F. ) ;
#19575=DIRECTION ( 'NONE',  ( -1.000000000000000000, 0.000000000000000000, -0.000000000000000000 ) ) ;
#19576=VERTEX_POINT ( 'NONE', #35374 ) ;
#19582=CARTESIAN_POINT ( 'NONE',  ( 11.99999999999999822, 0.000000000000000000, 0.000000000000000000 ) ) ;
#19588=AXIS2_PLACEMENT_3D ( 'NONE', #30450, #22855, #3278 ) ;
#19593=VERTEX_POINT ( 'NONE', #46887 ) ;
#19598=CARTESIAN_POINT ( 'NONE',  ( 0.000000000000000000, -73.72996012237449293, 14.67089635893687571 ) ) ;
#19601=DIRECTION ( 'NONE',  ( -1.000000000000000000, -0.000000000000000000, -0.000000000000000000 ) ) ;
#19606=AXIS2_PLACEMENT_3D ( 'NONE', #25731, #40672, #7631 ) ;
#19608=FACE_BOUND ( 'NONE', #14029, .T. ) ;
#19615=ORIENTED_EDGE ( 'NONE', *, *, #5690, .F. ) ;
#19617=DIRECTION ( 'NONE',  ( 0.000000000000000000, 0.000000000000000000, 1.000000000000000000 ) ) ;
#19621=CARTESIAN_POINT ( 'NONE',  ( 0.000000000000000000, -2.956366410620109519, -75.11725578898472122 ) ) ;
#19624=LINE ( 'NONE', #16231, #18358 ) ;
#19630=DIRECTION ( 'NONE',  ( 0.000000000000000000, 0.000000000000000000, 1.000000000000000000 ) ) ;
#19633=DIRECTION ( 'NONE',  ( -1.000000000000000000, 0.000000000000000000, 0.000000000000000000 ) ) ;
#19637=CARTESIAN_POINT ( 'NONE',  ( 11.99999999999999822, 68.67312586194995561, 35.91791733033500122 ) ) ;
#19638=ORIENTED_EDGE ( 'NONE', *, *, #11724, .F. ) ;
#19642=AXIS2_PLACEMENT_3D ( 'NONE', #31841, #16642, #34755 ) ;
#19643=ADVANCED_FACE ( 'NONE', ( #47588 ), #2325, .T. ) ;
#19645=DIRECTION ( 'NONE',  ( -1.000000000000000000, -0.000000000000000000, -0.000000000000000000 ) ) ;
#19649=ADVANCED_FACE ( 'NONE', ( #28762 ), #6487, .T. ) ;
#19652=DIRECTION ( 'NONE',  ( -1.000000000000000000, -0.000000000000000000, -0.000000000000000000 ) ) ;
#19654=CARTESIAN_POINT ( 'NONE',  ( 12.00000000000000000, -19.89357724624986545, 12.59942793731086219 ) ) ;
#19661=EDGE_CURVE ( 'NONE', #14617, #35941, #28989, .T. ) ;
#19662=VERTEX_POINT ( 'NONE', #39555 ) ;
#19664=DIRECTION ( 'NONE',  ( 1.000000000000000000, 0.000000000000000000, -0.000000000000000000 ) ) ;
#19666=ORIENTED_EDGE ( 'NONE', *, *, #4100, .T. ) ;
#19669=AXIS2_PLACEMENT_3D ( 'NONE', #45374, #8178, #38047 ) ;
#19671=AXIS2_PLACEMENT_3D ( 'NONE', #25796, #17968, #29246 ) ;
#19672=ORIENTED_EDGE ( 'NONE', *, *, #26993, .F. ) ;
#19678=FACE_OUTER_BOUND ( 'NONE', #7381, .T. ) ;
#19679=DIRECTION ( 'NONE',  ( 1.000000000000000000, 0.000000000000000000, 0.000000000000000000 ) ) ;
#19680=DIRECTION ( 'NONE',  ( 0.000000000000000000, 0.000000000000000000, 1.000000000000000000 ) ) ;
#19686=DIRECTION ( 'NONE',  ( 0.000000000000000000, -0.8090169943749426773, 0.5877852522924796874 ) ) ;
#19690=EDGE_LOOP ( 'NONE', ( #39116, #1367, #12718, #33132 ) ) ;
#19692=CARTESIAN_POINT ( 'NONE',  ( 0.000000000000000000, -66.50666863321973210, -39.78640506895674633 ) ) ;
#19695=CARTESIAN_POINT ( 'NONE',  ( 11.99999999999999822, 0.000000000000000000, 0.000000000000000000 ) ) ;
#19699=DIRECTION ( 'NONE',  ( -1.000000000000000000, -0.000000000000000000, -0.000000000000000000 ) ) ;
#19700=DIRECTION ( 'NONE',  ( -1.000000000000000000, -0.000000000000000000, 0.000000000000000000 ) ) ;
#19711=VECTOR ( 'NONE', #17037, 1000.000000000000114 ) ;
#19712=DIRECTION ( 'NONE',  ( 1.000000000000000000, -0.000000000000000000, -0.000000000000000000 ) ) ;
#19716=ADVANCED_FACE ( 'NONE', ( #34804 ), #42400, .T. ) ;
#19720=CARTESIAN_POINT ( 'NONE',  ( 11.99999999999999822, -68.27212725128254078, -31.46837873495049465 ) ) ;
#19721=EDGE_CURVE ( 'NONE', #16137, #37878, #16451, .T. ) ;
#19728=CIRCLE ( 'NONE', #2543, 77.49900000000000944 ) ;
#19732=ORIENTED_EDGE ( 'NONE', *, *, #38834, .T. ) ;
#19733=AXIS2_PLACEMENT_3D ( 'NONE', #38042, #7690, #22617 ) ;
#19737=DIRECTION ( 'NONE',  ( -1.000000000000000000, 0.000000000000000000, 0.000000000000000000 ) ) ;
#19738=AXIS2_PLACEMENT_3D ( 'NONE', #33115, #48284, #7166 ) ;
#19741=ORIENTED_EDGE ( 'NONE', *, *, #10966, .T. ) ;
#19747=VERTEX_POINT ( 'NONE', #16698 ) ;
#19749=ORIENTED_EDGE ( 'NONE', *, *, #45586, .T. ) ;
#19751=EDGE_CURVE ( 'NONE', #7167, #44170, #28947, .T. ) ;
#19755=EDGE_CURVE ( 'NONE', #23468, #11531, #40645, .T. ) ;
#19757=DIRECTION ( 'NONE',  ( -1.000000000000000000, 0.000000000000000000, 0.000000000000000000 ) ) ;
#19759=DIRECTION ( 'NONE',  ( 0.000000000000000000, 0.2079116908177664758, 0.9781476007338042455 ) ) ;
#19760=EDGE_LOOP ( 'NONE', ( #10481, #9754, #4648, #17983 ) ) ;
#19761=EDGE_CURVE ( 'NONE', #42120, #43790, #29715, .T. ) ;
#19763=CIRCLE ( 'NONE', #6506, 31.99999999999998224 ) ;
#19766=CARTESIAN_POINT ( 'NONE',  ( 5.999999999999999112, 74.74816331893477184, -33.71516098798660011 ) ) ;
#19767=EDGE_LOOP ( 'NONE', ( #36780, #47666, #8487, #7308 ) ) ;
#19768=EDGE_CURVE ( 'NONE', #43334, #41271, #19527, .T. ) ;
#19771=ORIENTED_EDGE ( 'NONE', *, *, #31691, .T. ) ;
#19776=DIRECTION ( 'NONE',  ( -1.000000000000000000, -0.000000000000000000, -0.000000000000000000 ) ) ;
#19779=AXIS2_PLACEMENT_3D ( 'NONE', #45750, #12229, #27154 ) ;
#19781=CARTESIAN_POINT ( 'NONE',  ( 0.000000000000000000, 0.000000000000000000, 0.000000000000000000 ) ) ;
#19784=CARTESIAN_POINT ( 'NONE',  ( 11.99999999999999822, -70.53064760720336324, 26.01480285779810231 ) ) ;
#19788=EDGE_LOOP ( 'NONE', ( #23533, #19615, #20899, #13447 ) ) ;
#19792=ORIENTED_EDGE ( 'NONE', *, *, #25945, .T. ) ;
#19798=DIRECTION ( 'NONE',  ( 0.000000000000000000, 0.4067366430758010409, 0.9135454576426005335 ) ) ;
#19801=ORIENTED_EDGE ( 'NONE', *, *, #1164, .F. ) ;
#19813=EDGE_CURVE ( 'NONE', #45628, #45301, #10960, .T. ) ;
#19814=DIRECTION ( 'NONE',  ( -1.000000000000000000, -0.000000000000000000, 0.000000000000000000 ) ) ;
#19816=CARTESIAN_POINT ( 'NONE',  ( 12.00000000000000000, -26.23277895567245466, 4.042438405570107030 ) ) ;
#19819=CIRCLE ( 'NONE', #13586, 77.49899999999999523 ) ;
#19821=CARTESIAN_POINT ( 'NONE',  ( 0.000000000000000000, -75.54627589209931671, -17.28742895386162814 ) ) ;
#19831=DIRECTION ( 'NONE',  ( -1.000000000000000000, 0.000000000000000000, -0.000000000000000000 ) ) ;
#19832=ORIENTED_EDGE ( 'NONE', *, *, #20947, .F. ) ;
#19833=CYLINDRICAL_SURFACE ( 'NONE', #11305, 21.00000000000000000 ) ;
#19835=DIRECTION ( 'NONE',  ( 0.000000000000000000, 0.000000000000000000, 1.000000000000000000 ) ) ;
#19836=DIRECTION ( 'NONE',  ( 0.000000000000000000, 0.000000000000000000, -1.000000000000000000 ) ) ;
#19842=CARTESIAN_POINT ( 'NONE',  ( 11.99999999999999822, -55.16347631943085617, 60.67117009219116852 ) ) ;
#19844=CIRCLE ( 'NONE', #25327, 31.99999999999998579 ) ;
#19852=ORIENTED_EDGE ( 'NONE', *, *, #35136, .T. ) ;
#19853=CIRCLE ( 'NONE', #46469, 82.00000000000000000 ) ;
#19865=CARTESIAN_POINT ( 'NONE',  ( 11.99999999999999822, 0.000000000000000000, 0.000000000000000000 ) ) ;
#19869=ORIENTED_EDGE ( 'NONE', *, *, #5429, .F. ) ;
#19876=DIRECTION ( 'NONE',  ( -1.000000000000000000, -0.000000000000000000, -0.000000000000000000 ) ) ;
#19879=CARTESIAN_POINT ( 'NONE',  ( 15.00000000000000000, 23.49999999999999645, 1.499999999999995337 ) ) ;
#19884=AXIS2_PLACEMENT_3D ( 'NONE', #47401, #1902, #43245 ) ;
#19889=ORIENTED_EDGE ( 'NONE', *, *, #41491, .T. ) ;
#19892=CARTESIAN_POINT ( 'NONE',  ( 11.99999999999999822, 0.000000000000000000, 0.000000000000000000 ) ) ;
#19896=VECTOR ( 'NONE', #9792, 1000.000000000000000 ) ;
#19902=AXIS2_PLACEMENT_3D ( 'NONE', #18978, #48367, #22664 ) ;
#19903=DIRECTION ( 'NONE',  ( -1.000000000000000000, 0.000000000000000000, 0.000000000000000000 ) ) ;
#19908=CARTESIAN_POINT ( 'NONE',  ( 12.00000000000000000, 24.81905959214260804, -9.408202855044827118 ) ) ;
#19919=CARTESIAN_POINT ( 'NONE',  ( 0.000000000000000000, -44.88180994100329713, -63.18004540533077318 ) ) ;
#19920=VECTOR ( 'NONE', #17960, 1000.000000000000000 ) ;
#19924=CIRCLE ( 'NONE', #45726, 77.49899999999999523 ) ;
#19932=AXIS2_PLACEMENT_3D ( 'NONE', #33203, #10930, #25842 ) ;
#19933=AXIS2_PLACEMENT_3D ( 'NONE', #11040, #10569, #33316 ) ;
#19947=VECTOR ( 'NONE', #36528, 1000.000000000000000 ) ;
#19954=DIRECTION ( 'NONE',  ( 0.000000000000000000, 0.000000000000000000, 1.000000000000000000 ) ) ;
#19959=CARTESIAN_POINT ( 'NONE',  ( 11.99999999999999822, -22.90783923731685334, 78.73519480814947258 ) ) ;
#19964=CARTESIAN_POINT ( 'NONE',  ( 0.000000000000000000, 36.73666225445988687, -65.58780272294035285 ) ) ;
#19966=VECTOR ( 'NONE', #42407, 1000.000000000000000 ) ;
#19968=ORIENTED_EDGE ( 'NONE', *, *, #34104, .F. ) ;
#19971=AXIS2_PLACEMENT_3D ( 'NONE', #10883, #37550, #25797 ) ;
#19972=CYLINDRICAL_SURFACE ( 'NONE', #40248, 31.99999999999999289 ) ;
#19980=DIRECTION ( 'NONE',  ( -1.000000000000000000, 0.000000000000000000, 0.000000000000000000 ) ) ;
#19982=ORIENTED_EDGE ( 'NONE', *, *, #30978, .F. ) ;
#19983=VERTEX_POINT ( 'NONE', #7854 ) ;
#19989=EDGE_CURVE ( 'NONE', #13555, #6779, #47725, .T. ) ;
#19990=ADVANCED_FACE ( 'NONE', ( #15454 ), #18630, .T. ) ;
#19996=CARTESIAN_POINT ( 'NONE',  ( 11.99999999999999822, -39.78640506895559525, -66.50666863322042843 ) ) ;
#19998=ORIENTED_EDGE ( 'NONE', *, *, #17382, .T. ) ;
#20000=AXIS2_PLACEMENT_3D ( 'NONE', #12565, #27502, #36029 ) ;
#20002=ADVANCED_FACE ( 'NONE', ( #37234 ), #33560, .F. ) ;
#20003=FACE_OUTER_BOUND ( 'NONE', #3298, .T. ) ;
#20004=DIRECTION ( 'NONE',  ( 0.000000000000000000, 0.000000000000000000, 1.000000000000000000 ) ) ;
#20008=VERTEX_POINT ( 'NONE', #26466 ) ;
#20010=LINE ( 'NONE', #16120, #45058 ) ;
#20015=DIRECTION ( 'NONE',  ( -1.000000000000000000, -0.000000000000000000, -0.000000000000000000 ) ) ;
#20016=VERTEX_POINT ( 'NONE', #4446 ) ;
#20024=ADVANCED_FACE ( 'NONE', ( #19351 ), #47999, .T. ) ;
#20026=DIRECTION ( 'NONE',  ( -1.000000000000000000, 0.000000000000000000, -0.000000000000000000 ) ) ;
#20027=VERTEX_POINT ( 'NONE', #19 ) ;
#20031=DIRECTION ( 'NONE',  ( -1.000000000000000000, -0.000000000000000000, 0.000000000000000000 ) ) ;
#20037=AXIS2_PLACEMENT_3D ( 'NONE', #11706, #34687, #4845 ) ;
#20043=ORIENTED_EDGE ( 'NONE', *, *, #14729, .T. ) ;
#20044=VECTOR ( 'NONE', #39849, 1000.000000000000000 ) ;
#20048=DIRECTION ( 'NONE',  ( -1.000000000000000000, -0.000000000000000000, -0.000000000000000000 ) ) ;
#20052=VERTEX_POINT ( 'NONE', #26958 ) ;
#20056=EDGE_LOOP ( 'NONE', ( #39333, #9955, #12983, #44553 ) ) ;
#20065=AXIS2_PLACEMENT_3D ( 'NONE', #136, #41279, #44455 ) ;
#20081=ADVANCED_FACE ( 'NONE', ( #8811 ), #27196, .T. ) ;
#20082=CARTESIAN_POINT ( 'NONE',  ( 11.99999999999999822, 68.27212725128275395, -31.46837873495001503 ) ) ;
#20087=CYLINDRICAL_SURFACE ( 'NONE', #28370, 82.00000000000000000 ) ;
#20088=DIRECTION ( 'NONE',  ( 0.000000000000000000, 0.000000000000000000, 1.000000000000000000 ) ) ;
#20092=FACE_OUTER_BOUND ( 'NONE', #24867, .T. ) ;
#20093=AXIS2_PLACEMENT_3D ( 'NONE', #25088, #2569, #6742 ) ;
#20094=LINE ( 'NONE', #32320, #6238 ) ;
#20098=EDGE_CURVE ( 'NONE', #17381, #37423, #25056, .T. ) ;
#20099=DIRECTION ( 'NONE',  ( 0.000000000000000000, 0.8910065241883690090, -0.4539904997395446395 ) ) ;
#20103=DIRECTION ( 'NONE',  ( 0.000000000000000000, 0.4999999999999938938, -0.8660254037844421493 ) ) ;
#20104=DIRECTION ( 'NONE',  ( -1.000000000000000000, 0.000000000000000000, 0.000000000000000000 ) ) ;
#20106=VERTEX_POINT ( 'NONE', #42610 ) ;
#20119=CIRCLE ( 'NONE', #24808, 31.99999999999998579 ) ;
#20122=EDGE_LOOP ( 'NONE', ( #30241, #38421, #17841, #40074 ) ) ;
#20125=CARTESIAN_POINT ( 'NONE',  ( 11.99999999999999822, 0.000000000000000000, 0.000000000000000000 ) ) ;
#20132=CYLINDRICAL_SURFACE ( 'NONE', #43134, 31.99999999999998579 ) ;
#20133=ORIENTED_EDGE ( 'NONE', *, *, #8328, .T. ) ;
#20138=DIRECTION ( 'NONE',  ( 0.000000000000000000, 0.000000000000000000, -1.000000000000000000 ) ) ;
#20140=PLANE ( 'NONE',  #23251 ) ;
#20143=DIRECTION ( 'NONE',  ( 0.000000000000000000, 0.000000000000000000, -1.000000000000000000 ) ) ;
#20146=DIRECTION ( 'NONE',  ( -1.000000000000000000, 0.000000000000000000, -0.000000000000000000 ) ) ;
#20148=FACE_OUTER_BOUND ( 'NONE', #21496, .T. ) ;
#20154=CYLINDRICAL_SURFACE ( 'NONE', #2068, 31.99999999999998579 ) ;
#20155=LINE ( 'NONE', #39741, #20729 ) ;
#20157=DIRECTION ( 'NONE',  ( -1.000000000000000000, 0.000000000000000000, -0.000000000000000000 ) ) ;
#20174=EDGE_LOOP ( 'NONE', ( #37184, #38513, #10817, #25152 ) ) ;
#20175=VECTOR ( 'NONE', #34538, 1000.000000000000000 ) ;
#20177=EDGE_CURVE ( 'NONE', #33371, #3949, #42264, .T. ) ;
#20178=ORIENTED_EDGE ( 'NONE', *, *, #13150, .F. ) ;
#20180=ORIENTED_EDGE ( 'NONE', *, *, #17227, .T. ) ;
#20181=LINE ( 'NONE', #5740, #12787 ) ;
#20182=CARTESIAN_POINT ( 'NONE',  ( 0.000000000000000000, 31.46837873495072913, -68.27212725128242710 ) ) ;
#20184=VERTEX_POINT ( 'NONE', #36209 ) ;
#20185=ADVANCED_FACE ( 'NONE', ( #43567 ), #35735, .T. ) ;
#20186=ORIENTED_EDGE ( 'NONE', *, *, #21965, .T. ) ;
#20189=ORIENTED_EDGE ( 'NONE', *, *, #39317, .T. ) ;
#20193=AXIS2_PLACEMENT_3D ( 'NONE', #12387, #34163, #636 ) ;
#20195=ORIENTED_EDGE ( 'NONE', *, *, #19721, .T. ) ;
#20198=CARTESIAN_POINT ( 'NONE',  ( 11.99999999999999822, 0.000000000000000000, 0.000000000000000000 ) ) ;
#20199=CARTESIAN_POINT ( 'NONE',  ( 0.000000000000000000, 18.89407956138257205, 75.16055320797038064 ) ) ;
#20200=CARTESIAN_POINT ( 'NONE',  ( 11.99999999999999822, 0.000000000000000000, 0.000000000000000000 ) ) ;
#20201=CARTESIAN_POINT ( 'NONE',  ( 11.99999999999999822, 58.39081064771751528, 50.95692526931350841 ) ) ;
#20205=ORIENTED_EDGE ( 'NONE', *, *, #520, .F. ) ;
#20211=ORIENTED_EDGE ( 'NONE', *, *, #27581, .T. ) ;
#20213=EDGE_CURVE ( 'NONE', #37878, #44222, #21978, .T. ) ;
#20215=DIRECTION ( 'NONE',  ( -1.000000000000000000, 0.000000000000000000, 0.000000000000000000 ) ) ;
#20219=DIRECTION ( 'NONE',  ( -1.000000000000000000, -0.000000000000000000, -0.000000000000000000 ) ) ;
#20223=VERTEX_POINT ( 'NONE', #21271 ) ;
#20228=CARTESIAN_POINT ( 'NONE',  ( 15.00000000000000000, -20.55727247249748402, -16.78983467731284307 ) ) ;
#20231=ORIENTED_EDGE ( 'NONE', *, *, #6854, .T. ) ;
#20232=VECTOR ( 'NONE', #31628, 1000.000000000000114 ) ;
#20237=ORIENTED_EDGE ( 'NONE', *, *, #40398, .F. ) ;
#20245=ORIENTED_EDGE ( 'NONE', *, *, #5360, .T. ) ;
#20247=CARTESIAN_POINT ( 'NONE',  ( 0.000000000000000000, -6.903761155838323837, 77.19088730480521576 ) ) ;
#20251=DIRECTION ( 'NONE',  ( 0.000000000000000000, 0.000000000000000000, 1.000000000000000000 ) ) ;
#20255=ORIENTED_EDGE ( 'NONE', *, *, #5950, .F. ) ;
#20258=CARTESIAN_POINT ( 'NONE',  ( 11.99999999999999822, 0.000000000000000000, 0.000000000000000000 ) ) ;
#20261=ADVANCED_FACE ( 'NONE', ( #10260 ), #21530, .F. ) ;
#20264=EDGE_CURVE ( 'NONE', #3749, #25146, #32077, .T. ) ;
#20271=CARTESIAN_POINT ( 'NONE',  ( 0.000000000000000000, -46.21855187248585395, -62.20884554314068993 ) ) ;
#20273=EDGE_CURVE ( 'NONE', #21915, #15144, #16896, .T. ) ;
#20274=ORIENTED_EDGE ( 'NONE', *, *, #6913, .F. ) ;
#20278=AXIS2_PLACEMENT_3D ( 'NONE', #35161, #20473, #12665 ) ;
#20289=EDGE_CURVE ( 'NONE', #18512, #7570, #20553, .T. ) ;
#20294=CIRCLE ( 'NONE', #11719, 82.00000000000000000 ) ;
#20298=EDGE_LOOP ( 'NONE', ( #16775, #32897, #42550, #34916 ) ) ;
#20302=ORIENTED_EDGE ( 'NONE', *, *, #13704, .F. ) ;
#20313=DIRECTION ( 'NONE',  ( -1.000000000000000000, -0.000000000000000000, 0.000000000000000000 ) ) ;
#20321=CARTESIAN_POINT ( 'NONE',  ( 11.99999999999999822, -31.47745569255189224, 68.26794271651249346 ) ) ;
#20325=CARTESIAN_POINT ( 'NONE',  ( 11.99999999999999822, 35.91791733033570466, -68.67312586194960033 ) ) ;
#20326=DIRECTION ( 'NONE',  ( -1.000000000000000000, -0.000000000000000000, 0.000000000000000000 ) ) ;
#20327=VERTEX_POINT ( 'NONE', #3148 ) ;
#20329=LINE ( 'NONE', #35986, #14413 ) ;
#20330=DIRECTION ( 'NONE',  ( -1.000000000000000000, -0.000000000000000000, -0.000000000000000000 ) ) ;
#20331=CARTESIAN_POINT ( 'NONE',  ( 15.00000000000000000, 0.000000000000000000, 0.000000000000000000 ) ) ;
#20333=ADVANCED_FACE ( 'NONE', ( #18077 ), #45249, .T. ) ;
#20336=CARTESIAN_POINT ( 'NONE',  ( 15.00000000000000000, -19.89357724624986545, 12.59942793731086219 ) ) ;
#20339=LINE ( 'NONE', #31393, #10373 ) ;
#20341=VECTOR ( 'NONE', #35230, 1000.000000000000000 ) ;
#20344=AXIS2_PLACEMENT_3D ( 'NONE', #2557, #47373, #36341 ) ;
#20345=VECTOR ( 'NONE', #272, 1000.000000000000000 ) ;
#20354=CYLINDRICAL_SURFACE ( 'NONE', #35491, 82.00000000000000000 ) ;
#20356=VERTEX_POINT ( 'NONE', #29357 ) ;
#20357=DIRECTION ( 'NONE',  ( 1.000000000000000000, 0.000000000000000000, 0.000000000000000000 ) ) ;
#20359=VERTEX_POINT ( 'NONE', #22728 ) ;
#20365=DIRECTION ( 'NONE',  ( 1.000000000000000000, 0.000000000000000000, 0.000000000000000000 ) ) ;
#20366=VERTEX_POINT ( 'NONE', #3888 ) ;
#20373=ORIENTED_EDGE ( 'NONE', *, *, #16636, .F. ) ;
#20375=DIRECTION ( 'NONE',  ( -1.000000000000000000, 0.000000000000000000, 0.000000000000000000 ) ) ;
#20380=LINE ( 'NONE', #13529, #23710 ) ;
#20387=DIRECTION ( 'NONE',  ( 0.000000000000000000, -0.1564344650402170744, -0.9876883405951398798 ) ) ;
#20388=CARTESIAN_POINT ( 'NONE',  ( 15.00000000000000000, 26.49999999999999645, 1.499999999999995781 ) ) ;
#20390=CARTESIAN_POINT ( 'NONE',  ( 11.99999999999999822, 0.000000000000000000, 0.000000000000000000 ) ) ;
#20396=ORIENTED_EDGE ( 'NONE', *, *, #23252, .F. ) ;
#20402=AXIS2_PLACEMENT_3D ( 'NONE', #21033, #2915, #2427 ) ;
#20407=ORIENTED_EDGE ( 'NONE', *, *, #9291, .T. ) ;
#20409=ORIENTED_EDGE ( 'NONE', *, *, #38852, .T. ) ;
#20412=DIRECTION ( 'NONE',  ( 0.000000000000000000, -0.9945218953682732899, 0.1045284632676548031 ) ) ;
#20414=CARTESIAN_POINT ( 'NONE',  ( 0.000000000000000000, 0.000000000000000000, 0.000000000000000000 ) ) ;
#20415=CIRCLE ( 'NONE', #47773, 77.49900000000000944 ) ;
#20417=DIRECTION ( 'NONE',  ( -1.000000000000000000, -0.000000000000000000, -0.000000000000000000 ) ) ;
#20419=FACE_OUTER_BOUND ( 'NONE', #25528, .T. ) ;
#20420=CARTESIAN_POINT ( 'NONE',  ( 0.000000000000000000, -41.76106447765443619, -62.50884508063471401 ) ) ;
#20424=EDGE_LOOP ( 'NONE', ( #11242, #4422, #25353, #39272 ) ) ;
#20427=ORIENTED_EDGE ( 'NONE', *, *, #19755, .T. ) ;
#20428=ADVANCED_FACE ( 'NONE', ( #22255 ), #37178, .F. ) ;
#20433=PLANE ( 'NONE',  #40686 ) ;
#20442=FACE_OUTER_BOUND ( 'NONE', #21745, .T. ) ;
#20447=CIRCLE ( 'NONE', #37676, 31.99999999999998579 ) ;
#20448=ADVANCED_BREP_SHAPE_REPRESENTATION ( '', ( #19105, #11636 ), #21023 ) ;
#20452=AXIS2_PLACEMENT_3D ( 'NONE', #38524, #24081, #5716 ) ;
#20455=DIRECTION ( 'NONE',  ( 0.000000000000000000, 0.7604059656000322631, -0.6494480483301821039 ) ) ;
#20457=PLANE ( 'NONE',  #44105 ) ;
#20458=ORIENTED_EDGE ( 'NONE', *, *, #15103, .F. ) ;
#20464=ORIENTED_EDGE ( 'NONE', *, *, #11947, .T. ) ;
#20469=ORIENTED_EDGE ( 'NONE', *, *, #13594, .F. ) ;
#20471=AXIS2_PLACEMENT_3D ( 'NONE', #5299, #20215, #35137 ) ;
#20473=DIRECTION ( 'NONE',  ( -1.000000000000000000, 0.000000000000000000, 0.000000000000000000 ) ) ;
#20474=VECTOR ( 'NONE', #25174, 1000.000000000000000 ) ;
#20479=CIRCLE ( 'NONE', #26747, 31.99999999999998579 ) ;
#20484=EDGE_LOOP ( 'NONE', ( #46254, #1109, #22771, #14399 ) ) ;
#20487=EDGE_LOOP ( 'NONE', ( #6533, #37584, #38427, #31868 ) ) ;
#20488=VERTEX_POINT ( 'NONE', #27145 ) ;
#20489=DIRECTION ( 'NONE',  ( 0.000000000000000000, 0.000000000000000000, 1.000000000000000000 ) ) ;
#20490=CARTESIAN_POINT ( 'NONE',  ( 11.99999999999999822, 0.000000000000000000, 0.000000000000000000 ) ) ;
#20494=EDGE_CURVE ( 'NONE', #44222, #40154, #12452, .T. ) ;
#20495=DIRECTION ( 'NONE',  ( 0.000000000000000000, -0.7431448254773938000, -0.6691306063588585706 ) ) ;
#20499=VERTEX_POINT ( 'NONE', #23693 ) ;
#20500=CARTESIAN_POINT ( 'NONE',  ( 11.99999999999999822, -21.60688246758642705, 79.10210256391358996 ) ) ;
#20503=DIRECTION ( 'NONE',  ( 0.000000000000000000, -0.8910065241883626808, -0.4539904997395569075 ) ) ;
#20505=VERTEX_POINT ( 'NONE', #12942 ) ;
#20507=DIRECTION ( 'NONE',  ( 0.000000000000000000, 0.000000000000000000, 1.000000000000000000 ) ) ;
#20514=AXIS2_PLACEMENT_3D ( 'NONE', #11076, #18153, #22075 ) ;
#20520=AXIS2_PLACEMENT_3D ( 'NONE', #20258, #24180, #12686 ) ;
#20521=CARTESIAN_POINT ( 'NONE',  ( 0.000000000000000000, -34.94270380257692921, 74.18225833017875459 ) ) ;
#20525=ORIENTED_EDGE ( 'NONE', *, *, #30845, .T. ) ;
#20526=VECTOR ( 'NONE', #35393, 1000.000000000000000 ) ;
#20530=EDGE_CURVE ( 'NONE', #1080, #36243, #23954, .T. ) ;
#20531=CARTESIAN_POINT ( 'NONE',  ( -10.00000000000000000, 0.000000000000000000, 0.000000000000000000 ) ) ;
#20539=CARTESIAN_POINT ( 'NONE',  ( 0.000000000000000000, 26.01480285779933510, -70.53064760720289428 ) ) ;
#20542=VERTEX_POINT ( 'NONE', #41829 ) ;
#20545=CARTESIAN_POINT ( 'NONE',  ( 11.99999999999999822, 0.000000000000000000, 0.000000000000000000 ) ) ;
#20547=ORIENTED_EDGE ( 'NONE', *, *, #37459, .F. ) ;
#20553=LINE ( 'NONE', #13227, #6347 ) ;
#20562=DIRECTION ( 'NONE',  ( 0.000000000000000000, 0.9945218953682732899, -0.1045284632676548031 ) ) ;
#20564=CARTESIAN_POINT ( 'NONE',  ( 11.99999999999999822, -26.02418014898359289, 70.52718814184250107 ) ) ;
#20565=DIRECTION ( 'NONE',  ( -1.000000000000000000, -0.000000000000000000, -0.000000000000000000 ) ) ;
#20566=DIRECTION ( 'NONE',  ( 1.000000000000000000, -0.000000000000000000, -0.000000000000000000 ) ) ;
#20567=EDGE_CURVE ( 'NONE', #37030, #44743, #45741, .T. ) ;
#20574=LINE ( 'NONE', #13245, #15993 ) ;
#20575=LINE ( 'NONE', #16916, #46011 ) ;
#20580=VECTOR ( 'NONE', #4410, 1000.000000000000000 ) ;
#20587=ORIENTED_EDGE ( 'NONE', *, *, #38760, .T. ) ;
#20594=CIRCLE ( 'NONE', #22138, 31.99999999999998934 ) ;
#20599=DIRECTION ( 'NONE',  ( -1.000000000000000000, -0.000000000000000000, -0.000000000000000000 ) ) ;
#20600=ADVANCED_FACE ( 'NONE', ( #35434 ), #20988, .T. ) ;
#20601=DIRECTION ( 'NONE',  ( 0.000000000000000000, 0.000000000000000000, 1.000000000000000000 ) ) ;
#20603=ORIENTED_EDGE ( 'NONE', *, *, #15202, .T. ) ;
#20606=ORIENTED_EDGE ( 'NONE', *, *, #40519, .T. ) ;
#20607=DIRECTION ( 'NONE',  ( 1.000000000000000000, 0.000000000000000000, 0.000000000000000000 ) ) ;
#20612=AXIS2_PLACEMENT_3D ( 'NONE', #16273, #38790, #35095 ) ;
#20613=DIRECTION ( 'NONE',  ( 0.000000000000000000, 0.000000000000000000, 1.000000000000000000 ) ) ;
#20616=FACE_OUTER_BOUND ( 'NONE', #38877, .T. ) ;
#20617=ORIENTED_EDGE ( 'NONE', *, *, #13483, .F. ) ;
#20621=FACE_OUTER_BOUND ( 'NONE', #26812, .T. ) ;
#20625=CARTESIAN_POINT ( 'NONE',  ( 11.99999999999999822, 16.65972982745045528, -80.28980883073741381 ) ) ;
#20627=ORIENTED_EDGE ( 'NONE', *, *, #45939, .T. ) ;
#20630=CYLINDRICAL_SURFACE ( 'NONE', #6492, 31.99999999999998579 ) ;
#20632=CYLINDRICAL_SURFACE ( 'NONE', #4900, 77.49899999999999523 ) ;
#20636=CARTESIAN_POINT ( 'NONE',  ( 12.00000000000000000, -11.95096189432345923, -23.69967320028757030 ) ) ;
#20643=LINE ( 'NONE', #2061, #10472 ) ;
#20647=ORIENTED_EDGE ( 'NONE', *, *, #38577, .T. ) ;
#20648=DIRECTION ( 'NONE',  ( -1.000000000000000000, 0.000000000000000000, 0.000000000000000000 ) ) ;
#20651=CIRCLE ( 'NONE', #22201, 77.49900000000000944 ) ;
#20656=AXIS2_PLACEMENT_3D ( 'NONE', #1777, #27493, #46324 ) ;
#20664=PLANE ( 'NONE',  #45622 ) ;
#20667=CARTESIAN_POINT ( 'NONE',  ( 0.000000000000000000, 71.91182617369187824, 28.89263327155770256 ) ) ;
#20679=ORIENTED_EDGE ( 'NONE', *, *, #34911, .T. ) ;
#20681=CARTESIAN_POINT ( 'NONE',  ( 15.00000000000000000, -19.89357724625003598, -12.59942793731059041 ) ) ;
#20687=DIRECTION ( 'NONE',  ( 0.000000000000000000, -0.1045284632676436454, 0.9945218953682744001 ) ) ;
#20696=EDGE_LOOP ( 'NONE', ( #43719, #45972, #8561, #10352 ) ) ;
#20697=VERTEX_POINT ( 'NONE', #16851 ) ;
#20704=EDGE_CURVE ( 'NONE', #23653, #41663, #7175, .T. ) ;
#20705=ORIENTED_EDGE ( 'NONE', *, *, #36028, .T. ) ;
#20708=DIRECTION ( 'NONE',  ( 0.000000000000000000, 0.7604059656000276002, 0.6494480483301875440 ) ) ;
#20710=ORIENTED_EDGE ( 'NONE', *, *, #45778, .F. ) ;
#20720=EDGE_CURVE ( 'NONE', #1751, #36740, #26721, .T. ) ;
#20724=VECTOR ( 'NONE', #41846, 1000.000000000000000 ) ;
#20727=EDGE_CURVE ( 'NONE', #13754, #24474, #44709, .T. ) ;
#20729=VECTOR ( 'NONE', #2506, 1000.000000000000000 ) ;
#20730=EDGE_CURVE ( 'NONE', #9234, #48128, #36071, .T. ) ;
#20733=CARTESIAN_POINT ( 'NONE',  ( 0.000000000000000000, -78.73519480814971416, 22.90783923731599359 ) ) ;
#20737=VERTEX_POINT ( 'NONE', #18751 ) ;
#20740=ORIENTED_EDGE ( 'NONE', *, *, #10790, .T. ) ;
#20742=AXIS2_PLACEMENT_3D ( 'NONE', #34554, #41939, #12081 ) ;
#20746=FACE_OUTER_BOUND ( 'NONE', #2366, .T. ) ;
#20748=LINE ( 'NONE', #27868, #5620 ) ;
#20750=VECTOR ( 'NONE', #1616, 1000.000000000000000 ) ;
#20753=PLANE ( 'NONE',  #41623 ) ;
#20754=ORIENTED_EDGE ( 'NONE', *, *, #40112, .T. ) ;
#20759=ORIENTED_EDGE ( 'NONE', *, *, #19042, .T. ) ;
#20761=ORIENTED_EDGE ( 'NONE', *, *, #14418, .T. ) ;
#20766=CARTESIAN_POINT ( 'NONE',  ( 0.000000000000000000, 81.34940948281337114, 10.30890764327411446 ) ) ;
#20768=DIRECTION ( 'NONE',  ( 0.000000000000000000, -0.5224985647159380298, -0.8526401643540988395 ) ) ;
#20787=EDGE_LOOP ( 'NONE', ( #40190, #18840, #23973, #40817 ) ) ;
#20790=CARTESIAN_POINT ( 'NONE',  ( 11.99999999999999822, 55.38113227695783536, 54.21277698773694453 ) ) ;
#20793=EDGE_CURVE ( 'NONE', #23206, #21915, #26359, .T. ) ;
#20796=AXIS2_PLACEMENT_3D ( 'NONE', #7085, #2935, #10771 ) ;
#20797=DIRECTION ( 'NONE',  ( -1.000000000000000000, 0.000000000000000000, 0.000000000000000000 ) ) ;
#20799=DIRECTION ( 'NONE',  ( 0.000000000000000000, 0.2079116908177555123, -0.9781476007338064660 ) ) ;
#20802=CARTESIAN_POINT ( 'NONE',  ( 0.000000000000000000, 0.000000000000000000, 0.000000000000000000 ) ) ;
#20803=CARTESIAN_POINT ( 'NONE',  ( 0.000000000000000000, 0.000000000000000000, 0.000000000000000000 ) ) ;
#20808=FACE_OUTER_BOUND ( 'NONE', #38153, .T. ) ;
#20809=CARTESIAN_POINT ( 'NONE',  ( 12.00000000000000000, 18.84667830672579569, -18.68964196561269375 ) ) ;
#20811=DIRECTION ( 'NONE',  ( 0.000000000000000000, -0.9238795325112906243, 0.3826834323650805114 ) ) ;
#20816=ORIENTED_EDGE ( 'NONE', *, *, #23713, .T. ) ;
#20817=CARTESIAN_POINT ( 'NONE',  ( 50.00005079999999680, 0.000000000000000000, 0.000000000000000000 ) ) ;
#20818=VECTOR ( 'NONE', #31, 1000.000000000000000 ) ;
#20819=CARTESIAN_POINT ( 'NONE',  ( 11.99999999999999822, 72.35432306680485226, -20.40083707022909110 ) ) ;
#20821=CARTESIAN_POINT ( 'NONE',  ( 11.99999999999999822, -24.73286445877655382, -73.44644590900085745 ) ) ;
#20822=CARTESIAN_POINT ( 'NONE',  ( 11.99999999999999822, -14.67089635893658794, -73.72996012237454977 ) ) ;
#20828=AXIS2_PLACEMENT_3D ( 'NONE', #5658, #27454, #8588 ) ;
#20830=CARTESIAN_POINT ( 'NONE',  ( 11.99999999999999822, 75.54627589209970040, -17.28742895386005785 ) ) ;
#20833=DIRECTION ( 'NONE',  ( -1.000000000000000000, 0.000000000000000000, -0.000000000000000000 ) ) ;
#20834=EDGE_CURVE ( 'NONE', #13485, #3749, #29541, .T. ) ;
#20842=EDGE_CURVE ( 'NONE', #31342, #28723, #30632, .T. ) ;
#20844=ORIENTED_EDGE ( 'NONE', *, *, #7687, .T. ) ;
#20849=DIRECTION ( 'NONE',  ( 0.000000000000000000, 0.000000000000000000, 1.000000000000000000 ) ) ;
#20852=AXIS2_PLACEMENT_3D ( 'NONE', #28873, #10273, #25194 ) ;
#20855=ORIENTED_EDGE ( 'NONE', *, *, #5867, .F. ) ;
#20857=DIRECTION ( 'NONE',  ( -1.000000000000000000, -0.000000000000000000, -0.000000000000000000 ) ) ;
#20865=CARTESIAN_POINT ( 'NONE',  ( 11.99999999999999822, 0.000000000000000000, 0.000000000000000000 ) ) ;
#20868=CIRCLE ( 'NONE', #42754, 82.00000000000000000 ) ;
#20873=DIRECTION ( 'NONE',  ( 0.000000000000000000, -0.2079116908177651990, -0.9781476007338044676 ) ) ;
#20874=ORIENTED_EDGE ( 'NONE', *, *, #15479, .T. ) ;
#20875=ORIENTED_EDGE ( 'NONE', *, *, #30974, .F. ) ;
#20877=ORIENTED_EDGE ( 'NONE', *, *, #45778, .T. ) ;
#20878=CARTESIAN_POINT ( 'NONE',  ( 11.99999999999999822, -70.52718814184240159, -26.02418014898383802 ) ) ;
#20879=CARTESIAN_POINT ( 'NONE',  ( 0.000000000000000000, 0.000000000000000000, 0.000000000000000000 ) ) ;
#20880=DIRECTION ( 'NONE',  ( -1.000000000000000000, 0.000000000000000000, 0.000000000000000000 ) ) ;
#20883=CARTESIAN_POINT ( 'NONE',  ( 11.99999999999999822, 0.000000000000000000, 0.000000000000000000 ) ) ;
#20885=FACE_OUTER_BOUND ( 'NONE', #19088, .T. ) ;
#20888=EDGE_LOOP ( 'NONE', ( #24814, #44746, #34475, #7420 ) ) ;
#20889=EDGE_CURVE ( 'NONE', #29937, #29716, #25616, .T. ) ;
#20890=CARTESIAN_POINT ( 'NONE',  ( 11.99999999999999822, -68.26794271651286294, 31.47745569255117104 ) ) ;
#20893=FACE_OUTER_BOUND ( 'NONE', #47147, .T. ) ;
#20899=ORIENTED_EDGE ( 'NONE', *, *, #45460, .F. ) ;
#20902=VERTEX_POINT ( 'NONE', #8232 ) ;
#20906=EDGE_CURVE ( 'NONE', #12269, #41614, #40795, .T. ) ;
#20913=VECTOR ( 'NONE', #17416, 1000.000000000000000 ) ;
#20914=DIRECTION ( 'NONE',  ( -0.000000000000000000, 0.1045284632676548031, 0.9945218953682732899 ) ) ;
#20916=CARTESIAN_POINT ( 'NONE',  ( 15.00000000000000000, -10.45096189432344502, -21.10159698893425784 ) ) ;
#20921=ORIENTED_EDGE ( 'NONE', *, *, #35464, .F. ) ;
#20928=VECTOR ( 'NONE', #4925, 1000.000000000000227 ) ;
#20929=ORIENTED_EDGE ( 'NONE', *, *, #12131, .F. ) ;
#20930=CARTESIAN_POINT ( 'NONE',  ( 0.000000000000000000, 0.000000000000000000, 0.000000000000000000 ) ) ;
#20935=LINE ( 'NONE', #39287, #18865 ) ;
#20936=DIRECTION ( 'NONE',  ( -1.000000000000000000, -0.000000000000000000, 0.000000000000000000 ) ) ;
#20939=CARTESIAN_POINT ( 'NONE',  ( 11.99999999999999822, -75.54627589209931671, -17.28742895386162814 ) ) ;
#20940=AXIS2_PLACEMENT_3D ( 'NONE', #2226, #9810, #10050 ) ;
#20942=DIRECTION ( 'NONE',  ( -1.000000000000000000, -0.000000000000000000, 0.000000000000000000 ) ) ;
#20943=VERTEX_POINT ( 'NONE', #30506 ) ;
#20944=EDGE_CURVE ( 'NONE', #45638, #488, #19468, .T. ) ;
#20947=EDGE_CURVE ( 'NONE', #15373, #29567, #12396, .T. ) ;
#20948=LINE ( 'NONE', #31255, #7588 ) ;
#20950=DIRECTION ( 'NONE',  ( -1.000000000000000000, 0.000000000000000000, 0.000000000000000000 ) ) ;
#20951=DIRECTION ( 'NONE',  ( -1.000000000000000000, 0.000000000000000000, 0.000000000000000000 ) ) ;
#20953=EDGE_CURVE ( 'NONE', #16941, #14753, #37644, .T. ) ;
#20955=VERTEX_POINT ( 'NONE', #45429 ) ;
#20956=CIRCLE ( 'NONE', #30362, 82.00000000000000000 ) ;
#20957=CARTESIAN_POINT ( 'NONE',  ( 11.99999999999999822, -41.19522573413689059, -65.64334221924951862 ) ) ;
#20960=EDGE_CURVE ( 'NONE', #31411, #36422, #32212, .T. ) ;
#20962=ORIENTED_EDGE ( 'NONE', *, *, #43492, .T. ) ;
#20972=DIRECTION ( 'NONE',  ( 0.000000000000000000, 0.8526401643540935105, -0.5224985647159468005 ) ) ;
#20977=ORIENTED_EDGE ( 'NONE', *, *, #42134, .F. ) ;
#20979=ORIENTED_EDGE ( 'NONE', *, *, #31239, .F. ) ;
#20987=CARTESIAN_POINT ( 'NONE',  ( 0.000000000000000000, 55.19960302592066625, 51.03279382321107249 ) ) ;
#20988=CYLINDRICAL_SURFACE ( 'NONE', #36869, 31.99999999999998579 ) ;
#20991=LINE ( 'NONE', #5842, #12404 ) ;
#20992=VERTEX_POINT ( 'NONE', #27325 ) ;
#20997=AXIS2_PLACEMENT_3D ( 'NONE', #13328, #14285, #47801 ) ;
#21005=CARTESIAN_POINT ( 'NONE',  ( 11.99999999999999822, -12.93880638057260946, -76.41127070299286572 ) ) ;
#21006=EDGE_CURVE ( 'NONE', #35973, #36243, #947, .T. ) ;
#21009=ORIENTED_EDGE ( 'NONE', *, *, #3886, .T. ) ;
#21016=EDGE_CURVE ( 'NONE', #1488, #2398, #46286, .T. ) ;
#21018=VERTEX_POINT ( 'NONE', #17246 ) ;
#21023=( GEOMETRIC_REPRESENTATION_CONTEXT ( 3 ) GLOBAL_UNCERTAINTY_ASSIGNED_CONTEXT ( ( #15898 ) ) GLOBAL_UNIT_ASSIGNED_CONTEXT ( ( #23466, #38408, #15179 ) ) REPRESENTATION_CONTEXT ( 'NONE', 'WORKASPACE' ) );
#21028=ORIENTED_EDGE ( 'NONE', *, *, #36083, .T. ) ;
#21030=CYLINDRICAL_SURFACE ( 'NONE', #6677, 77.49899999999999523 ) ;
#21033=CARTESIAN_POINT ( 'NONE',  ( 11.99999999999999822, 0.000000000000000000, 0.000000000000000000 ) ) ;
#21037=CARTESIAN_POINT ( 'NONE',  ( 0.000000000000000000, 65.58780272294129077, -36.73666225445822420 ) ) ;
#21040=ORIENTED_EDGE ( 'NONE', *, *, #13088, .F. ) ;
#21041=EDGE_CURVE ( 'NONE', #37092, #17765, #43209, .T. ) ;
#21047=CYLINDRICAL_SURFACE ( 'NONE', #1850, 31.99999999999997868 ) ;
#21049=CARTESIAN_POINT ( 'NONE',  ( 11.99999999999999822, 6.903761155837791819, 77.19088730480525840 ) ) ;
#21051=CARTESIAN_POINT ( 'NONE',  ( 0.000000000000000000, 59.03342792756263435, 46.54456581323825048 ) ) ;
#21052=CIRCLE ( 'NONE', #7005, 31.99999999999998579 ) ;
#21065=CARTESIAN_POINT ( 'NONE',  ( 11.99999999999999822, 51.03279382321166224, -55.19960302592011914 ) ) ;
#21068=VECTOR ( 'NONE', #36379, 1000.000000000000000 ) ;
#21069=CARTESIAN_POINT ( 'NONE',  ( 15.00000000000000000, -19.89357724625003598, -12.59942793731059041 ) ) ;
#21072=AXIS2_PLACEMENT_3D ( 'NONE', #44201, #28554, #10675 ) ;
#21075=ORIENTED_EDGE ( 'NONE', *, *, #11250, .F. ) ;
#21076=DIRECTION ( 'NONE',  ( 0.000000000000000000, 0.000000000000000000, 1.000000000000000000 ) ) ;
#21077=AXIS2_PLACEMENT_3D ( 'NONE', #44820, #36981, #43850 ) ;
#21078=DIRECTION ( 'NONE',  ( 0.000000000000000000, -0.07845909572783056618, -0.9969173337331290741 ) ) ;
#21090=LINE ( 'NONE', #42417, #6079 ) ;
#21091=VERTEX_POINT ( 'NONE', #1862 ) ;
#21097=VERTEX_POINT ( 'NONE', #42977 ) ;
#21098=CARTESIAN_POINT ( 'NONE',  ( 15.00000000000000000, -25.60904388321916159, 6.976881207771517879 ) ) ;
#21108=LINE ( 'NONE', #17691, #45777 ) ;
#21110=CARTESIAN_POINT ( 'NONE',  ( 15.00000000000000000, 18.84667830672579569, -18.68964196561269375 ) ) ;
#21118=AXIS2_PLACEMENT_3D ( 'NONE', #33150, #36337, #6248 ) ;
#21122=ORIENTED_EDGE ( 'NONE', *, *, #43282, .F. ) ;
#21127=CARTESIAN_POINT ( 'NONE',  ( 11.99999999999999822, 0.000000000000000000, 0.000000000000000000 ) ) ;
#21128=ORIENTED_EDGE ( 'NONE', *, *, #24768, .T. ) ;
#21131=EDGE_CURVE ( 'NONE', #36385, #18965, #2327, .T. ) ;
#21135=LINE ( 'NONE', #40250, #3923 ) ;
#21142=ORIENTED_EDGE ( 'NONE', *, *, #32101, .F. ) ;
#21143=EDGE_CURVE ( 'NONE', #4357, #37720, #18695, .T. ) ;
#21150=VERTEX_POINT ( 'NONE', #14568 ) ;
#21155=EDGE_CURVE ( 'NONE', #29636, #8637, #29961, .T. ) ;
#21156=DIRECTION ( 'NONE',  ( 1.000000000000000000, -0.000000000000000000, -0.000000000000000000 ) ) ;
#21160=DIRECTION ( 'NONE',  ( 0.000000000000000000, 0.7431448254773863615, -0.6691306063588670083 ) ) ;
#21177=AXIS2_PLACEMENT_3D ( 'NONE', #46695, #13631, #20004 ) ;
#21179=CARTESIAN_POINT ( 'NONE',  ( 15.00000000000000000, 26.50000000000000355, -1.500000000000000000 ) ) ;
#21183=VECTOR ( 'NONE', #10512, 1000.000000000000114 ) ;
#21185=ORIENTED_EDGE ( 'NONE', *, *, #21571, .F. ) ;
#21186=CIRCLE ( 'NONE', #43070, 77.49900000000000944 ) ;
#21188=DIRECTION ( 'NONE',  ( 0.000000000000000000, 0.000000000000000000, 1.000000000000000000 ) ) ;
#21190=ORIENTED_EDGE ( 'NONE', *, *, #25529, .F. ) ;
#21191=LINE ( 'NONE', #25826, #15598 ) ;
#21195=ORIENTED_EDGE ( 'NONE', *, *, #18495, .T. ) ;
#21196=ORIENTED_EDGE ( 'NONE', *, *, #40618, .F. ) ;
#21199=LINE ( 'NONE', #29033, #1628 ) ;
#21204=EDGE_LOOP ( 'NONE', ( #40323, #41985, #3415, #47567 ) ) ;
#21212=DIRECTION ( 'NONE',  ( 0.000000000000000000, 0.9781476007338045786, -0.2079116908177641720 ) ) ;
#21214=VECTOR ( 'NONE', #3593, 1000.000000000000000 ) ;
#21215=EDGE_CURVE ( 'NONE', #47807, #13122, #40994, .T. ) ;
#21226=CARTESIAN_POINT ( 'NONE',  ( 15.00000000000000000, -23.29833615347104470, 3.418703333116808629 ) ) ;
#21229=VERTEX_POINT ( 'NONE', #6968 ) ;
#21230=DIRECTION ( 'NONE',  ( -1.000000000000000000, 0.000000000000000000, 0.000000000000000000 ) ) ;
#21231=DIRECTION ( 'NONE',  ( 0.000000000000000000, 0.000000000000000000, 1.000000000000000000 ) ) ;
#21235=DIRECTION ( 'NONE',  ( 0.000000000000000000, 0.000000000000000000, 1.000000000000000000 ) ) ;
#21238=ORIENTED_EDGE ( 'NONE', *, *, #36353, .F. ) ;
#21241=VECTOR ( 'NONE', #22601, 1000.000000000000000 ) ;
#21243=CARTESIAN_POINT ( 'NONE',  ( 0.000000000000000000, -35.91791733033427647, -68.67312586195032509 ) ) ;
#21246=ORIENTED_EDGE ( 'NONE', *, *, #3937, .F. ) ;
#21255=EDGE_CURVE ( 'NONE', #15376, #46628, #44704, .T. ) ;
#21256=EDGE_CURVE ( 'NONE', #20697, #23468, #36109, .T. ) ;
#21257=DIRECTION ( 'NONE',  ( -1.000000000000000000, -0.000000000000000000, -0.000000000000000000 ) ) ;
#21259=DIRECTION ( 'NONE',  ( -1.000000000000000000, -0.000000000000000000, 0.000000000000000000 ) ) ;
#21263=AXIS2_PLACEMENT_3D ( 'NONE', #8762, #15631, #33737 ) ;
#21264=FACE_OUTER_BOUND ( 'NONE', #2513, .T. ) ;
#21265=CARTESIAN_POINT ( 'NONE',  ( 6.000000000000000000, -81.34940948281344220, 10.30890764327355846 ) ) ;
#21267=CARTESIAN_POINT ( 'NONE',  ( 15.00000000000000000, -1.278221433540145391, 26.51162292216073979 ) ) ;
#21268=ORIENTED_EDGE ( 'NONE', *, *, #27683, .F. ) ;
#21271=CARTESIAN_POINT ( 'NONE',  ( 11.99999999999999822, -64.81221759200306565, -50.23322058963420034 ) ) ;
#21272=ORIENTED_EDGE ( 'NONE', *, *, #10899, .F. ) ;
#21275=CARTESIAN_POINT ( 'NONE',  ( 5.999999999999999112, 2.543863470248399761, 81.96053171279903893 ) ) ;
#21277=EDGE_LOOP ( 'NONE', ( #37152, #13698, #32189, #25163 ) ) ;
#21284=VECTOR ( 'NONE', #34231, 1000.000000000000000 ) ;
#21286=EDGE_CURVE ( 'NONE', #36432, #25492, #20479, .T. ) ;
#21287=CARTESIAN_POINT ( 'NONE',  ( 0.000000000000000000, 0.000000000000000000, 0.000000000000000000 ) ) ;
#21289=AXIS2_PLACEMENT_3D ( 'NONE', #2577, #5546, #43708 ) ;
#21296=ORIENTED_EDGE ( 'NONE', *, *, #6010, .T. ) ;
#21298=EDGE_CURVE ( 'NONE', #40177, #35673, #27525, .T. ) ;
#21300=CIRCLE ( 'NONE', #10369, 82.00000000000000000 ) ;
#21301=AXIS2_PLACEMENT_3D ( 'NONE', #42880, #24037, #39203 ) ;
#21304=CIRCLE ( 'NONE', #41617, 31.99999999999998579 ) ;
#21316=EDGE_CURVE ( 'NONE', #20223, #27571, #11135, .T. ) ;
#21318=DIRECTION ( 'NONE',  ( 0.000000000000000000, 0.1045284632676558162, 0.9945218953682731788 ) ) ;
#21320=EDGE_CURVE ( 'NONE', #5793, #17817, #2519, .T. ) ;
#21324=VECTOR ( 'NONE', #28011, 1000.000000000000000 ) ;
#21326=FACE_OUTER_BOUND ( 'NONE', #8410, .T. ) ;
#21329=CARTESIAN_POINT ( 'NONE',  ( 6.000000000000000000, -16.65972982744991171, 80.28980883073752750 ) ) ;
#21331=DIRECTION ( 'NONE',  ( 0.000000000000000000, 0.000000000000000000, 1.000000000000000000 ) ) ;
#21335=CARTESIAN_POINT ( 'NONE',  ( 12.00000000000000000, -4.261787119645322974, -26.19803753235774479 ) ) ;
#21338=CARTESIAN_POINT ( 'NONE',  ( 0.000000000000000000, -68.67312586194971402, -35.91791733033549860 ) ) ;
#21340=ORIENTED_EDGE ( 'NONE', *, *, #7535, .F. ) ;
#21344=ORIENTED_EDGE ( 'NONE', *, *, #7904, .T. ) ;
#21348=CARTESIAN_POINT ( 'NONE',  ( 11.99999999999999822, 0.000000000000000000, 0.000000000000000000 ) ) ;
#21350=CARTESIAN_POINT ( 'NONE',  ( 0.000000000000000000, 0.000000000000000000, 0.000000000000000000 ) ) ;
#21360=CIRCLE ( 'NONE', #26855, 31.99999999999998224 ) ;
#21361=ORIENTED_EDGE ( 'NONE', *, *, #43823, .F. ) ;
#21365=DIRECTION ( 'NONE',  ( 0.000000000000000000, -0.9510565162951499785, -0.3090169943749582204 ) ) ;
#21369=VERTEX_POINT ( 'NONE', #4985 ) ;
#21371=DIRECTION ( 'NONE',  ( 0.000000000000000000, 0.000000000000000000, -1.000000000000000000 ) ) ;
#21373=EDGE_CURVE ( 'NONE', #17814, #20223, #23630, .T. ) ;
#21380=DIRECTION ( 'NONE',  ( -1.000000000000000000, 0.000000000000000000, 0.000000000000000000 ) ) ;
#21381=VECTOR ( 'NONE', #813, 1000.000000000000000 ) ;
#21382=AXIS2_PLACEMENT_3D ( 'NONE', #21940, #14852, #43513 ) ;
#21385=ORIENTED_EDGE ( 'NONE', *, *, #1337, .T. ) ;
#21387=ADVANCED_FACE ( 'NONE', ( #45370 ), #34113, .T. ) ;
#21391=CYLINDRICAL_SURFACE ( 'NONE', #46275, 82.00000000000000000 ) ;
#21392=AXIS2_PLACEMENT_3D ( 'NONE', #26505, #8140, #30190 ) ;
#21393=CIRCLE ( 'NONE', #37049, 77.49899999999999523 ) ;
#21396=ORIENTED_EDGE ( 'NONE', *, *, #20720, .T. ) ;
#21397=ORIENTED_EDGE ( 'NONE', *, *, #45642, .F. ) ;
#21398=VECTOR ( 'NONE', #15464, 1000.000000000000000 ) ;
#21399=DIRECTION ( 'NONE',  ( -1.000000000000000000, 0.000000000000000000, 0.000000000000000000 ) ) ;
#21401=CARTESIAN_POINT ( 'NONE',  ( 6.000000000000000000, -79.10210256391383155, 21.60688246758558506 ) ) ;
#21408=DIRECTION ( 'NONE',  ( -1.000000000000000000, -0.000000000000000000, 0.000000000000000000 ) ) ;
#21418=CIRCLE ( 'NONE', #16058, 82.00000000000000000 ) ;
#21419=EDGE_CURVE ( 'NONE', #12997, #31342, #47864, .T. ) ;
#21420=LINE ( 'NONE', #17256, #38872 ) ;
#21424=CARTESIAN_POINT ( 'NONE',  ( 11.99999999999999822, 0.000000000000000000, 0.000000000000000000 ) ) ;
#21425=CIRCLE ( 'NONE', #25329, 31.99999999999998579 ) ;
#21427=VECTOR ( 'NONE', #39475, 1000.000000000000000 ) ;
#21434=AXIS2_PLACEMENT_3D ( 'NONE', #16205, #46061, #24028 ) ;
#21436=AXIS2_PLACEMENT_3D ( 'NONE', #31090, #46247, #27647 ) ;
#21438=EDGE_CURVE ( 'NONE', #42832, #14950, #29881, .T. ) ;
#21442=ADVANCED_FACE ( 'NONE', ( #20885 ), #35809, .T. ) ;
#21449=EDGE_LOOP ( 'NONE', ( #43239, #32247, #30607, #30354 ) ) ;
#21460=ORIENTED_EDGE ( 'NONE', *, *, #24042, .F. ) ;
#21468=DIRECTION ( 'NONE',  ( -1.000000000000000000, -0.000000000000000000, -0.000000000000000000 ) ) ;
#21475=AXIS2_PLACEMENT_3D ( 'NONE', #14382, #14632, #48384 ) ;
#21476=CARTESIAN_POINT ( 'NONE',  ( 11.99999999999999822, -46.54456581323847786, 59.03342792756247093 ) ) ;
#21486=DIRECTION ( 'NONE',  ( 1.000000000000000000, -0.000000000000000000, 0.000000000000000000 ) ) ;
#21491=DIRECTION ( 'NONE',  ( -1.000000000000000000, 0.000000000000000000, -0.000000000000000000 ) ) ;
#21496=EDGE_LOOP ( 'NONE', ( #21921, #35043, #39977, #12275 ) ) ;
#21498=ORIENTED_EDGE ( 'NONE', *, *, #9276, .F. ) ;
#21502=CARTESIAN_POINT ( 'NONE',  ( 0.000000000000000000, -51.29473840253269401, 63.97538442413407012 ) ) ;
#21505=ADVANCED_FACE ( 'NONE', ( #13297 ), #20632, .T. ) ;
#21507=CIRCLE ( 'NONE', #24624, 31.99999999999998579 ) ;
#21508=CIRCLE ( 'NONE', #14456, 31.99999999999999289 ) ;
#21514=CIRCLE ( 'NONE', #416, 31.99999999999998934 ) ;
#21520=LINE ( 'NONE', #47458, #47377 ) ;
#21521=ORIENTED_EDGE ( 'NONE', *, *, #20494, .T. ) ;
#21526=CARTESIAN_POINT ( 'NONE',  ( 11.99999999999999822, 0.000000000000000000, 0.000000000000000000 ) ) ;
#21529=AXIS2_PLACEMENT_3D ( 'NONE', #30455, #15764, #30691 ) ;
#21530=PLANE ( 'NONE',  #41538 ) ;
#21533=DIRECTION ( 'NONE',  ( 0.000000000000000000, 0.000000000000000000, 1.000000000000000000 ) ) ;
#21534=CARTESIAN_POINT ( 'NONE',  ( 11.99999999999999822, 73.44644590900061587, 24.73286445877730699 ) ) ;
#21540=ORIENTED_EDGE ( 'NONE', *, *, #25375, .T. ) ;
#21541=DIRECTION ( 'NONE',  ( 0.000000000000000000, 0.000000000000000000, -1.000000000000000000 ) ) ;
#21544=AXIS2_PLACEMENT_3D ( 'NONE', #28971, #18443, #25290 ) ;
#21545=DIRECTION ( 'NONE',  ( 1.000000000000000000, 0.000000000000000000, 0.000000000000000000 ) ) ;
#21548=AXIS2_PLACEMENT_3D ( 'NONE', #4280, #7205, #22133 ) ;
#21549=DIRECTION ( 'NONE',  ( 0.000000000000000000, 0.9723699203976773342, -0.2334453638559026156 ) ) ;
#21551=EDGE_CURVE ( 'NONE', #22095, #30146, #8777, .T. ) ;
#21555=EDGE_CURVE ( 'NONE', #4566, #24540, #31681, .T. ) ;
#21567=ADVANCED_FACE ( 'NONE', ( #18812 ), #22983, .T. ) ;
#21570=ORIENTED_EDGE ( 'NONE', *, *, #15106, .F. ) ;
#21571=EDGE_CURVE ( 'NONE', #1311, #15059, #18342, .T. ) ;
#21580=ORIENTED_EDGE ( 'NONE', *, *, #28892, .T. ) ;
#21582=CIRCLE ( 'NONE', #486, 77.49899999999999523 ) ;
#21584=CARTESIAN_POINT ( 'NONE',  ( 6.000000000000000000, -40.65526001592564853, -71.21200624218839437 ) ) ;
#21587=CARTESIAN_POINT ( 'NONE',  ( 15.00000000000000000, 23.59884966291538078, 12.14883922797231008 ) ) ;
#21591=AXIS2_PLACEMENT_3D ( 'NONE', #11140, #34356, #602 ) ;
#21593=VERTEX_POINT ( 'NONE', #4149 ) ;
#21594=ORIENTED_EDGE ( 'NONE', *, *, #16928, .F. ) ;
#21595=CARTESIAN_POINT ( 'NONE',  ( 15.00000000000000000, 20.85821328998741109, -10.92862929874522671 ) ) ;
#21599=VECTOR ( 'NONE', #26488, 1000.000000000000000 ) ;
#21600=DIRECTION ( 'NONE',  ( 0.000000000000000000, 0.9510565162951544194, -0.3090169943749448977 ) ) ;
#21611=CARTESIAN_POINT ( 'NONE',  ( 11.99999999999999822, 74.65491531819118620, 23.16904090965732621 ) ) ;
#21612=EDGE_CURVE ( 'NONE', #17963, #48059, #15413, .T. ) ;
#21618=CARTESIAN_POINT ( 'NONE',  ( 0.000000000000000000, -50.95692526931287603, -58.39081064771804819 ) ) ;
#21621=ORIENTED_EDGE ( 'NONE', *, *, #7540, .T. ) ;
#21622=FACE_OUTER_BOUND ( 'NONE', #31668, .T. ) ;
#21623=ORIENTED_EDGE ( 'NONE', *, *, #24428, .F. ) ;
#21625=CARTESIAN_POINT ( 'NONE',  ( 0.000000000000000000, 0.000000000000000000, 0.000000000000000000 ) ) ;
#21628=DIRECTION ( 'NONE',  ( -1.000000000000000000, -0.000000000000000000, -0.000000000000000000 ) ) ;
#21635=CYLINDRICAL_SURFACE ( 'NONE', #20997, 31.99999999999998579 ) ;
#21637=ORIENTED_EDGE ( 'NONE', *, *, #16352, .F. ) ;
#21640=AXIS2_PLACEMENT_3D ( 'NONE', #4514, #346, #22860 ) ;
#21650=AXIS2_PLACEMENT_3D ( 'NONE', #46726, #13184, #20768 ) ;
#21653=CARTESIAN_POINT ( 'NONE',  ( 11.99999999999999822, -5.256550761632340141, -77.32052557432847095 ) ) ;
#21660=ORIENTED_EDGE ( 'NONE', *, *, #37797, .T. ) ;
#21672=ORIENTED_EDGE ( 'NONE', *, *, #10431, .T. ) ;
#21679=EDGE_LOOP ( 'NONE', ( #857, #45954, #39666, #17116 ) ) ;
#21685=AXIS2_PLACEMENT_3D ( 'NONE', #37987, #18648, #38225 ) ;
#21687=FACE_OUTER_BOUND ( 'NONE', #8097, .T. ) ;
#21695=CARTESIAN_POINT ( 'NONE',  ( 0.000000000000000000, 62.50329211542494789, -41.76937507738723099 ) ) ;
#21707=DIRECTION ( 'NONE',  ( -0.000000000000000000, -0.9135454576426058626, -0.4067366430757889395 ) ) ;
#21708=DIRECTION ( 'NONE',  ( -1.000000000000000000, 0.000000000000000000, -0.000000000000000000 ) ) ;
#21709=EDGE_CURVE ( 'NONE', #39901, #5700, #14310, .T. ) ;
#21710=DIRECTION ( 'NONE',  ( -1.000000000000000000, -0.000000000000000000, -0.000000000000000000 ) ) ;
#21711=CARTESIAN_POINT ( 'NONE',  ( 0.000000000000000000, -8.830959090342926032, 74.65491531819115778 ) ) ;
#21718=CARTESIAN_POINT ( 'NONE',  ( 11.99999999999999822, -16.65972982744876774, -80.28980883073775487 ) ) ;
#21721=CARTESIAN_POINT ( 'NONE',  ( 11.99999999999999822, 36.73666225445894185, 65.58780272294090707 ) ) ;
#21722=EDGE_CURVE ( 'NONE', #14957, #32083, #23963, .T. ) ;
#21726=DIRECTION ( 'NONE',  ( -1.000000000000000000, 0.000000000000000000, -0.000000000000000000 ) ) ;
#21727=LINE ( 'NONE', #32514, #48179 ) ;
#21730=CARTESIAN_POINT ( 'NONE',  ( 11.99999999999999822, -16.65972982744991171, 80.28980883073751329 ) ) ;
#21737=DIRECTION ( 'NONE',  ( -1.000000000000000000, -0.000000000000000000, -0.000000000000000000 ) ) ;
#21741=AXIS2_PLACEMENT_3D ( 'NONE', #36614, #47866, #20972 ) ;
#21743=LINE ( 'NONE', #5879, #29781 ) ;
#21744=EDGE_CURVE ( 'NONE', #10422, #13639, #15639, .T. ) ;
#21745=EDGE_LOOP ( 'NONE', ( #10999, #7362, #34962, #12416 ) ) ;
#21753=EDGE_CURVE ( 'NONE', #37621, #21091, #47906, .T. ) ;
#21755=ORIENTED_EDGE ( 'NONE', *, *, #28786, .F. ) ;
#21759=EDGE_LOOP ( 'NONE', ( #19299, #2563, #39212, #44384 ) ) ;
#21762=CARTESIAN_POINT ( 'NONE',  ( 0.000000000000000000, 24.73286445877704764, 73.44644590900067271 ) ) ;
#21764=VERTEX_POINT ( 'NONE', #34963 ) ;
#21767=DIRECTION ( 'NONE',  ( 0.000000000000000000, -1.000000000000000000, -1.040834085586084730E-14 ) ) ;
#21771=EDGE_CURVE ( 'NONE', #23939, #2410, #11202, .T. ) ;
#21781=CARTESIAN_POINT ( 'NONE',  ( 0.000000000000000000, 24.73286445877808148, -73.44644590900034586 ) ) ;
#21783=VERTEX_POINT ( 'NONE', #16141 ) ;
#21787=PLANE ( 'NONE',  #5736 ) ;
#21788=DIRECTION ( 'NONE',  ( -1.000000000000000000, 0.000000000000000000, 0.000000000000000000 ) ) ;
#21802=ORIENTED_EDGE ( 'NONE', *, *, #3795, .T. ) ;
#21814=FACE_OUTER_BOUND ( 'NONE', #7386, .T. ) ;
#21825=ORIENTED_EDGE ( 'NONE', *, *, #10779, .F. ) ;
#21831=VERTEX_POINT ( 'NONE', #45995 ) ;
#21837=DIRECTION ( 'NONE',  ( 0.000000000000000000, -0.9510565162951502005, -0.3090169943749581094 ) ) ;
#21843=AXIS2_PLACEMENT_3D ( 'NONE', #10592, #6432, #25982 ) ;
#21851=AXIS2_PLACEMENT_3D ( 'NONE', #8874, #15506, #33849 ) ;
#21857=EDGE_CURVE ( 'NONE', #31210, #46446, #17397, .T. ) ;
#21859=LINE ( 'NONE', #11097, #26974 ) ;
#21863=VERTEX_POINT ( 'NONE', #39851 ) ;
#21864=EDGE_CURVE ( 'NONE', #36432, #44023, #40343, .T. ) ;
#21867=CARTESIAN_POINT ( 'NONE',  ( 0.000000000000000000, -81.34940948281344220, 10.30890764327355846 ) ) ;
#21868=EDGE_CURVE ( 'NONE', #27438, #14436, #32276, .T. ) ;
#21872=ADVANCED_FACE ( 'NONE', ( #32729 ), #40088, .T. ) ;
#21875=ORIENTED_EDGE ( 'NONE', *, *, #27242, .T. ) ;
#21877=EDGE_CURVE ( 'NONE', #34997, #30063, #18967, .T. ) ;
#21881=CARTESIAN_POINT ( 'NONE',  ( 11.99999999999999822, -56.15606465355001120, 59.75363087400055662 ) ) ;
#21882=DIRECTION ( 'NONE',  ( -1.000000000000000000, 0.000000000000000000, 0.000000000000000000 ) ) ;
#21887=DIRECTION ( 'NONE',  ( -1.000000000000000000, 0.000000000000000000, 0.000000000000000000 ) ) ;
#21895=ADVANCED_FACE ( 'NONE', ( #9494 ), #6087, .T. ) ;
#21896=LINE ( 'NONE', #10164, #48251 ) ;
#21898=VERTEX_POINT ( 'NONE', #43279 ) ;
#21904=CIRCLE ( 'NONE', #43778, 77.49900000000000944 ) ;
#21913=CARTESIAN_POINT ( 'NONE',  ( 6.000000000000000000, 15.33399622253601002, -80.55351364060572905 ) ) ;
#21915=VERTEX_POINT ( 'NONE', #6319 ) ;
#21918=LINE ( 'NONE', #10684, #36317 ) ;
#21921=ORIENTED_EDGE ( 'NONE', *, *, #43049, .F. ) ;
#21922=EDGE_CURVE ( 'NONE', #5918, #14629, #1936, .T. ) ;
#21925=ORIENTED_EDGE ( 'NONE', *, *, #4528, .F. ) ;
#21928=EDGE_LOOP ( 'NONE', ( #27072, #14834, #25476, #1331 ) ) ;
#21929=DIRECTION ( 'NONE',  ( 1.000000000000000000, -0.000000000000000000, -0.000000000000000000 ) ) ;
#21937=CARTESIAN_POINT ( 'NONE',  ( 15.00000000000000000, -22.32062822937469093, 14.36278369418830181 ) ) ;
#21940=CARTESIAN_POINT ( 'NONE',  ( 0.000000000000000000, 0.000000000000000000, 0.000000000000000000 ) ) ;
#21947=VECTOR ( 'NONE', #37404, 1000.000000000000000 ) ;
#21952=CARTESIAN_POINT ( 'NONE',  ( 5.999999999999999112, 56.15606465355041621, -59.75363087400017292 ) ) ;
#21956=AXIS2_PLACEMENT_3D ( 'NONE', #20819, #32557, #25190 ) ;
#21957=CARTESIAN_POINT ( 'NONE',  ( 0.000000000000000000, -39.78640506895559525, -66.50666863322042843 ) ) ;
#21964=ORIENTED_EDGE ( 'NONE', *, *, #9135, .F. ) ;
#21965=EDGE_CURVE ( 'NONE', #44445, #26225, #28823, .T. ) ;
#21967=CARTESIAN_POINT ( 'NONE',  ( 0.000000000000000000, 74.65491531819118620, 23.16904090965732621 ) ) ;
#21970=AXIS2_PLACEMENT_3D ( 'NONE', #15697, #4457, #8826 ) ;
#21972=DIRECTION ( 'NONE',  ( 0.000000000000000000, -0.7604059656000227152, -0.6494480483301934282 ) ) ;
#21973=VECTOR ( 'NONE', #37844, 1000.000000000000000 ) ;
#21975=VERTEX_POINT ( 'NONE', #20766 ) ;
#21978=CIRCLE ( 'NONE', #9480, 31.99999999999998579 ) ;
#21982=CYLINDRICAL_SURFACE ( 'NONE', #35661, 77.49899999999999523 ) ;
#21984=EDGE_CURVE ( 'NONE', #39718, #13449, #36172, .T. ) ;
#21988=CARTESIAN_POINT ( 'NONE',  ( 0.000000000000000000, 0.000000000000000000, 0.000000000000000000 ) ) ;
#21997=DIRECTION ( 'NONE',  ( 0.000000000000000000, 0.000000000000000000, 1.000000000000000000 ) ) ;
#22000=DIRECTION ( 'NONE',  ( 0.000000000000000000, 0.000000000000000000, 1.000000000000000000 ) ) ;
#22001=EDGE_CURVE ( 'NONE', #13122, #46849, #22457, .T. ) ;
#22002=DIRECTION ( 'NONE',  ( 0.000000000000000000, 0.000000000000000000, 1.000000000000000000 ) ) ;
#22003=DIRECTION ( 'NONE',  ( -1.000000000000000000, 0.000000000000000000, -0.000000000000000000 ) ) ;
#22007=DIRECTION ( 'NONE',  ( 0.000000000000000000, 0.000000000000000000, 1.000000000000000000 ) ) ;
#22010=CARTESIAN_POINT ( 'NONE',  ( 11.99999999999999822, 39.47590169984944453, -71.87247863392373404 ) ) ;
#22013=CIRCLE ( 'NONE', #29043, 31.99999999999998934 ) ;
#22018=VECTOR ( 'NONE', #10457, 1000.000000000000000 ) ;
#22019=ORIENTED_EDGE ( 'NONE', *, *, #13925, .F. ) ;
#22020=ORIENTED_EDGE ( 'NONE', *, *, #20273, .T. ) ;
#22022=CARTESIAN_POINT ( 'NONE',  ( 11.99999999999999822, 0.000000000000000000, 0.000000000000000000 ) ) ;
#22024=EDGE_CURVE ( 'NONE', #4021, #14629, #35402, .T. ) ;
#22025=CARTESIAN_POINT ( 'NONE',  ( -10.00000000000000000, 0.000000000000000000, 0.000000000000000000 ) ) ;
#22026=EDGE_CURVE ( 'NONE', #7117, #6056, #44031, .T. ) ;
#22034=ORIENTED_EDGE ( 'NONE', *, *, #16147, .T. ) ;
#22036=EDGE_CURVE ( 'NONE', #30527, #2177, #10945, .T. ) ;
#22038=CARTESIAN_POINT ( 'NONE',  ( 11.99999999999999822, 0.000000000000000000, 0.000000000000000000 ) ) ;
#22039=EDGE_LOOP ( 'NONE', ( #22604, #33076, #38655, #15910 ) ) ;
#22041=DIRECTION ( 'NONE',  ( -1.000000000000000000, 0.000000000000000000, 0.000000000000000000 ) ) ;
#22042=AXIS2_PLACEMENT_3D ( 'NONE', #20545, #42350, #35490 ) ;
#22043=ORIENTED_EDGE ( 'NONE', *, *, #20727, .T. ) ;
#22044=DIRECTION ( 'NONE',  ( 0.000000000000000000, -0.9781476007338043566, 0.2079116908177651712 ) ) ;
#22047=CARTESIAN_POINT ( 'NONE',  ( 0.000000000000000000, 0.000000000000000000, 0.000000000000000000 ) ) ;
#22058=DIRECTION ( 'NONE',  ( -1.000000000000000000, 0.000000000000000000, 0.000000000000000000 ) ) ;
#22071=CARTESIAN_POINT ( 'NONE',  ( 11.99999999999999822, 0.000000000000000000, 0.000000000000000000 ) ) ;
#22075=DIRECTION ( 'NONE',  ( 0.000000000000000000, 0.000000000000000000, 1.000000000000000000 ) ) ;
#22076=DIRECTION ( 'NONE',  ( 0.000000000000000000, 0.000000000000000000, 1.000000000000000000 ) ) ;
#22080=EDGE_CURVE ( 'NONE', #43252, #36432, #23705, .T. ) ;
#22086=DIRECTION ( 'NONE',  ( -1.000000000000000000, 0.000000000000000000, 0.000000000000000000 ) ) ;
#22095=VERTEX_POINT ( 'NONE', #40564 ) ;
#22100=ORIENTED_EDGE ( 'NONE', *, *, #31084, .F. ) ;
#22108=DIRECTION ( 'NONE',  ( 0.000000000000000000, -0.1564344650402381687, 0.9876883405951365491 ) ) ;
#22119=CARTESIAN_POINT ( 'NONE',  ( 0.000000000000000000, -55.38113227695820484, 54.21277698773656084 ) ) ;
#22120=ORIENTED_EDGE ( 'NONE', *, *, #3424, .T. ) ;
#22121=ORIENTED_EDGE ( 'NONE', *, *, #19989, .T. ) ;
#22123=AXIS2_PLACEMENT_3D ( 'NONE', #8394, #45857, #4719 ) ;
#22127=VERTEX_POINT ( 'NONE', #31254 ) ;
#22129=VECTOR ( 'NONE', #17312, 1000.000000000000000 ) ;
#22133=DIRECTION ( 'NONE',  ( 0.000000000000000000, 0.000000000000000000, 1.000000000000000000 ) ) ;
#22135=CYLINDRICAL_SURFACE ( 'NONE', #2717, 31.99999999999998579 ) ;
#22137=CARTESIAN_POINT ( 'NONE',  ( 11.99999999999999822, -54.21277698773636899, -55.38113227695839669 ) ) ;
#22138=AXIS2_PLACEMENT_3D ( 'NONE', #3008, #25041, #6449 ) ;
#22139=CARTESIAN_POINT ( 'NONE',  ( 0.000000000000000000, 0.000000000000000000, 0.000000000000000000 ) ) ;
#22147=EDGE_CURVE ( 'NONE', #23778, #47607, #11917, .T. ) ;
#22148=CIRCLE ( 'NONE', #8064, 31.99999999999998934 ) ;
#22150=CARTESIAN_POINT ( 'NONE',  ( 11.99999999999999822, -62.50329211542465657, 41.76937507738766442 ) ) ;
#22154=EDGE_CURVE ( 'NONE', #46674, #1488, #241, .T. ) ;
#22160=ORIENTED_EDGE ( 'NONE', *, *, #23546, .T. ) ;
#22162=EDGE_CURVE ( 'NONE', #46621, #7146, #21360, .T. ) ;
#22166=EDGE_CURVE ( 'NONE', #5585, #24462, #8477, .T. ) ;
#22168=CARTESIAN_POINT ( 'NONE',  ( 11.99999999999999822, 0.000000000000000000, 0.000000000000000000 ) ) ;
#22172=VERTEX_POINT ( 'NONE', #42250 ) ;
#22173=CARTESIAN_POINT ( 'NONE',  ( 12.00000000000000000, 9.615535125379096826, 24.73947219025905042 ) ) ;
#22174=VERTEX_POINT ( 'NONE', #27332 ) ;
#22178=CARTESIAN_POINT ( 'NONE',  ( 0.000000000000000000, -77.32052557432837148, -5.256550761633681290 ) ) ;
#22184=VERTEX_POINT ( 'NONE', #27826 ) ;
#22187=DIRECTION ( 'NONE',  ( 1.000000000000000000, 0.000000000000000000, 0.000000000000000000 ) ) ;
#22192=CYLINDRICAL_SURFACE ( 'NONE', #3114, 31.99999999999998579 ) ;
#22193=LINE ( 'NONE', #41767, #30048 ) ;
#22201=AXIS2_PLACEMENT_3D ( 'NONE', #41960, #27756, #26769 ) ;
#22204=CARTESIAN_POINT ( 'NONE',  ( 0.000000000000000000, -5.256550761633393520, 77.32052557432838569 ) ) ;
#22205=VERTEX_POINT ( 'NONE', #26840 ) ;
#22210=EDGE_CURVE ( 'NONE', #59, #33522, #42749, .T. ) ;
#22212=VECTOR ( 'NONE', #44975, 999.9999999999998863 ) ;
#22214=CARTESIAN_POINT ( 'NONE',  ( -10.00000000000000000, 0.000000000000000000, 0.000000000000000000 ) ) ;
#22220=AXIS2_PLACEMENT_3D ( 'NONE', #2027, #1769, #20601 ) ;
#22223=VERTEX_POINT ( 'NONE', #16079 ) ;
#22224=EDGE_CURVE ( 'NONE', #7935, #45678, #27568, .T. ) ;
#22229=DIRECTION ( 'NONE',  ( -1.000000000000000000, -0.000000000000000000, 0.000000000000000000 ) ) ;
#22235=AXIS2_PLACEMENT_3D ( 'NONE', #29996, #30249, #4306 ) ;
#22237=ORIENTED_EDGE ( 'NONE', *, *, #17456, .F. ) ;
#22241=DIRECTION ( 'NONE',  ( 0.000000000000000000, 0.3826834323650905589, -0.9238795325112864054 ) ) ;
#22242=CIRCLE ( 'NONE', #10577, 82.00000000000000000 ) ;
#22245=CARTESIAN_POINT ( 'NONE',  ( 11.99999999999999822, 21.60688246758696351, -79.10210256391344785 ) ) ;
#22247=CIRCLE ( 'NONE', #48027, 31.99999999999998224 ) ;
#22249=AXIS2_PLACEMENT_3D ( 'NONE', #40479, #14038, #3503 ) ;
#22254=DIRECTION ( 'NONE',  ( -1.000000000000000000, -0.000000000000000000, 0.000000000000000000 ) ) ;
#22255=FACE_OUTER_BOUND ( 'NONE', #24596, .T. ) ;
#22259=DIRECTION ( 'NONE',  ( -1.000000000000000000, 0.000000000000000000, -0.000000000000000000 ) ) ;
#22260=ORIENTED_EDGE ( 'NONE', *, *, #9765, .T. ) ;
#22263=CARTESIAN_POINT ( 'NONE',  ( 11.99999999999999822, 41.76937507738788469, 62.50329211542452157 ) ) ;
#22264=CARTESIAN_POINT ( 'NONE',  ( 5.999999999999999112, 33.71516098798849015, -74.74816331893393340 ) ) ;
#22269=CIRCLE ( 'NONE', #8985, 31.99999999999998579 ) ;
#22270=CARTESIAN_POINT ( 'NONE',  ( 0.000000000000000000, -77.49459641780886443, -0.8261519478439277586 ) ) ;
#22275=LINE ( 'NONE', #47488, #39448 ) ;
#22277=DIRECTION ( 'NONE',  ( 0.000000000000000000, -0.9238795325112821866, -0.3826834323651008285 ) ) ;
#22278=ORIENTED_EDGE ( 'NONE', *, *, #36246, .F. ) ;
#22282=DIRECTION ( 'NONE',  ( 0.000000000000000000, 0.000000000000000000, 1.000000000000000000 ) ) ;
#22286=DIRECTION ( 'NONE',  ( 1.000000000000000000, -0.000000000000000000, -0.000000000000000000 ) ) ;
#22287=CIRCLE ( 'NONE', #40258, 82.00000000000000000 ) ;
#22288=EDGE_LOOP ( 'NONE', ( #40497, #45639, #3092, #20407 ) ) ;
#22289=VECTOR ( 'NONE', #19101, 1000.000000000000000 ) ;
#22290=VERTEX_POINT ( 'NONE', #14078 ) ;
#22291=DIRECTION ( 'NONE',  ( -1.000000000000000000, -0.000000000000000000, 0.000000000000000000 ) ) ;
#22296=VERTEX_POINT ( 'NONE', #39798 ) ;
#22297=ORIENTED_EDGE ( 'NONE', *, *, #6036, .F. ) ;
#22298=AXIS2_PLACEMENT_3D ( 'NONE', #37675, #25928, #40868 ) ;
#22300=DIRECTION ( 'NONE',  ( -1.000000000000000000, -0.000000000000000000, -0.000000000000000000 ) ) ;
#22304=VERTEX_POINT ( 'NONE', #17500 ) ;
#22317=AXIS2_PLACEMENT_3D ( 'NONE', #44392, #29220, #7182 ) ;
#22326=DIRECTION ( 'NONE',  ( -1.000000000000000000, -0.000000000000000000, -0.000000000000000000 ) ) ;
#22329=FACE_OUTER_BOUND ( 'NONE', #10470, .T. ) ;
#22331=CIRCLE ( 'NONE', #2748, 31.99999999999999289 ) ;
#22339=LINE ( 'NONE', #8365, #30201 ) ;
#22342=FACE_OUTER_BOUND ( 'NONE', #71, .T. ) ;
#22343=EDGE_CURVE ( 'NONE', #40483, #33807, #13852, .T. ) ;
#22350=CARTESIAN_POINT ( 'NONE',  ( 12.00000000000000000, -10.45096189432344502, -21.10159698893425073 ) ) ;
#22352=DIRECTION ( 'NONE',  ( 0.000000000000000000, 0.000000000000000000, 1.000000000000000000 ) ) ;
#22356=DIRECTION ( 'NONE',  ( -1.000000000000000000, 0.000000000000000000, 0.000000000000000000 ) ) ;
#22363=ORIENTED_EDGE ( 'NONE', *, *, #618, .F. ) ;
#22366=CIRCLE ( 'NONE', #45011, 82.00000000000000000 ) ;
#22370=CARTESIAN_POINT ( 'NONE',  ( 15.00000000000000000, -0.9646360437372099028, 23.52805723605590771 ) ) ;
#22375=LINE ( 'NONE', #3032, #10718 ) ;
#22383=ORIENTED_EDGE ( 'NONE', *, *, #15439, .T. ) ;
#22389=CYLINDRICAL_SURFACE ( 'NONE', #26237, 77.49899999999999523 ) ;
#22390=AXIS2_PLACEMENT_3D ( 'NONE', #6535, #9714, #17059 ) ;
#22394=VECTOR ( 'NONE', #34527, 1000.000000000000000 ) ;
#22395=FACE_OUTER_BOUND ( 'NONE', #20056, .T. ) ;
#22396=DIRECTION ( 'NONE',  ( -1.000000000000000000, -0.000000000000000000, -0.000000000000000000 ) ) ;
#22398=EDGE_CURVE ( 'NONE', #33047, #188, #4988, .T. ) ;
#22399=DIRECTION ( 'NONE',  ( -1.000000000000000000, 0.000000000000000000, 0.000000000000000000 ) ) ;
#22402=CIRCLE ( 'NONE', #1296, 82.00000000000000000 ) ;
#22403=CARTESIAN_POINT ( 'NONE',  ( 15.00000000000000000, -10.45096189432314127, 21.10159698893440350 ) ) ;
#22405=CIRCLE ( 'NONE', #25503, 31.99999999999998934 ) ;
#22406=FACE_OUTER_BOUND ( 'NONE', #15281, .T. ) ;
#22408=ORIENTED_EDGE ( 'NONE', *, *, #15133, .F. ) ;
#22412=ORIENTED_EDGE ( 'NONE', *, *, #17990, .F. ) ;
#22417=FACE_OUTER_BOUND ( 'NONE', #6158, .T. ) ;
#22423=DIRECTION ( 'NONE',  ( 1.000000000000000000, -0.000000000000000000, 0.000000000000000000 ) ) ;
#22426=ORIENTED_EDGE ( 'NONE', *, *, #12225, .T. ) ;
#22429=DIRECTION ( 'NONE',  ( -1.000000000000000000, -0.000000000000000000, -0.000000000000000000 ) ) ;
#22430=ORIENTED_EDGE ( 'NONE', *, *, #37873, .F. ) ;
#22434=ORIENTED_EDGE ( 'NONE', *, *, #35541, .T. ) ;
#22435=DIRECTION ( 'NONE',  ( 0.000000000000000000, 1.000000000000000000, 3.491481338843133355E-15 ) ) ;
#22438=CARTESIAN_POINT ( 'NONE',  ( -10.00000000000000000, 0.000000000000000000, 0.000000000000000000 ) ) ;
#22439=DIRECTION ( 'NONE',  ( 0.000000000000000000, 0.3090169943749410675, 0.9510565162951556406 ) ) ;
#22449=AXIS2_PLACEMENT_3D ( 'NONE', #43699, #28287, #9934 ) ;
#22451=ORIENTED_EDGE ( 'NONE', *, *, #12173, .F. ) ;
#22454=EDGE_LOOP ( 'NONE', ( #22363, #39418, #48363, #41167 ) ) ;
#22457=LINE ( 'NONE', #33935, #25215 ) ;
#22458=AXIS2_PLACEMENT_3D ( 'NONE', #37067, #2812, #43931 ) ;
#22461=CARTESIAN_POINT ( 'NONE',  ( 11.99999999999999822, 69.42325613327489009, -34.44570377933524696 ) ) ;
#22474=ORIENTED_EDGE ( 'NONE', *, *, #18157, .F. ) ;
#22476=DIRECTION ( 'NONE',  ( -1.000000000000000000, -0.000000000000000000, -0.000000000000000000 ) ) ;
#22478=EDGE_CURVE ( 'NONE', #31583, #45656, #17477, .T. ) ;
#22485=CARTESIAN_POINT ( 'NONE',  ( 11.99999999999999822, -29.01471420065506379, -76.69515212746047439 ) ) ;
#22491=CARTESIAN_POINT ( 'NONE',  ( 0.000000000000000000, 0.000000000000000000, 0.000000000000000000 ) ) ;
#22492=DIRECTION ( 'NONE',  ( -1.000000000000000000, -0.000000000000000000, 0.000000000000000000 ) ) ;
#22497=DIRECTION ( 'NONE',  ( 0.000000000000000000, 0.000000000000000000, 1.000000000000000000 ) ) ;
#22499=ORIENTED_EDGE ( 'NONE', *, *, #48139, .F. ) ;
#22502=ORIENTED_EDGE ( 'NONE', *, *, #41607, .F. ) ;
#22506=FACE_OUTER_BOUND ( 'NONE', #2142, .T. ) ;
#22510=LINE ( 'NONE', #25924, #45063 ) ;
#22511=CARTESIAN_POINT ( 'NONE',  ( 0.000000000000000000, 35.91791733033476675, 68.67312586195008350 ) ) ;
#22512=CARTESIAN_POINT ( 'NONE',  ( 0.000000000000000000, 0.000000000000000000, 0.000000000000000000 ) ) ;
#22513=ORIENTED_EDGE ( 'NONE', *, *, #27721, .F. ) ;
#22514=LINE ( 'NONE', #33516, #10379 ) ;
#22516=SURFACE_STYLE_FILL_AREA ( #485 ) ;
#22519=AXIS2_PLACEMENT_3D ( 'NONE', #37363, #48137, #33678 ) ;
#22522=AXIS2_PLACEMENT_3D ( 'NONE', #32850, #5533, #20455 ) ;
#22524=EDGE_CURVE ( 'NONE', #13690, #35068, #6740, .T. ) ;
#22528=CARTESIAN_POINT ( 'NONE',  ( 6.000000000000000000, -81.96053171279901051, -2.543863470249253300 ) ) ;
#22530=ORIENTED_EDGE ( 'NONE', *, *, #7422, .F. ) ;
#22531=ORIENTED_EDGE ( 'NONE', *, *, #44995, .F. ) ;
#22537=ORIENTED_EDGE ( 'NONE', *, *, #39068, .T. ) ;
#22542=CARTESIAN_POINT ( 'NONE',  ( 11.99999999999999822, 0.000000000000000000, 0.000000000000000000 ) ) ;
#22543=EDGE_CURVE ( 'NONE', #41271, #7167, #26309, .T. ) ;
#22545=VERTEX_POINT ( 'NONE', #36588 ) ;
#22550=CARTESIAN_POINT ( 'NONE',  ( 0.000000000000000000, 2.946379043146343246, 75.11764819372150725 ) ) ;
#22556=DIRECTION ( 'NONE',  ( -1.000000000000000000, -0.000000000000000000, -0.000000000000000000 ) ) ;
#22557=DIRECTION ( 'NONE',  ( 0.000000000000000000, 0.7071067811865486830, -0.7071067811865463515 ) ) ;
#22559=CIRCLE ( 'NONE', #48336, 77.49900000000002365 ) ;
#22562=CARTESIAN_POINT ( 'NONE',  ( 12.00000000000000000, 18.84667830672605859, 18.68964196561243085 ) ) ;
#22563=LINE ( 'NONE', #10824, #35455 ) ;
#22567=DIRECTION ( 'NONE',  ( -1.000000000000000000, -0.000000000000000000, -0.000000000000000000 ) ) ;
#22576=ORIENTED_EDGE ( 'NONE', *, *, #43344, .T. ) ;
#22581=DIRECTION ( 'NONE',  ( 0.000000000000000000, 0.000000000000000000, 1.000000000000000000 ) ) ;
#22585=CARTESIAN_POINT ( 'NONE',  ( 15.00000000000000000, -25.60904388321925040, -6.976881207771165272 ) ) ;
#22591=EDGE_LOOP ( 'NONE', ( #3622, #8215, #25912, #25332 ) ) ;
#22593=DIRECTION ( 'NONE',  ( 0.000000000000000000, -0.4539904997395351471, -0.8910065241883738940 ) ) ;
#22601=DIRECTION ( 'NONE',  ( -1.000000000000000000, -0.000000000000000000, 0.000000000000000000 ) ) ;
#22604=ORIENTED_EDGE ( 'NONE', *, *, #25412, .F. ) ;
#22616=CARTESIAN_POINT ( 'NONE',  ( 0.000000000000000000, 0.000000000000000000, 0.000000000000000000 ) ) ;
#22617=DIRECTION ( 'NONE',  ( 0.000000000000000000, 0.000000000000000000, 1.000000000000000000 ) ) ;
#22618=FACE_OUTER_BOUND ( 'NONE', #23796, .T. ) ;
#22619=AXIS2_PLACEMENT_3D ( 'NONE', #9545, #42861, #31862 ) ;
#22623=DIRECTION ( 'NONE',  ( -1.000000000000000000, 0.000000000000000000, -0.000000000000000000 ) ) ;
#22625=CARTESIAN_POINT ( 'NONE',  ( 0.000000000000000000, 0.000000000000000000, 0.000000000000000000 ) ) ;
#22631=DIRECTION ( 'NONE',  ( 0.000000000000000000, 0.5877852522924684742, 0.8090169943749507819 ) ) ;
#22632=ORIENTED_EDGE ( 'NONE', *, *, #4429, .T. ) ;
#22635=EDGE_CURVE ( 'NONE', #1236, #16242, #30697, .T. ) ;
#22642=CARTESIAN_POINT ( 'NONE',  ( 6.000000000000000000, -71.87247863392443037, 39.47590169984818687 ) ) ;
#22645=DIRECTION ( 'NONE',  ( -1.000000000000000000, 0.000000000000000000, 0.000000000000000000 ) ) ;
#22650=EDGE_LOOP ( 'NONE', ( #35559, #4816, #17110, #36300 ) ) ;
#22654=ADVANCED_FACE ( 'NONE', ( #16264 ), #31197, .T. ) ;
#22655=DIRECTION ( 'NONE',  ( 0.000000000000000000, 0.000000000000000000, -1.000000000000000000 ) ) ;
#22656=CARTESIAN_POINT ( 'NONE',  ( 6.000000000000000000, 29.01471420065563933, 76.69515212746026123 ) ) ;
#22658=ORIENTED_EDGE ( 'NONE', *, *, #21612, .T. ) ;
#22660=ORIENTED_EDGE ( 'NONE', *, *, #34204, .F. ) ;
#22664=DIRECTION ( 'NONE',  ( 0.000000000000000000, -0.3826834323650970537, 0.9238795325112838519 ) ) ;
#22666=DIRECTION ( 'NONE',  ( -1.000000000000000000, -0.000000000000000000, 0.000000000000000000 ) ) ;
#22667=DIRECTION ( 'NONE',  ( -1.000000000000000000, 0.000000000000000000, -0.000000000000000000 ) ) ;
#22674=EDGE_CURVE ( 'NONE', #461, #37099, #44038, .T. ) ;
#22677=CARTESIAN_POINT ( 'NONE',  ( 11.99999999999999822, 3.894527615419054456, -81.90746397400384637 ) ) ;
#22680=CARTESIAN_POINT ( 'NONE',  ( 11.99999999999999822, 0.000000000000000000, 0.000000000000000000 ) ) ;
#22682=CIRCLE ( 'NONE', #1585, 82.00000000000000000 ) ;
#22691=AXIS2_PLACEMENT_3D ( 'NONE', #4951, #20599, #46565 ) ;
#22700=CARTESIAN_POINT ( 'NONE',  ( 0.000000000000000000, 0.000000000000000000, 0.000000000000000000 ) ) ;
#22702=ADVANCED_FACE ( 'NONE', ( #13074 ), #28004, .F. ) ;
#22710=CIRCLE ( 'NONE', #32870, 82.00000000000000000 ) ;
#22712=VECTOR ( 'NONE', #36387, 1000.000000000000000 ) ;
#22713=DIRECTION ( 'NONE',  ( -1.000000000000000000, 0.000000000000000000, 0.000000000000000000 ) ) ;
#22714=EDGE_CURVE ( 'NONE', #11938, #3320, #36291, .T. ) ;
#22719=CIRCLE ( 'NONE', #4768, 31.99999999999998579 ) ;
#22722=VERTEX_POINT ( 'NONE', #27767 ) ;
#22727=EDGE_CURVE ( 'NONE', #34943, #39901, #27661, .T. ) ;
#22728=CARTESIAN_POINT ( 'NONE',  ( 11.99999999999999822, 63.18004540533092239, -44.88180994100307686 ) ) ;
#22729=ORIENTED_EDGE ( 'NONE', *, *, #31372, .F. ) ;
#22738=CARTESIAN_POINT ( 'NONE',  ( 11.99999999999999822, -8.830959090341869100, -74.65491531819127147 ) ) ;
#22740=CARTESIAN_POINT ( 'NONE',  ( 0.000000000000000000, 14.66109333815564852, -73.73191006444555740 ) ) ;
#22744=CARTESIAN_POINT ( 'NONE',  ( 11.99999999999999822, 26.02418014898310261, 70.52718814184268581 ) ) ;
#22747=EDGE_LOOP ( 'NONE', ( #7038, #39397, #33545, #35492 ) ) ;
#22750=FACE_OUTER_BOUND ( 'NONE', #12611, .T. ) ;
#22756=EDGE_CURVE ( 'NONE', #15029, #20027, #20643, .T. ) ;
#22757=ORIENTED_EDGE ( 'NONE', *, *, #47137, .T. ) ;
#22758=EDGE_CURVE ( 'NONE', #2924, #7777, #16974, .T. ) ;
#22765=ORIENTED_EDGE ( 'NONE', *, *, #6359, .T. ) ;
#22769=ORIENTED_EDGE ( 'NONE', *, *, #40301, .F. ) ;
#22771=ORIENTED_EDGE ( 'NONE', *, *, #14392, .T. ) ;
#22772=EDGE_CURVE ( 'NONE', #12014, #31321, #24558, .T. ) ;
#22775=EDGE_LOOP ( 'NONE', ( #859, #1752, #47674, #2643 ) ) ;
#22776=FACE_OUTER_BOUND ( 'NONE', #8615, .T. ) ;
#22778=EDGE_LOOP ( 'NONE', ( #41386, #15252, #11275, #32014 ) ) ;
#22779=ORIENTED_EDGE ( 'NONE', *, *, #40122, .F. ) ;
#22795=VECTOR ( 'NONE', #28568, 1000.000000000000114 ) ;
#22801=DIRECTION ( 'NONE',  ( 0.000000000000000000, 0.000000000000000000, 1.000000000000000000 ) ) ;
#22802=DIRECTION ( 'NONE',  ( 1.000000000000000000, 0.000000000000000000, 0.000000000000000000 ) ) ;
#22804=ORIENTED_EDGE ( 'NONE', *, *, #38189, .T. ) ;
#22807=CARTESIAN_POINT ( 'NONE',  ( 11.99999999999999822, -26.02418014898359289, 70.52718814184250107 ) ) ;
#22813=CARTESIAN_POINT ( 'NONE',  ( 11.99999999999999822, -54.21277698773713638, 55.38113227695764351 ) ) ;
#22825=VERTEX_POINT ( 'NONE', #40464 ) ;
#22827=AXIS2_PLACEMENT_3D ( 'NONE', #34349, #14576, #29491 ) ;
#22829=AXIS2_PLACEMENT_3D ( 'NONE', #7960, #48362, #14612 ) ;
#22831=EDGE_LOOP ( 'NONE', ( #27425, #14098, #5572, #34374 ) ) ;
#22832=AXIS2_PLACEMENT_3D ( 'NONE', #23164, #4562, #34394 ) ;
#22838=ORIENTED_EDGE ( 'NONE', *, *, #26167, .T. ) ;
#22839=DIRECTION ( 'NONE',  ( 0.000000000000000000, 0.000000000000000000, 1.000000000000000000 ) ) ;
#22840=DIRECTION ( 'NONE',  ( -1.000000000000000000, 0.000000000000000000, 0.000000000000000000 ) ) ;
#22847=CARTESIAN_POINT ( 'NONE',  ( 11.99999999999999822, -55.19960302592029677, -51.03279382321147750 ) ) ;
#22851=FACE_OUTER_BOUND ( 'NONE', #30602, .T. ) ;
#22854=FACE_OUTER_BOUND ( 'NONE', #21449, .T. ) ;
#22855=DIRECTION ( 'NONE',  ( -1.000000000000000000, -0.000000000000000000, -0.000000000000000000 ) ) ;
#22857=CYLINDRICAL_SURFACE ( 'NONE', #21548, 31.99999999999998579 ) ;
#22860=DIRECTION ( 'NONE',  ( 0.000000000000000000, -0.5877852522924797984, -0.8090169943749426773 ) ) ;
#22865=AXIS2_PLACEMENT_3D ( 'NONE', #22738, #11004, #48205 ) ;
#22866=CYLINDRICAL_SURFACE ( 'NONE', #12214, 77.49899999999999523 ) ;
#22872=EDGE_CURVE ( 'NONE', #2440, #46432, #9694, .T. ) ;
#22876=ADVANCED_FACE ( 'NONE', ( #6687 ), #48032, .T. ) ;
#22878=ORIENTED_EDGE ( 'NONE', *, *, #39947, .F. ) ;
#22883=ORIENTED_EDGE ( 'NONE', *, *, #28892, .F. ) ;
#22886=CYLINDRICAL_SURFACE ( 'NONE', #10116, 77.49899999999999523 ) ;
#22887=AXIS2_PLACEMENT_3D ( 'NONE', #45010, #458, #37906 ) ;
#22891=AXIS2_PLACEMENT_3D ( 'NONE', #688, #30551, #45475 ) ;
#22895=CYLINDRICAL_SURFACE ( 'NONE', #6873, 82.00000000000000000 ) ;
#22896=CARTESIAN_POINT ( 'NONE',  ( 15.00000000000000000, -10.45096189432314127, 21.10159698893440350 ) ) ;
#22897=FACE_OUTER_BOUND ( 'NONE', #26699, .T. ) ;
#22898=ORIENTED_EDGE ( 'NONE', *, *, #33025, .T. ) ;
#22903=ORIENTED_EDGE ( 'NONE', *, *, #14929, .T. ) ;
#22904=LINE ( 'NONE', #37839, #34747 ) ;
#22908=CARTESIAN_POINT ( 'NONE',  ( 11.99999999999999822, 63.97538442413427617, 51.29473840253247374 ) ) ;
#22912=VERTEX_POINT ( 'NONE', #36535 ) ;
#22915=ORIENTED_EDGE ( 'NONE', *, *, #6457, .T. ) ;
#22916=VERTEX_POINT ( 'NONE', #7407 ) ;
#22919=CYLINDRICAL_SURFACE ( 'NONE', #23053, 31.99999999999998579 ) ;
#22926=VECTOR ( 'NONE', #43535, 1000.000000000000000 ) ;
#22930=AXIS2_PLACEMENT_3D ( 'NONE', #13993, #10312, #11538 ) ;
#22936=ADVANCED_FACE ( 'NONE', ( #29440 ), #33348, .T. ) ;
#22937=EDGE_CURVE ( 'NONE', #36554, #7777, #3428, .T. ) ;
#22938=VERTEX_POINT ( 'NONE', #37262 ) ;
#22939=AXIS2_PLACEMENT_3D ( 'NONE', #9824, #39707, #27720 ) ;
#22940=AXIS2_PLACEMENT_3D ( 'NONE', #38283, #27038, #45377 ) ;
#22943=CARTESIAN_POINT ( 'NONE',  ( 11.99999999999999822, -75.54627589209955829, 17.28742895386058009 ) ) ;
#22944=CARTESIAN_POINT ( 'NONE',  ( 12.00000000000000000, 23.49999999999999645, -1.500000000000003997 ) ) ;
#22951=VERTEX_POINT ( 'NONE', #29912 ) ;
#22952=AXIS2_PLACEMENT_3D ( 'NONE', #12836, #20648, #35586 ) ;
#22954=DIRECTION ( 'NONE',  ( -1.000000000000000000, 0.000000000000000000, 0.000000000000000000 ) ) ;
#22960=LINE ( 'NONE', #12208, #4850 ) ;
#22962=VECTOR ( 'NONE', #19699, 1000.000000000000000 ) ;
#22966=ORIENTED_EDGE ( 'NONE', *, *, #9750, .T. ) ;
#22970=CIRCLE ( 'NONE', #45646, 77.49899999999999523 ) ;
#22971=AXIS2_PLACEMENT_3D ( 'NONE', #2763, #17696, #47546 ) ;
#22980=CARTESIAN_POINT ( 'NONE',  ( 0.000000000000000000, -8.840884882374576037, -74.65374052328658649 ) ) ;
#22982=CYLINDRICAL_SURFACE ( 'NONE', #23784, 31.99999999999998579 ) ;
#22983=CYLINDRICAL_SURFACE ( 'NONE', #22865, 31.99999999999998579 ) ;
#22984=CARTESIAN_POINT ( 'NONE',  ( 11.99999999999999822, -75.11764819372145041, -2.946379043147127064 ) ) ;
#22985=EDGE_CURVE ( 'NONE', #21783, #43334, #21393, .T. ) ;
#22988=CYLINDRICAL_SURFACE ( 'NONE', #45832, 31.99999999999998579 ) ;
#22994=DIRECTION ( 'NONE',  ( 0.000000000000000000, -0.3826834323650774583, -0.9238795325112919565 ) ) ;
#22996=EDGE_CURVE ( 'NONE', #6721, #43680, #8921, .T. ) ;
#22999=DIRECTION ( 'NONE',  ( -1.000000000000000000, 0.000000000000000000, 0.000000000000000000 ) ) ;
#23000=AXIS2_PLACEMENT_3D ( 'NONE', #28460, #13784, #32144 ) ;
#23001=AXIS2_PLACEMENT_3D ( 'NONE', #33881, #26785, #34596 ) ;
#23004=CARTESIAN_POINT ( 'NONE',  ( -10.00000000000000000, 0.000000000000000000, 0.000000000000000000 ) ) ;
#23005=ORIENTED_EDGE ( 'NONE', *, *, #35938, .T. ) ;
#23008=AXIS2_PLACEMENT_3D ( 'NONE', #240, #27353, #29869 ) ;
#23016=AXIS2_PLACEMENT_3D ( 'NONE', #26356, #33213, #37848 ) ;
#23017=CARTESIAN_POINT ( 'NONE',  ( 0.000000000000000000, 71.91182617369230456, -28.89263327155667938 ) ) ;
#23023=DIRECTION ( 'NONE',  ( -1.000000000000000000, -0.000000000000000000, -0.000000000000000000 ) ) ;
#23027=VERTEX_POINT ( 'NONE', #15959 ) ;
#23030=DIRECTION ( 'NONE',  ( 0.000000000000000000, -0.3090169943749471737, 0.9510565162951537532 ) ) ;
#23031=EDGE_LOOP ( 'NONE', ( #2470, #18949, #35349, #24737 ) ) ;
#23032=CYLINDRICAL_SURFACE ( 'NONE', #16240, 77.49899999999999523 ) ;
#23034=VERTEX_POINT ( 'NONE', #8121 ) ;
#23036=AXIS2_PLACEMENT_3D ( 'NONE', #37580, #44930, #617 ) ;
#23038=EDGE_CURVE ( 'NONE', #14224, #5001, #23298, .T. ) ;
#23045=DIRECTION ( 'NONE',  ( -1.000000000000000000, -0.000000000000000000, -0.000000000000000000 ) ) ;
#23051=LINE ( 'NONE', #30404, #592 ) ;
#23053=AXIS2_PLACEMENT_3D ( 'NONE', #1131, #13305, #42248 ) ;
#23055=CARTESIAN_POINT ( 'NONE',  ( 0.000000000000000000, -51.29473840253177030, -63.97538442413482329 ) ) ;
#23057=CARTESIAN_POINT ( 'NONE',  ( 11.99999999999999822, 17.28742895386084655, 75.54627589209950145 ) ) ;
#23061=FACE_BOUND ( 'NONE', #25820, .T. ) ;
#23062=VERTEX_POINT ( 'NONE', #41419 ) ;
#23074=EDGE_CURVE ( 'NONE', #26344, #24460, #766, .T. ) ;
#23077=DIRECTION ( 'NONE',  ( -1.000000000000000000, 0.000000000000000000, 0.000000000000000000 ) ) ;
#23078=DIRECTION ( 'NONE',  ( 0.000000000000000000, 0.000000000000000000, 1.000000000000000000 ) ) ;
#23081=VECTOR ( 'NONE', #28390, 1000.000000000000000 ) ;
#23083=CIRCLE ( 'NONE', #19932, 31.99999999999998934 ) ;
#23087=CARTESIAN_POINT ( 'NONE',  ( 0.000000000000000000, -59.03342792756231461, -46.54456581323868392 ) ) ;
#23088=DIRECTION ( 'NONE',  ( 0.000000000000000000, 0.6691306063588661202, 0.7431448254773871387 ) ) ;
#23096=FACE_OUTER_BOUND ( 'NONE', #1536, .T. ) ;
#23098=DIRECTION ( 'NONE',  ( -1.000000000000000000, 0.000000000000000000, 0.000000000000000000 ) ) ;
#23100=FACE_OUTER_BOUND ( 'NONE', #12940, .T. ) ;
#23101=CARTESIAN_POINT ( 'NONE',  ( 11.99999999999999822, 68.27212725128275395, 31.46837873495001503 ) ) ;
#23102=ORIENTED_EDGE ( 'NONE', *, *, #30777, .T. ) ;
#23105=EDGE_CURVE ( 'NONE', #48222, #29618, #3478, .T. ) ;
#23106=CYLINDRICAL_SURFACE ( 'NONE', #36019, 31.99999999999998579 ) ;
#23107=DIRECTION ( 'NONE',  ( -1.000000000000000000, 0.000000000000000000, 0.000000000000000000 ) ) ;
#23108=AXIS2_PLACEMENT_3D ( 'NONE', #9145, #5243, #36045 ) ;
#23110=FACE_OUTER_BOUND ( 'NONE', #28343, .T. ) ;
#23111=DIRECTION ( 'NONE',  ( -0.000000000000000000, 0.8090169943749491166, 0.5877852522924709167 ) ) ;
#23114=FACE_OUTER_BOUND ( 'NONE', #35696, .T. ) ;
#23116=FACE_OUTER_BOUND ( 'NONE', #9583, .T. ) ;
#23119=LINE ( 'NONE', #45157, #47972 ) ;
#23123=AXIS2_PLACEMENT_3D ( 'NONE', #8881, #23821, #35070 ) ;
#23129=ORIENTED_EDGE ( 'NONE', *, *, #25291, .F. ) ;
#23132=ORIENTED_EDGE ( 'NONE', *, *, #140, .T. ) ;
#23137=FACE_OUTER_BOUND ( 'NONE', #17060, .T. ) ;
#23144=CYLINDRICAL_SURFACE ( 'NONE', #1697, 31.99999999999998579 ) ;
#23145=CIRCLE ( 'NONE', #40382, 82.00000000000000000 ) ;
#23148=DIRECTION ( 'NONE',  ( 1.000000000000000000, 0.000000000000000000, 0.000000000000000000 ) ) ;
#23149=ORIENTED_EDGE ( 'NONE', *, *, #14151, .F. ) ;
#23151=DIRECTION ( 'NONE',  ( 0.000000000000000000, 0.000000000000000000, 1.000000000000000000 ) ) ;
#23153=DIRECTION ( 'NONE',  ( 0.000000000000000000, 0.8526401643540935105, -0.5224985647159466895 ) ) ;
#23154=DIRECTION ( 'NONE',  ( 0.000000000000000000, -0.4539904997395350361, -0.8910065241883738940 ) ) ;
#23157=EDGE_CURVE ( 'NONE', #47105, #6091, #37087, .T. ) ;
#23162=DIRECTION ( 'NONE',  ( 0.000000000000000000, -0.7431448254773878048, 0.6691306063588654540 ) ) ;
#23164=CARTESIAN_POINT ( 'NONE',  ( 0.000000000000000000, -65.58780272294100655, 36.73666225445870737 ) ) ;
#23167=VERTEX_POINT ( 'NONE', #20830 ) ;
#23168=DIRECTION ( 'NONE',  ( 0.000000000000000000, -0.9945218953682742891, -0.1045284632676436315 ) ) ;
#23171=VECTOR ( 'NONE', #18416, 1000.000000000000114 ) ;
#23172=EDGE_CURVE ( 'NONE', #26733, #19547, #20329, .T. ) ;
#23175=AXIS2_PLACEMENT_3D ( 'NONE', #34269, #38438, #12991 ) ;
#23177=DIRECTION ( 'NONE',  ( 0.000000000000000000, 0.9723699203976773342, -0.2334453638559024491 ) ) ;
#23179=CARTESIAN_POINT ( 'NONE',  ( 11.99999999999999822, 0.000000000000000000, 0.000000000000000000 ) ) ;
#23182=ORIENTED_EDGE ( 'NONE', *, *, #42134, .T. ) ;
#23186=CIRCLE ( 'NONE', #45882, 77.49899999999999523 ) ;
#23190=EDGE_CURVE ( 'NONE', #3822, #38262, #20574, .T. ) ;
#23201=AXIS2_PLACEMENT_3D ( 'NONE', #23905, #45943, #31987 ) ;
#23202=CARTESIAN_POINT ( 'NONE',  ( 0.000000000000000000, 8.966570791701871102, -81.50828551894218776 ) ) ;
#23206=VERTEX_POINT ( 'NONE', #35271 ) ;
#23207=CARTESIAN_POINT ( 'NONE',  ( 11.99999999999999822, 58.39081064771822582, -50.95692526931267707 ) ) ;
#23216=AXIS2_PLACEMENT_3D ( 'NONE', #26544, #37317, #19417 ) ;
#23217=DIRECTION ( 'NONE',  ( 0.000000000000000000, 1.000000000000000000, 1.445602896647339410E-16 ) ) ;
#23218=VECTOR ( 'NONE', #10382, 1000.000000000000000 ) ;
#23225=AXIS2_PLACEMENT_3D ( 'NONE', #8528, #16143, #11979 ) ;
#23226=CARTESIAN_POINT ( 'NONE',  ( 6.000000000000000000, 79.10210256391398786, -21.60688246758503794 ) ) ;
#23230=DIRECTION ( 'NONE',  ( 0.000000000000000000, 0.9945218953682742891, 0.1045284632676436315 ) ) ;
#23233=CARTESIAN_POINT ( 'NONE',  ( 11.99999999999999822, -24.73286445877655382, -73.44644590900085745 ) ) ;
#23236=ADVANCED_FACE ( 'NONE', ( #24252 ), #39192, .F. ) ;
#23249=ORIENTED_EDGE ( 'NONE', *, *, #12401, .F. ) ;
#23251=AXIS2_PLACEMENT_3D ( 'NONE', #24538, #20873, #46330 ) ;
#23252=EDGE_CURVE ( 'NONE', #45060, #526, #43361, .T. ) ;
#23253=CARTESIAN_POINT ( 'NONE',  ( 0.000000000000000000, -77.16300072079641836, -27.74655509720752278 ) ) ;
#23261=CARTESIAN_POINT ( 'NONE',  ( 0.000000000000000000, -8.966570791700167575, -81.50828551894237251 ) ) ;
#23263=ORIENTED_EDGE ( 'NONE', *, *, #40249, .T. ) ;
#23270=EDGE_CURVE ( 'NONE', #2149, #24044, #10776, .T. ) ;
#23272=EDGE_CURVE ( 'NONE', #43433, #11777, #41787, .T. ) ;
#23277=VERTEX_POINT ( 'NONE', #40400 ) ;
#23278=DIRECTION ( 'NONE',  ( -1.000000000000000000, 0.000000000000000000, -0.000000000000000000 ) ) ;
#23280=DIRECTION ( 'NONE',  ( 0.000000000000000000, 0.000000000000000000, 1.000000000000000000 ) ) ;
#23284=DIRECTION ( 'NONE',  ( 0.000000000000000000, -0.07845909572785234043, 0.9969173337331274087 ) ) ;
#23298=LINE ( 'NONE', #30173, #4230 ) ;
#23300=CIRCLE ( 'NONE', #38148, 77.49900000000000944 ) ;
#23302=FACE_BOUND ( 'NONE', #39641, .T. ) ;
#23311=ORIENTED_EDGE ( 'NONE', *, *, #45758, .F. ) ;
#23314=DIRECTION ( 'NONE',  ( 1.000000000000000000, 0.000000000000000000, 0.000000000000000000 ) ) ;
#23320=AXIS2_PLACEMENT_3D ( 'NONE', #8591, #13021, #41656 ) ;
#23329=ORIENTED_EDGE ( 'NONE', *, *, #9252, .T. ) ;
#23332=FACE_OUTER_BOUND ( 'NONE', #5737, .T. ) ;
#23338=DIRECTION ( 'NONE',  ( 0.000000000000000000, 0.4067366430757908824, -0.9135454576426050854 ) ) ;
#23339=DIRECTION ( 'NONE',  ( -1.000000000000000000, -0.000000000000000000, -0.000000000000000000 ) ) ;
#23365=EDGE_CURVE ( 'NONE', #11714, #17149, #22275, .T. ) ;
#23371=DIRECTION ( 'NONE',  ( 0.000000000000000000, 0.000000000000000000, 1.000000000000000000 ) ) ;
#23383=FACE_OUTER_BOUND ( 'NONE', #29005, .T. ) ;
#23384=VECTOR ( 'NONE', #29800, 1000.000000000000000 ) ;
#23387=CYLINDRICAL_SURFACE ( 'NONE', #42508, 77.49899999999999523 ) ;
#23388=CARTESIAN_POINT ( 'NONE',  ( 11.99999999999999822, -0.8261519478436571973, 77.49459641780886443 ) ) ;
#23389=DIRECTION ( 'NONE',  ( 0.000000000000000000, -0.7071067811865536790, 0.7071067811865414665 ) ) ;
#23397=ORIENTED_EDGE ( 'NONE', *, *, #16636, .T. ) ;
#23398=CIRCLE ( 'NONE', #47634, 31.99999999999999645 ) ;
#23401=CARTESIAN_POINT ( 'NONE',  ( 5.999999999999999112, 51.29473840253223216, 63.97538442413444670 ) ) ;
#23402=DIRECTION ( 'NONE',  ( -1.000000000000000000, 0.000000000000000000, -0.000000000000000000 ) ) ;
#23410=ORIENTED_EDGE ( 'NONE', *, *, #33166, .T. ) ;
#23418=ADVANCED_FACE ( 'NONE', ( #4633 ), #30350, .T. ) ;
#23437=ORIENTED_EDGE ( 'NONE', *, *, #17209, .T. ) ;
#23443=DIRECTION ( 'NONE',  ( -1.000000000000000000, 0.000000000000000000, -0.000000000000000000 ) ) ;
#23445=VERTEX_POINT ( 'NONE', #38168 ) ;
#23447=CARTESIAN_POINT ( 'NONE',  ( 11.99999999999999822, -11.30684508768393748, 76.66974797899833050 ) ) ;
#23453=AXIS2_PLACEMENT_3D ( 'NONE', #32801, #18112, #47730 ) ;
#23454=DIRECTION ( 'NONE',  ( 0.000000000000000000, 0.7604059656000276002, 0.6494480483301876550 ) ) ;
#23455=CARTESIAN_POINT ( 'NONE',  ( 11.99999999999999822, 73.73191006444551476, 14.66109333815590254 ) ) ;
#23462=DIRECTION ( 'NONE',  ( 0.000000000000000000, 0.000000000000000000, 1.000000000000000000 ) ) ;
#23466=( LENGTH_UNIT ( ) NAMED_UNIT ( * ) SI_UNIT ( .MILLI., .METRE. ) );
#23467=DIRECTION ( 'NONE',  ( -1.000000000000000000, 0.000000000000000000, 0.000000000000000000 ) ) ;
#23468=VERTEX_POINT ( 'NONE', #45271 ) ;
#23474=FACE_OUTER_BOUND ( 'NONE', #47527, .T. ) ;
#23477=ADVANCED_FACE ( 'NONE', ( #7587 ), #712, .T. ) ;
#23479=AXIS2_PLACEMENT_3D ( 'NONE', #9347, #45582, #30924 ) ;
#23484=ORIENTED_EDGE ( 'NONE', *, *, #42329, .F. ) ;
#23491=VECTOR ( 'NONE', #13781, 1000.000000000000000 ) ;
#23492=DIRECTION ( 'NONE',  ( 0.000000000000000000, 0.1564344650402311743, -0.9876883405951376593 ) ) ;
#23493=AXIS2_PLACEMENT_3D ( 'NONE', #42356, #13226, #32307 ) ;
#23499=CARTESIAN_POINT ( 'NONE',  ( 15.00000000000000000, -3.948201729842355068, -23.21447184625292692 ) ) ;
#23500=DIRECTION ( 'NONE',  ( -1.000000000000000000, -0.000000000000000000, -0.000000000000000000 ) ) ;
#23502=DIRECTION ( 'NONE',  ( -1.000000000000000000, -0.000000000000000000, -0.000000000000000000 ) ) ;
#23503=ORIENTED_EDGE ( 'NONE', *, *, #16087, .T. ) ;
#23504=ADVANCED_FACE ( 'NONE', ( #37930 ), #15178, .T. ) ;
#23516=CARTESIAN_POINT ( 'NONE',  ( 11.99999999999999822, 65.58780272294129077, -36.73666225445822420 ) ) ;
#23519=EDGE_CURVE ( 'NONE', #27398, #43433, #41365, .T. ) ;
#23522=CARTESIAN_POINT ( 'NONE',  ( 0.000000000000000000, 0.000000000000000000, 0.000000000000000000 ) ) ;
#23523=CIRCLE ( 'NONE', #15706, 77.49900000000000944 ) ;
#23528=CARTESIAN_POINT ( 'NONE',  ( 15.00000000000000000, -13.04903810567675393, -19.60159698893424718 ) ) ;
#23533=ORIENTED_EDGE ( 'NONE', *, *, #30016, .T. ) ;
#23534=DIRECTION ( 'NONE',  ( -1.000000000000000000, -0.000000000000000000, 0.000000000000000000 ) ) ;
#23535=MECHANICAL_DESIGN_GEOMETRIC_PRESENTATION_REPRESENTATION('',(#25064),#40725);
#23540=VERTEX_POINT ( 'NONE', #2119 ) ;
#23542=EDGE_CURVE ( 'NONE', #32361, #44059, #6037, .T. ) ;
#23543=CARTESIAN_POINT ( 'NONE',  ( 12.00000000000000000, -3.948201729842032215, 23.21447184625297666 ) ) ;
#23546=EDGE_CURVE ( 'NONE', #45870, #6838, #39481, .T. ) ;
#23548=CYLINDRICAL_SURFACE ( 'NONE', #18297, 82.00000000000000000 ) ;
#23549=AXIS2_PLACEMENT_3D ( 'NONE', #9906, #40261, #6237 ) ;
#23552=DIRECTION ( 'NONE',  ( -1.000000000000000000, -0.000000000000000000, 0.000000000000000000 ) ) ;
#23555=ORIENTED_EDGE ( 'NONE', *, *, #32332, .F. ) ;
#23561=CARTESIAN_POINT ( 'NONE',  ( 11.99999999999999822, -55.20638768913724448, -51.02545421589383068 ) ) ;
#23572=ORIENTED_EDGE ( 'NONE', *, *, #21965, .F. ) ;
#23586=ORIENTED_EDGE ( 'NONE', *, *, #14085, .T. ) ;
#23591=EDGE_LOOP ( 'NONE', ( #33923, #35459, #19434, #3569 ) ) ;
#23592=ORIENTED_EDGE ( 'NONE', *, *, #45786, .T. ) ;
#23601=EDGE_CURVE ( 'NONE', #15144, #12730, #13367, .T. ) ;
#23602=VERTEX_POINT ( 'NONE', #32218 ) ;
#23607=EDGE_CURVE ( 'NONE', #29157, #42296, #19924, .T. ) ;
#23612=CARTESIAN_POINT ( 'NONE',  ( 0.000000000000000000, 0.000000000000000000, 0.000000000000000000 ) ) ;
#23614=ORIENTED_EDGE ( 'NONE', *, *, #20834, .F. ) ;
#23618=CIRCLE ( 'NONE', #4063, 82.00000000000000000 ) ;
#23620=ORIENTED_EDGE ( 'NONE', *, *, #382, .F. ) ;
#23623=AXIS2_PLACEMENT_3D ( 'NONE', #20803, #38699, #12988 ) ;
#23624=DIRECTION ( 'NONE',  ( 0.000000000000000000, 0.000000000000000000, 1.000000000000000000 ) ) ;
#23626=FACE_OUTER_BOUND ( 'NONE', #21204, .T. ) ;
#23628=CARTESIAN_POINT ( 'NONE',  ( 0.000000000000000000, -71.87247863392384772, -39.47590169984923136 ) ) ;
#23630=CIRCLE ( 'NONE', #19733, 82.00000000000000000 ) ;
#23635=CYLINDRICAL_SURFACE ( 'NONE', #17588, 31.99999999999998579 ) ;
#23642=DIRECTION ( 'NONE',  ( 0.000000000000000000, 0.000000000000000000, 1.000000000000000000 ) ) ;
#23647=CARTESIAN_POINT ( 'NONE',  ( 0.000000000000000000, 2.946379043147425492, -75.11764819372145041 ) ) ;
#23651=VERTEX_POINT ( 'NONE', #9684 ) ;
#23653=VERTEX_POINT ( 'NONE', #25809 ) ;
#23654=VECTOR ( 'NONE', #15004, 1000.000000000000114 ) ;
#23660=ORIENTED_EDGE ( 'NONE', *, *, #39061, .T. ) ;
#23662=EDGE_CURVE ( 'NONE', #30137, #7347, #2735, .T. ) ;
#23663=VERTEX_POINT ( 'NONE', #14815 ) ;
#23665=CIRCLE ( 'NONE', #31515, 82.00000000000000000 ) ;
#23673=LINE ( 'NONE', #11286, #41740 ) ;
#23676=DIRECTION ( 'NONE',  ( -1.000000000000000000, -0.000000000000000000, -0.000000000000000000 ) ) ;
#23680=DIRECTION ( 'NONE',  ( 0.000000000000000000, -0.7071067811865536790, 0.7071067811865414665 ) ) ;
#23683=DIRECTION ( 'NONE',  ( -1.000000000000000000, 0.000000000000000000, 0.000000000000000000 ) ) ;
#23691=AXIS2_PLACEMENT_3D ( 'NONE', #32566, #17144, #31870 ) ;
#23693=CARTESIAN_POINT ( 'NONE',  ( 0.000000000000000000, -77.32052557432845674, 5.256550761632577284 ) ) ;
#23697=ORIENTED_EDGE ( 'NONE', *, *, #29993, .T. ) ;
#23698=AXIS2_PLACEMENT_3D ( 'NONE', #16785, #27321, #23389 ) ;
#23704=DIRECTION ( 'NONE',  ( 0.000000000000000000, 0.000000000000000000, -1.000000000000000000 ) ) ;
#23705=CIRCLE ( 'NONE', #1838, 77.49899999999999523 ) ;
#23709=VECTOR ( 'NONE', #48047, 1000.000000000000000 ) ;
#23710=VECTOR ( 'NONE', #46598, 1000.000000000000000 ) ;
#23713=EDGE_CURVE ( 'NONE', #36455, #4586, #21508, .T. ) ;
#23714=CIRCLE ( 'NONE', #25271, 77.49899999999999523 ) ;
#23717=ORIENTED_EDGE ( 'NONE', *, *, #13798, .T. ) ;
#23718=DIRECTION ( 'NONE',  ( -1.000000000000000000, 0.000000000000000000, 0.000000000000000000 ) ) ;
#23725=AXIS2_PLACEMENT_3D ( 'NONE', #33153, #7453, #7920 ) ;
#23726=CIRCLE ( 'NONE', #38599, 77.49899999999999523 ) ;
#23730=ORIENTED_EDGE ( 'NONE', *, *, #7285, .T. ) ;
#23731=ORIENTED_EDGE ( 'NONE', *, *, #32752, .T. ) ;
#23733=ORIENTED_EDGE ( 'NONE', *, *, #14091, .F. ) ;
#23738=ORIENTED_EDGE ( 'NONE', *, *, #20289, .F. ) ;
#23739=CIRCLE ( 'NONE', #42518, 31.99999999999998224 ) ;
#23742=DIRECTION ( 'NONE',  ( 0.000000000000000000, 0.000000000000000000, 1.000000000000000000 ) ) ;
#23748=CARTESIAN_POINT ( 'NONE',  ( 0.000000000000000000, 6.903761155837791819, 77.19088730480525840 ) ) ;
#23750=ORIENTED_EDGE ( 'NONE', *, *, #47425, .F. ) ;
#23753=EDGE_LOOP ( 'NONE', ( #6691, #12193, #4176, #15064 ) ) ;
#23757=CARTESIAN_POINT ( 'NONE',  ( 11.99999999999999822, 41.19522573413826194, -65.64334221924865176 ) ) ;
#23758=DIRECTION ( 'NONE',  ( 0.000000000000000000, -0.2079116908177532363, 0.9781476007338069101 ) ) ;
#23760=EDGE_CURVE ( 'NONE', #5341, #20027, #27780, .T. ) ;
#23765=VECTOR ( 'NONE', #30883, 1000.000000000000000 ) ;
#23778=VERTEX_POINT ( 'NONE', #10900 ) ;
#23779=VERTEX_POINT ( 'NONE', #18483 ) ;
#23782=AXIS2_PLACEMENT_3D ( 'NONE', #14997, #44603, #29187 ) ;
#23784=AXIS2_PLACEMENT_3D ( 'NONE', #18339, #33020, #37188 ) ;
#23792=DIRECTION ( 'NONE',  ( -1.000000000000000000, 0.000000000000000000, 0.000000000000000000 ) ) ;
#23796=EDGE_LOOP ( 'NONE', ( #36618, #34504, #12864, #30015 ) ) ;
#23797=CIRCLE ( 'NONE', #41770, 31.99999999999998224 ) ;
#23799=CARTESIAN_POINT ( 'NONE',  ( -10.00000000000000000, 0.000000000000000000, 0.000000000000000000 ) ) ;
#23800=DIRECTION ( 'NONE',  ( -1.000000000000000000, 0.000000000000000000, 0.000000000000000000 ) ) ;
#23803=VERTEX_POINT ( 'NONE', #37563 ) ;
#23804=AXIS2_PLACEMENT_3D ( 'NONE', #7933, #30703, #4522 ) ;
#23810=DIRECTION ( 'NONE',  ( 0.000000000000000000, -0.3090169943749548342, 0.9510565162951510887 ) ) ;
#23812=LINE ( 'NONE', #323, #749 ) ;
#23816=EDGE_LOOP ( 'NONE', ( #3857, #13909, #45607, #21296 ) ) ;
#23819=ORIENTED_EDGE ( 'NONE', *, *, #16872, .T. ) ;
#23821=DIRECTION ( 'NONE',  ( -1.000000000000000000, 0.000000000000000000, 0.000000000000000000 ) ) ;
#23825=CYLINDRICAL_SURFACE ( 'NONE', #18801, 77.49899999999999523 ) ;
#23826=CARTESIAN_POINT ( 'NONE',  ( 15.00000000000000000, -18.13022148937242761, 15.02647892043569122 ) ) ;
#23830=CIRCLE ( 'NONE', #19140, 82.00000000000000000 ) ;
#23834=CARTESIAN_POINT ( 'NONE',  ( 11.99999999999999822, -81.50828551894220197, -8.966570791701590437 ) ) ;
#23848=CARTESIAN_POINT ( 'NONE',  ( 0.000000000000000000, 20.41045688087824317, 72.35160999960824313 ) ) ;
#23850=CIRCLE ( 'NONE', #40283, 31.99999999999998934 ) ;
#23853=ORIENTED_EDGE ( 'NONE', *, *, #35759, .F. ) ;
#23856=AXIS2_PLACEMENT_3D ( 'NONE', #19695, #4791, #23624 ) ;
#23857=ADVANCED_FACE ( 'NONE', ( #21814 ), #17665, .T. ) ;
#23861=DIRECTION ( 'NONE',  ( -1.000000000000000000, -0.000000000000000000, -0.000000000000000000 ) ) ;
#23862=EDGE_CURVE ( 'NONE', #20052, #24067, #26229, .T. ) ;
#23874=EDGE_LOOP ( 'NONE', ( #3185, #2264, #33017, #1308 ) ) ;
#23875=DIRECTION ( 'NONE',  ( 1.000000000000000000, 0.000000000000000000, 0.000000000000000000 ) ) ;
#23882=CARTESIAN_POINT ( 'NONE',  ( 0.000000000000000000, 0.000000000000000000, 0.000000000000000000 ) ) ;
#23888=LINE ( 'NONE', #24130, #26942 ) ;
#23889=DIRECTION ( 'NONE',  ( -1.000000000000000000, 0.000000000000000000, 0.000000000000000000 ) ) ;
#23891=CIRCLE ( 'NONE', #2774, 82.00000000000000000 ) ;
#23894=CARTESIAN_POINT ( 'NONE',  ( 11.99999999999999822, -41.76106447765533147, 62.50884508063410294 ) ) ;
#23896=FACE_OUTER_BOUND ( 'NONE', #26204, .T. ) ;
#23897=CARTESIAN_POINT ( 'NONE',  ( 5.999999999999999112, 51.29473840253317007, -63.97538442413369353 ) ) ;
#23905=CARTESIAN_POINT ( 'NONE',  ( 11.99999999999999822, -70.53064760720297954, -26.01480285779911839 ) ) ;
#23906=LINE ( 'NONE', #2572, #12052 ) ;
#23912=DIRECTION ( 'NONE',  ( -1.000000000000000000, 0.000000000000000000, 0.000000000000000000 ) ) ;
#23919=EDGE_LOOP ( 'NONE', ( #3691, #46187, #21385, #38565 ) ) ;
#23921=DIRECTION ( 'NONE',  ( -1.000000000000000000, 0.000000000000000000, 0.000000000000000000 ) ) ;
#23922=DIRECTION ( 'NONE',  ( -1.000000000000000000, -0.000000000000000000, 0.000000000000000000 ) ) ;
#23927=VERTEX_POINT ( 'NONE', #32132 ) ;
#23935=ORIENTED_EDGE ( 'NONE', *, *, #13150, .T. ) ;
#23937=FACE_OUTER_BOUND ( 'NONE', #198, .T. ) ;
#23939=VERTEX_POINT ( 'NONE', #28446 ) ;
#23940=ORIENTED_EDGE ( 'NONE', *, *, #8820, .F. ) ;
#23942=DIRECTION ( 'NONE',  ( -1.000000000000000000, 0.000000000000000000, 0.000000000000000000 ) ) ;
#23950=ORIENTED_EDGE ( 'NONE', *, *, #21722, .F. ) ;
#23954=LINE ( 'NONE', #38889, #18833 ) ;
#23957=LINE ( 'NONE', #31549, #11117 ) ;
#23958=ORIENTED_EDGE ( 'NONE', *, *, #15324, .F. ) ;
#23962=VERTEX_POINT ( 'NONE', #17879 ) ;
#23963=LINE ( 'NONE', #16604, #31519 ) ;
#23965=CARTESIAN_POINT ( 'NONE',  ( 11.99999999999999822, 60.67117009219136037, 55.16347631943064300 ) ) ;
#23973=ORIENTED_EDGE ( 'NONE', *, *, #3408, .T. ) ;
#23975=AXIS2_PLACEMENT_3D ( 'NONE', #38398, #48089, #18472 ) ;
#23978=ORIENTED_EDGE ( 'NONE', *, *, #45829, .T. ) ;
#23983=AXIS2_PLACEMENT_3D ( 'NONE', #26127, #4351, #44974 ) ;
#23986=EDGE_CURVE ( 'NONE', #35412, #37888, #37158, .T. ) ;
#23993=ORIENTED_EDGE ( 'NONE', *, *, #46065, .T. ) ;
#23994=CARTESIAN_POINT ( 'NONE',  ( 0.000000000000000000, -81.90746397400391743, 3.894527615417586741 ) ) ;
#23996=ORIENTED_EDGE ( 'NONE', *, *, #7478, .F. ) ;
#23998=AXIS2_PLACEMENT_3D ( 'NONE', #11502, #40152, #6611 ) ;
#23999=CARTESIAN_POINT ( 'NONE',  ( 11.99999999999999822, 51.03279382321088065, 55.19960302592086521 ) ) ;
#24001=ORIENTED_EDGE ( 'NONE', *, *, #34034, .T. ) ;
#24002=CARTESIAN_POINT ( 'NONE',  ( 15.00000000000000000, -22.67460108101782978, -6.353146135317906840 ) ) ;
#24006=ORIENTED_EDGE ( 'NONE', *, *, #38081, .T. ) ;
#24007=AXIS2_PLACEMENT_3D ( 'NONE', #4030, #33874, #4515 ) ;
#24010=ORIENTED_EDGE ( 'NONE', *, *, #17382, .F. ) ;
#24012=DIRECTION ( 'NONE',  ( -1.000000000000000000, 0.000000000000000000, -0.000000000000000000 ) ) ;
#24020=CARTESIAN_POINT ( 'NONE',  ( 0.000000000000000000, 0.000000000000000000, 0.000000000000000000 ) ) ;
#24024=CARTESIAN_POINT ( 'NONE',  ( 0.000000000000000000, 16.65972982744933972, 80.28980883073764119 ) ) ;
#24028=DIRECTION ( 'NONE',  ( 0.000000000000000000, 0.000000000000000000, -1.000000000000000000 ) ) ;
#24030=EDGE_CURVE ( 'NONE', #22304, #10568, #13727, .T. ) ;
#24034=EDGE_LOOP ( 'NONE', ( #43199, #18491, #39646, #12295 ) ) ;
#24037=DIRECTION ( 'NONE',  ( -1.000000000000000000, 0.000000000000000000, -0.000000000000000000 ) ) ;
#24039=DIRECTION ( 'NONE',  ( 0.000000000000000000, -0.6494480483301903195, 0.7604059656000251577 ) ) ;
#24041=CIRCLE ( 'NONE', #7608, 31.99999999999998579 ) ;
#24042=EDGE_CURVE ( 'NONE', #32098, #6289, #23891, .T. ) ;
#24044=VERTEX_POINT ( 'NONE', #3260 ) ;
#24048=EDGE_CURVE ( 'NONE', #6120, #23445, #14542, .T. ) ;
#24056=EDGE_LOOP ( 'NONE', ( #6997, #38606, #33960, #48256 ) ) ;
#24057=ADVANCED_FACE ( 'NONE', ( #3022 ), #3510, .T. ) ;
#24059=CARTESIAN_POINT ( 'NONE',  ( 11.99999999999999822, -8.840884882375609877, 74.65374052328647281 ) ) ;
#24062=CARTESIAN_POINT ( 'NONE',  ( 11.99999999999999822, 0.000000000000000000, 0.000000000000000000 ) ) ;
#24063=CIRCLE ( 'NONE', #42029, 82.00000000000000000 ) ;
#24064=DIRECTION ( 'NONE',  ( -1.000000000000000000, 0.000000000000000000, 0.000000000000000000 ) ) ;
#24065=ORIENTED_EDGE ( 'NONE', *, *, #19002, .F. ) ;
#24067=VERTEX_POINT ( 'NONE', #6464 ) ;
#24072=CARTESIAN_POINT ( 'NONE',  ( 11.99999999999999822, 0.000000000000000000, 0.000000000000000000 ) ) ;
#24080=CARTESIAN_POINT ( 'NONE',  ( 11.99999999999999822, -73.73191006444582740, 14.66109333815435889 ) ) ;
#24081=DIRECTION ( 'NONE',  ( 1.000000000000000000, 0.000000000000000000, 0.000000000000000000 ) ) ;
#24085=ORIENTED_EDGE ( 'NONE', *, *, #11552, .T. ) ;
#24086=AXIS2_PLACEMENT_3D ( 'NONE', #32714, #11177, #41049 ) ;
#24093=CIRCLE ( 'NONE', #35789, 31.99999999999998934 ) ;
#24099=VERTEX_POINT ( 'NONE', #17718 ) ;
#24101=EDGE_CURVE ( 'NONE', #37099, #9873, #32423, .T. ) ;
#24105=DIRECTION ( 'NONE',  ( -1.000000000000000000, 0.000000000000000000, 0.000000000000000000 ) ) ;
#24108=CARTESIAN_POINT ( 'NONE',  ( 0.000000000000000000, 0.000000000000000000, 0.000000000000000000 ) ) ;
#24115=VECTOR ( 'NONE', #42383, 999.9999999999998863 ) ;
#24117=ORIENTED_EDGE ( 'NONE', *, *, #8373, .T. ) ;
#24119=ORIENTED_EDGE ( 'NONE', *, *, #35922, .T. ) ;
#24123=DIRECTION ( 'NONE',  ( 0.000000000000000000, 0.000000000000000000, 1.000000000000000000 ) ) ;
#24125=DIRECTION ( 'NONE',  ( 0.000000000000000000, -0.9945218953682742891, -0.1045284632676436315 ) ) ;
#24129=CARTESIAN_POINT ( 'NONE',  ( 11.99999999999999822, -81.96053171279901051, -2.543863470249249747 ) ) ;
#24130=CARTESIAN_POINT ( 'NONE',  ( 11.99999999999999822, 49.70050353004889132, 59.46389618801982380 ) ) ;
#24133=VERTEX_POINT ( 'NONE', #1476 ) ;
#24134=AXIS2_PLACEMENT_3D ( 'NONE', #28123, #12970, #9758 ) ;
#24144=DIRECTION ( 'NONE',  ( -1.000000000000000000, -0.000000000000000000, -0.000000000000000000 ) ) ;
#24148=EDGE_CURVE ( 'NONE', #35892, #10741, #27183, .T. ) ;
#24157=ORIENTED_EDGE ( 'NONE', *, *, #4960, .F. ) ;
#24159=CYLINDRICAL_SURFACE ( 'NONE', #26542, 31.99999999999998579 ) ;
#24160=CARTESIAN_POINT ( 'NONE',  ( 12.00000000000000000, -13.04903810567646971, 19.60159698893442481 ) ) ;
#24168=CYLINDRICAL_SURFACE ( 'NONE', #29778, 31.99999999999998579 ) ;
#24170=DIRECTION ( 'NONE',  ( 0.000000000000000000, -0.1045284632676437703, 0.9945218953682742891 ) ) ;
#24172=CARTESIAN_POINT ( 'NONE',  ( 0.000000000000000000, -20.40083707022935400, 72.35432306680478121 ) ) ;
#24177=EDGE_LOOP ( 'NONE', ( #29229, #38773, #20606, #47451 ) ) ;
#24180=DIRECTION ( 'NONE',  ( -1.000000000000000000, 0.000000000000000000, -0.000000000000000000 ) ) ;
#24183=DIRECTION ( 'NONE',  ( -1.000000000000000000, -0.000000000000000000, 0.000000000000000000 ) ) ;
#24186=DIRECTION ( 'NONE',  ( -1.000000000000000000, 0.000000000000000000, -0.000000000000000000 ) ) ;
#24188=DIRECTION ( 'NONE',  ( -1.000000000000000000, 0.000000000000000000, 0.000000000000000000 ) ) ;
#24189=CARTESIAN_POINT ( 'NONE',  ( 11.99999999999999822, -39.47590169984795239, -71.87247863392457248 ) ) ;
#24193=AXIS2_PLACEMENT_3D ( 'NONE', #10329, #44831, #43869 ) ;
#24194=VERTEX_POINT ( 'NONE', #34498 ) ;
#24196=CARTESIAN_POINT ( 'NONE',  ( 0.000000000000000000, -75.16055320797043748, 18.89407956138231270 ) ) ;
#24198=VECTOR ( 'NONE', #1156, 1000.000000000000000 ) ;
#24200=VERTEX_POINT ( 'NONE', #23994 ) ;
#24201=EDGE_CURVE ( 'NONE', #40188, #21764, #38693, .T. ) ;
#24202=CARTESIAN_POINT ( 'NONE',  ( 6.000000000000000000, -74.18225833017913828, 34.94270380257611208 ) ) ;
#24204=EDGE_LOOP ( 'NONE', ( #7007, #27932, #12222, #35403 ) ) ;
#24214=ORIENTED_EDGE ( 'NONE', *, *, #35759, .T. ) ;
#24218=AXIS2_PLACEMENT_3D ( 'NONE', #2929, #48206, #36696 ) ;
#24219=CARTESIAN_POINT ( 'NONE',  ( 11.99999999999999822, 75.11764819372149304, 29.05362095685338275 ) ) ;
#24220=CIRCLE ( 'NONE', #34370, 31.99999999999998579 ) ;
#24224=DIRECTION ( 'NONE',  ( 0.000000000000000000, -0.9969173337331271867, -0.07845909572785571273 ) ) ;
#24231=VERTEX_POINT ( 'NONE', #12260 ) ;
#24236=VECTOR ( 'NONE', #27738, 1000.000000000000000 ) ;
#24241=FACE_OUTER_BOUND ( 'NONE', #43549, .T. ) ;
#24245=CARTESIAN_POINT ( 'NONE',  ( 0.000000000000000000, 71.27951684758026829, 30.41916302227139113 ) ) ;
#24249=DIRECTION ( 'NONE',  ( -1.000000000000000000, -0.000000000000000000, 0.000000000000000000 ) ) ;
#24252=FACE_OUTER_BOUND ( 'NONE', #3003, .T. ) ;
#24260=VECTOR ( 'NONE', #32937, 1000.000000000000000 ) ;
#24264=ADVANCED_FACE ( 'NONE', ( #16886 ), #39406, .T. ) ;
#24267=AXIS2_PLACEMENT_3D ( 'NONE', #17881, #32809, #47734 ) ;
#24270=AXIS2_PLACEMENT_3D ( 'NONE', #35285, #39213, #13267 ) ;
#24273=EDGE_CURVE ( 'NONE', #17933, #33199, #21520, .T. ) ;
#24279=LINE ( 'NONE', #38982, #33646 ) ;
#24287=DIRECTION ( 'NONE',  ( 0.000000000000000000, 0.000000000000000000, 1.000000000000000000 ) ) ;
#24288=AXIS2_PLACEMENT_3D ( 'NONE', #16519, #2305, #43444 ) ;
#24289=EDGE_CURVE ( 'NONE', #28665, #3463, #24940, .T. ) ;
#24291=ORIENTED_EDGE ( 'NONE', *, *, #37409, .F. ) ;
#24296=CARTESIAN_POINT ( 'NONE',  ( 5.999999999999999112, 59.75363087400153006, -56.15606465354896670 ) ) ;
#24306=DIRECTION ( 'NONE',  ( -1.000000000000000000, -0.000000000000000000, 0.000000000000000000 ) ) ;
#24312=CARTESIAN_POINT ( 'NONE',  ( 15.00000000000000000, 14.60985201121729737, 18.46759930825687235 ) ) ;
#24313=LINE ( 'NONE', #20388, #35297 ) ;
#24314=LINE ( 'NONE', #8898, #16185 ) ;
#24318=EDGE_CURVE ( 'NONE', #9001, #19747, #45801, .T. ) ;
#24319=EDGE_CURVE ( 'NONE', #28070, #37785, #32521, .T. ) ;
#24320=VERTEX_POINT ( 'NONE', #43075 ) ;
#24331=ORIENTED_EDGE ( 'NONE', *, *, #35704, .T. ) ;
#24333=VECTOR ( 'NONE', #7806, 1000.000000000000000 ) ;
#24334=CARTESIAN_POINT ( 'NONE',  ( 11.99999999999999822, 72.35432306680455383, 20.40083707023012494 ) ) ;
#24341=ORIENTED_EDGE ( 'NONE', *, *, #22635, .F. ) ;
#24349=CARTESIAN_POINT ( 'NONE',  ( 11.99999999999999822, -72.35160999960831418, 20.41045688087797672 ) ) ;
#24352=CARTESIAN_POINT ( 'NONE',  ( 0.000000000000000000, 51.03279382321088065, 55.19960302592086521 ) ) ;
#24355=CARTESIAN_POINT ( 'NONE',  ( 0.000000000000000000, 75.54627589209970040, -17.28742895386005785 ) ) ;
#24360=PLANE ( 'NONE',  #2033 ) ;
#24363=FACE_OUTER_BOUND ( 'NONE', #7684, .T. ) ;
#24372=DIRECTION ( 'NONE',  ( -1.000000000000000000, 0.000000000000000000, 0.000000000000000000 ) ) ;
#24379=ADVANCED_FACE ( 'NONE', ( #14895 ), #3634, .T. ) ;
#24382=ORIENTED_EDGE ( 'NONE', *, *, #14984, .T. ) ;
#24384=CARTESIAN_POINT ( 'NONE',  ( 0.000000000000000000, -33.71516098798685590, -74.74816331893465815 ) ) ;
#24392=ORIENTED_EDGE ( 'NONE', *, *, #44532, .F. ) ;
#24394=ORIENTED_EDGE ( 'NONE', *, *, #38592, .T. ) ;
#24395=ORIENTED_EDGE ( 'NONE', *, *, #36190, .F. ) ;
#24403=ORIENTED_EDGE ( 'NONE', *, *, #46316, .F. ) ;
#24405=ORIENTED_EDGE ( 'NONE', *, *, #10526, .T. ) ;
#24406=CARTESIAN_POINT ( 'NONE',  ( 11.99999999999999822, -50.95692526931287603, -58.39081064771804819 ) ) ;
#24407=CARTESIAN_POINT ( 'NONE',  ( 0.000000000000000000, 63.18004540533092239, -44.88180994100307686 ) ) ;
#24408=CIRCLE ( 'NONE', #32250, 31.99999999999998579 ) ;
#24418=EDGE_LOOP ( 'NONE', ( #17925, #33434, #42406, #23733 ) ) ;
#24428=EDGE_CURVE ( 'NONE', #17321, #42306, #29579, .T. ) ;
#24434=ORIENTED_EDGE ( 'NONE', *, *, #41245, .F. ) ;
#24435=DIRECTION ( 'NONE',  ( 0.000000000000000000, -0.6691306063588661202, -0.7431448254773871387 ) ) ;
#24439=CIRCLE ( 'NONE', #22891, 77.49900000000000944 ) ;
#24447=CARTESIAN_POINT ( 'NONE',  ( 0.000000000000000000, -46.11716303203233736, 67.80270845531873647 ) ) ;
#24448=ORIENTED_EDGE ( 'NONE', *, *, #13926, .T. ) ;
#24457=DIRECTION ( 'NONE',  ( 0.000000000000000000, 0.000000000000000000, -1.000000000000000000 ) ) ;
#24460=VERTEX_POINT ( 'NONE', #41333 ) ;
#24462=VERTEX_POINT ( 'NONE', #22485 ) ;
#24464=AXIS2_PLACEMENT_3D ( 'NONE', #5289, #46649, #13112 ) ;
#24470=EDGE_CURVE ( 'NONE', #27706, #39316, #9105, .T. ) ;
#24473=DIRECTION ( 'NONE',  ( 0.000000000000000000, 0.8660254037844374864, -0.5000000000000019984 ) ) ;
#24474=VERTEX_POINT ( 'NONE', #22245 ) ;
#24476=DIRECTION ( 'NONE',  ( -1.000000000000000000, 0.000000000000000000, 0.000000000000000000 ) ) ;
#24482=FACE_OUTER_BOUND ( 'NONE', #33287, .T. ) ;
#24484=CIRCLE ( 'NONE', #44047, 77.49900000000000944 ) ;
#24490=ADVANCED_FACE ( 'NONE', ( #18565 ), #21982, .T. ) ;
#24494=CARTESIAN_POINT ( 'NONE',  ( 11.99999999999999822, 68.67312586195046720, -35.91791733033404199 ) ) ;
#24495=DIRECTION ( 'NONE',  ( 0.000000000000000000, 0.000000000000000000, 1.000000000000000000 ) ) ;
#24497=CIRCLE ( 'NONE', #29939, 77.49899999999999523 ) ;
#24499=DIRECTION ( 'NONE',  ( 0.000000000000000000, 0.000000000000000000, -1.000000000000000000 ) ) ;
#24506=CIRCLE ( 'NONE', #44027, 82.00000000000000000 ) ;
#24508=CARTESIAN_POINT ( 'NONE',  ( 11.99999999999999822, -72.35432306680469594, -20.40083707022958848 ) ) ;
#24514=AXIS2_PLACEMENT_3D ( 'NONE', #46284, #9312, #19835 ) ;
#24518=CYLINDRICAL_SURFACE ( 'NONE', #31588, 31.99999999999998579 ) ;
#24525=DIRECTION ( 'NONE',  ( 0.000000000000000000, 0.000000000000000000, -1.000000000000000000 ) ) ;
#24528=EDGE_CURVE ( 'NONE', #41278, #5585, #23145, .T. ) ;
#24533=AXIS2_PLACEMENT_3D ( 'NONE', #48393, #30046, #26132 ) ;
#24537=VERTEX_POINT ( 'NONE', #19504 ) ;
#24538=CARTESIAN_POINT ( 'NONE',  ( 15.00000000000000000, -22.67460108101774452, 6.353146135318220367 ) ) ;
#24540=VERTEX_POINT ( 'NONE', #45239 ) ;
#24542=AXIS2_PLACEMENT_3D ( 'NONE', #2747, #28710, #31677 ) ;
#24554=CARTESIAN_POINT ( 'NONE',  ( 11.99999999999999822, -73.73191006444582740, 14.66109333815435889 ) ) ;
#24557=AXIS2_PLACEMENT_3D ( 'NONE', #46439, #17277, #36380 ) ;
#24558=CIRCLE ( 'NONE', #44072, 77.49900000000000944 ) ;
#24560=ADVANCED_FACE ( 'NONE', ( #23937 ), #27363, .F. ) ;
#24563=DIRECTION ( 'NONE',  ( 0.000000000000000000, 0.6691306063588579045, -0.7431448254773945772 ) ) ;
#24564=AXIS2_PLACEMENT_3D ( 'NONE', #6852, #13470, #21767 ) ;
#24565=AXIS2_PLACEMENT_3D ( 'NONE', #38230, #7825, #30119 ) ;
#24568=CIRCLE ( 'NONE', #16742, 31.99999999999997868 ) ;
#24569=EDGE_CURVE ( 'NONE', #15076, #31175, #20010, .T. ) ;
#24572=ORIENTED_EDGE ( 'NONE', *, *, #4905, .T. ) ;
#24576=ORIENTED_EDGE ( 'NONE', *, *, #13086, .F. ) ;
#24581=ORIENTED_EDGE ( 'NONE', *, *, #34579, .F. ) ;
#24584=AXIS2_PLACEMENT_3D ( 'NONE', #37824, #26566, #4309 ) ;
#24590=CIRCLE ( 'NONE', #3484, 77.49899999999999523 ) ;
#24591=DIRECTION ( 'NONE',  ( -1.000000000000000000, 0.000000000000000000, -0.000000000000000000 ) ) ;
#24596=EDGE_LOOP ( 'NONE', ( #20180, #33901, #42097, #2357 ) ) ;
#24598=DIRECTION ( 'NONE',  ( -1.000000000000000000, 0.000000000000000000, -0.000000000000000000 ) ) ;
#24601=ORIENTED_EDGE ( 'NONE', *, *, #25823, .T. ) ;
#24605=EDGE_CURVE ( 'NONE', #14595, #43138, #48163, .T. ) ;
#24609=DIRECTION ( 'NONE',  ( 0.000000000000000000, 0.000000000000000000, -1.000000000000000000 ) ) ;
#24610=CARTESIAN_POINT ( 'NONE',  ( 11.99999999999999822, 0.000000000000000000, 0.000000000000000000 ) ) ;
#24616=ORIENTED_EDGE ( 'NONE', *, *, #13635, .F. ) ;
#24620=DIRECTION ( 'NONE',  ( 0.000000000000000000, -0.8526401643540860720, -0.5224985647159589019 ) ) ;
#24624=AXIS2_PLACEMENT_3D ( 'NONE', #1031, #30925, #22593 ) ;
#24627=DIRECTION ( 'NONE',  ( 0.000000000000000000, 0.000000000000000000, 1.000000000000000000 ) ) ;
#24631=ORIENTED_EDGE ( 'NONE', *, *, #29765, .F. ) ;
#24632=FACE_OUTER_BOUND ( 'NONE', #29829, .T. ) ;
#24639=VERTEX_POINT ( 'NONE', #27603 ) ;
#24648=EDGE_CURVE ( 'NONE', #4757, #45468, #15616, .T. ) ;
#24668=AXIS2_PLACEMENT_3D ( 'NONE', #15808, #42006, #38569 ) ;
#24669=CIRCLE ( 'NONE', #38756, 82.00000000000000000 ) ;
#24671=CARTESIAN_POINT ( 'NONE',  ( 0.000000000000000000, 0.000000000000000000, 0.000000000000000000 ) ) ;
#24672=ORIENTED_EDGE ( 'NONE', *, *, #36630, .T. ) ;
#24673=LINE ( 'NONE', #27619, #13957 ) ;
#24679=ORIENTED_EDGE ( 'NONE', *, *, #6359, .F. ) ;
#24684=ORIENTED_EDGE ( 'NONE', *, *, #25340, .F. ) ;
#24688=CARTESIAN_POINT ( 'NONE',  ( 0.000000000000000000, 0.000000000000000000, 0.000000000000000000 ) ) ;
#24689=ORIENTED_EDGE ( 'NONE', *, *, #43282, .T. ) ;
#24694=ADVANCED_FACE ( 'NONE', ( #25120 ), #9964, .T. ) ;
#24695=AXIS2_PLACEMENT_3D ( 'NONE', #17914, #46602, #9371 ) ;
#24696=DIRECTION ( 'NONE',  ( -1.000000000000000000, -0.000000000000000000, 0.000000000000000000 ) ) ;
#24698=ADVANCED_FACE ( 'NONE', ( #42784 ), #13884, .T. ) ;
#24699=AXIS2_PLACEMENT_3D ( 'NONE', #13055, #5699, #42911 ) ;
#24704=ORIENTED_EDGE ( 'NONE', *, *, #11552, .F. ) ;
#24711=AXIS2_PLACEMENT_3D ( 'NONE', #43046, #46957, #24435 ) ;
#24712=DIRECTION ( 'NONE',  ( 0.000000000000000000, 0.000000000000000000, 1.000000000000000000 ) ) ;
#24720=AXIS2_PLACEMENT_3D ( 'NONE', #42747, #39299, #39064 ) ;
#24721=VERTEX_POINT ( 'NONE', #2600 ) ;
#24724=DIRECTION ( 'NONE',  ( 0.000000000000000000, 0.000000000000000000, 1.000000000000000000 ) ) ;
#24726=AXIS2_PLACEMENT_3D ( 'NONE', #5570, #28807, #9238 ) ;
#24733=EDGE_CURVE ( 'NONE', #34678, #15200, #37218, .T. ) ;
#24734=CIRCLE ( 'NONE', #38010, 77.49899999999999523 ) ;
#24737=ORIENTED_EDGE ( 'NONE', *, *, #47467, .T. ) ;
#24740=VECTOR ( 'NONE', #48326, 1000.000000000000000 ) ;
#24747=VECTOR ( 'NONE', #42413, 1000.000000000000000 ) ;
#24748=DIRECTION ( 'NONE',  ( -1.000000000000000000, -0.000000000000000000, -0.000000000000000000 ) ) ;
#24749=DIRECTION ( 'NONE',  ( -0.000000000000000000, 0.9781476007338064660, 0.2079116908177554846 ) ) ;
#24755=CARTESIAN_POINT ( 'NONE',  ( 11.99999999999999822, 34.44570377933693806, -69.42325613327405165 ) ) ;
#24756=EDGE_CURVE ( 'NONE', #25415, #43483, #25473, .T. ) ;
#24757=CARTESIAN_POINT ( 'NONE',  ( 0.000000000000000000, 0.000000000000000000, 0.000000000000000000 ) ) ;
#24761=CARTESIAN_POINT ( 'NONE',  ( 0.000000000000000000, -76.66974797899828786, -11.30684508768420393 ) ) ;
#24762=VERTEX_POINT ( 'NONE', #35419 ) ;
#24764=AXIS2_PLACEMENT_3D ( 'NONE', #2681, #24962, #27948 ) ;
#24768=EDGE_CURVE ( 'NONE', #44062, #35871, #10654, .T. ) ;
#24772=ORIENTED_EDGE ( 'NONE', *, *, #36575, .T. ) ;
#24773=CARTESIAN_POINT ( 'NONE',  ( 0.000000000000000000, 65.59268652807210742, 36.72794159290264560 ) ) ;
#24779=ADVANCED_FACE ( 'NONE', ( #40069 ), #16580, .T. ) ;
#24781=FACE_OUTER_BOUND ( 'NONE', #32191, .T. ) ;
#24785=ORIENTED_EDGE ( 'NONE', *, *, #9750, .F. ) ;
#24786=ORIENTED_EDGE ( 'NONE', *, *, #37646, .T. ) ;
#24794=DIRECTION ( 'NONE',  ( 0.000000000000000000, -0.9945218953682730678, 0.1045284632676570929 ) ) ;
#24797=FACE_OUTER_BOUND ( 'NONE', #34150, .T. ) ;
#24801=DIRECTION ( 'NONE',  ( 0.000000000000000000, 0.000000000000000000, 1.000000000000000000 ) ) ;
#24802=LINE ( 'NONE', #39744, #21599 ) ;
#24808=AXIS2_PLACEMENT_3D ( 'NONE', #1393, #4352, #8483 ) ;
#24811=ADVANCED_FACE ( 'NONE', ( #20746 ), #46932, .T. ) ;
#24812=DIRECTION ( 'NONE',  ( 0.000000000000000000, 0.000000000000000000, 1.000000000000000000 ) ) ;
#24814=ORIENTED_EDGE ( 'NONE', *, *, #8913, .F. ) ;
#24816=ORIENTED_EDGE ( 'NONE', *, *, #15324, .T. ) ;
#24819=EDGE_CURVE ( 'NONE', #31175, #1469, #15086, .T. ) ;
#24823=EDGE_CURVE ( 'NONE', #23779, #34978, #43528, .T. ) ;
#24826=ORIENTED_EDGE ( 'NONE', *, *, #46431, .T. ) ;
#24828=FACE_OUTER_BOUND ( 'NONE', #47693, .T. ) ;
#24829=ORIENTED_EDGE ( 'NONE', *, *, #19761, .T. ) ;
#24831=CARTESIAN_POINT ( 'NONE',  ( 11.99999999999999822, 74.65491531819105830, 8.830959090343693418 ) ) ;
#24836=DIRECTION ( 'NONE',  ( 0.000000000000000000, 0.000000000000000000, 1.000000000000000000 ) ) ;
#24848=LINE ( 'NONE', #44176, #12969 ) ;
#24860=CIRCLE ( 'NONE', #28778, 31.99999999999998934 ) ;
#24861=EDGE_CURVE ( 'NONE', #18, #26898, #6780, .T. ) ;
#24863=AXIS2_PLACEMENT_3D ( 'NONE', #18969, #854, #22655 ) ;
#24867=EDGE_LOOP ( 'NONE', ( #37897, #34942, #20921, #20464 ) ) ;
#24869=EDGE_CURVE ( 'NONE', #27429, #9625, #29293, .T. ) ;
#24872=ORIENTED_EDGE ( 'NONE', *, *, #15191, .T. ) ;
#24875=EDGE_CURVE ( 'NONE', #4907, #13485, #26345, .T. ) ;
#24877=CARTESIAN_POINT ( 'NONE',  ( 5.999999999999999112, 33.71516098798741012, 74.74816331893441657 ) ) ;
#24881=FACE_OUTER_BOUND ( 'NONE', #23816, .T. ) ;
#24882=CARTESIAN_POINT ( 'NONE',  ( 5.999999999999999112, -71.21200624218768382, -40.65526001592688488 ) ) ;
#24886=ORIENTED_EDGE ( 'NONE', *, *, #21215, .T. ) ;
#24890=CYLINDRICAL_SURFACE ( 'NONE', #5442, 31.99999999999998579 ) ;
#24892=VECTOR ( 'NONE', #5340, 999.9999999999998863 ) ;
#24895=PLANE ( 'NONE',  #3422 ) ;
#24896=DIRECTION ( 'NONE',  ( 0.000000000000000000, 0.8090169943749498938, 0.5877852522924696954 ) ) ;
#24900=ADVANCED_FACE ( 'NONE', ( #11172 ), #3328, .T. ) ;
#24905=DIRECTION ( 'NONE',  ( -1.000000000000000000, 0.000000000000000000, 0.000000000000000000 ) ) ;
#24906=LINE ( 'NONE', #28336, #20044 ) ;
#24913=DIRECTION ( 'NONE',  ( -1.000000000000000000, -0.000000000000000000, 0.000000000000000000 ) ) ;
#24923=VERTEX_POINT ( 'NONE', #44945 ) ;
#24928=AXIS2_PLACEMENT_3D ( 'NONE', #36179, #3366, #6335 ) ;
#24939=ORIENTED_EDGE ( 'NONE', *, *, #22398, .T. ) ;
#24940=LINE ( 'NONE', #36443, #37966 ) ;
#24942=LINE ( 'NONE', #6355, #4089 ) ;
#24947=ORIENTED_EDGE ( 'NONE', *, *, #2230, .T. ) ;
#24948=DIRECTION ( 'NONE',  ( 0.000000000000000000, -0.2334453638558922628, -0.9723699203976798877 ) ) ;
#24958=DIRECTION ( 'NONE',  ( 0.000000000000000000, 0.000000000000000000, 1.000000000000000000 ) ) ;
#24961=CARTESIAN_POINT ( 'NONE',  ( 0.000000000000000000, 70.52718814184294160, -26.02418014898236720 ) ) ;
#24962=DIRECTION ( 'NONE',  ( -1.000000000000000000, -0.000000000000000000, -0.000000000000000000 ) ) ;
#24964=AXIS2_PLACEMENT_3D ( 'NONE', #28697, #20365, #20138 ) ;
#24965=CARTESIAN_POINT ( 'NONE',  ( 11.99999999999999822, -50.23322058963393744, 64.81221759200325039 ) ) ;
#24966=CARTESIAN_POINT ( 'NONE',  ( -10.00000000000000000, 0.000000000000000000, 0.000000000000000000 ) ) ;
#24974=ORIENTED_EDGE ( 'NONE', *, *, #37364, .T. ) ;
#24975=DIRECTION ( 'NONE',  ( 0.000000000000000000, 0.7431448254773862505, -0.6691306063588671194 ) ) ;
#24980=VERTEX_POINT ( 'NONE', #19692 ) ;
#24988=EDGE_LOOP ( 'NONE', ( #36233, #41142, #14675, #11644 ) ) ;
#24991=CARTESIAN_POINT ( 'NONE',  ( 0.000000000000000000, 59.75363087400076267, 56.15606465354979093 ) ) ;
#24998=DIRECTION ( 'NONE',  ( 0.000000000000000000, 0.8526401643540897357, 0.5224985647159527957 ) ) ;
#25000=CARTESIAN_POINT ( 'NONE',  ( 11.99999999999999822, -66.50666863322028632, 39.78640506895582973 ) ) ;
#25001=CARTESIAN_POINT ( 'NONE',  ( 11.99999999999999822, -49.70050353004932475, 59.46389618801947563 ) ) ;
#25005=ORIENTED_EDGE ( 'NONE', *, *, #21419, .T. ) ;
#25007=ORIENTED_EDGE ( 'NONE', *, *, #2072, .F. ) ;
#25009=CARTESIAN_POINT ( 'NONE',  ( 0.000000000000000000, -3.894527615417333610, -81.90746397400393164 ) ) ;
#25010=LINE ( 'NONE', #24296, #2778 ) ;
#25011=VERTEX_POINT ( 'NONE', #34384 ) ;
#25014=DIRECTION ( 'NONE',  ( -1.000000000000000000, -0.000000000000000000, 0.000000000000000000 ) ) ;
#25017=CARTESIAN_POINT ( 'NONE',  ( 0.000000000000000000, 10.30890764327382136, 81.34940948281339956 ) ) ;
#25029=CARTESIAN_POINT ( 'NONE',  ( 12.00000000000000000, 5.835314593368777558, 22.81335362449846471 ) ) ;
#25033=VERTEX_POINT ( 'NONE', #30268 ) ;
#25038=CIRCLE ( 'NONE', #2351, 82.00000000000000000 ) ;
#25041=DIRECTION ( 'NONE',  ( -1.000000000000000000, 0.000000000000000000, -0.000000000000000000 ) ) ;
#25043=EDGE_CURVE ( 'NONE', #34450, #28702, #30997, .T. ) ;
#25046=CIRCLE ( 'NONE', #13361, 82.00000000000000000 ) ;
#25048=CIRCLE ( 'NONE', #23479, 77.49899999999999523 ) ;
#25049=FACE_OUTER_BOUND ( 'NONE', #16697, .T. ) ;
#25052=AXIS2_PLACEMENT_3D ( 'NONE', #25705, #29142, #21076 ) ;
#25056=CIRCLE ( 'NONE', #28218, 31.99999999999999289 ) ;
#25058=FACE_OUTER_BOUND ( 'NONE', #21928, .T. ) ;
#25062=EDGE_CURVE ( 'NONE', #36250, #42347, #28673, .T. ) ;
#25064=STYLED_ITEM ( 'NONE', ( #201 ), #19105 ) ;
#25065=CARTESIAN_POINT ( 'NONE',  ( 0.000000000000000000, 0.8261519478441983200, -77.49459641780885022 ) ) ;
#25071=DIRECTION ( 'NONE',  ( -1.000000000000000000, 0.000000000000000000, 0.000000000000000000 ) ) ;
#25074=LINE ( 'NONE', #31967, #35467 ) ;
#25081=VERTEX_POINT ( 'NONE', #11652 ) ;
#25083=DIRECTION ( 'NONE',  ( 0.000000000000000000, 0.000000000000000000, -1.000000000000000000 ) ) ;
#25086=EDGE_CURVE ( 'NONE', #2861, #5309, #10681, .T. ) ;
#25088=CARTESIAN_POINT ( 'NONE',  ( 0.000000000000000000, 0.000000000000000000, 0.000000000000000000 ) ) ;
#25092=VECTOR ( 'NONE', #18255, 1000.000000000000000 ) ;
#25096=VECTOR ( 'NONE', #46021, 1000.000000000000000 ) ;
#25115=VECTOR ( 'NONE', #9202, 1000.000000000000000 ) ;
#25117=VECTOR ( 'NONE', #28034, 1000.000000000000000 ) ;
#25120=FACE_OUTER_BOUND ( 'NONE', #9403, .T. ) ;
#25127=CARTESIAN_POINT ( 'NONE',  ( 15.00000000000000000, -23.29833615347109088, -3.418703333116486665 ) ) ;
#25129=ADVANCED_FACE ( 'NONE', ( #17479 ), #9415, .T. ) ;
#25131=VECTOR ( 'NONE', #37608, 1000.000000000000000 ) ;
#25136=EDGE_CURVE ( 'NONE', #42577, #3648, #27113, .T. ) ;
#25137=DIRECTION ( 'NONE',  ( 0.000000000000000000, -0.5224985647159559043, 0.8526401643540879594 ) ) ;
#25145=LINE ( 'NONE', #40090, #27960 ) ;
#25146=VERTEX_POINT ( 'NONE', #20681 ) ;
#25148=CARTESIAN_POINT ( 'NONE',  ( 0.000000000000000000, -41.76937507738831812, 62.50329211542423025 ) ) ;
#25149=CARTESIAN_POINT ( 'NONE',  ( 11.99999999999999822, 71.91182617369190666, 28.89263327155770966 ) ) ;
#25152=ORIENTED_EDGE ( 'NONE', *, *, #38970, .T. ) ;
#25153=ORIENTED_EDGE ( 'NONE', *, *, #21438, .T. ) ;
#25156=CIRCLE ( 'NONE', #44696, 77.49899999999999523 ) ;
#25157=DIRECTION ( 'NONE',  ( 0.000000000000000000, -0.5877852522924624790, -0.8090169943749551118 ) ) ;
#25160=AXIS2_PLACEMENT_3D ( 'NONE', #31487, #35376, #17493 ) ;
#25161=EDGE_CURVE ( 'NONE', #21975, #24320, #7598, .T. ) ;
#25162=FACE_OUTER_BOUND ( 'NONE', #24056, .T. ) ;
#25163=ORIENTED_EDGE ( 'NONE', *, *, #27600, .F. ) ;
#25168=DIRECTION ( 'NONE',  ( -1.000000000000000000, 0.000000000000000000, 0.000000000000000000 ) ) ;
#25173=CARTESIAN_POINT ( 'NONE',  ( 11.99999999999999822, 0.000000000000000000, 0.000000000000000000 ) ) ;
#25174=DIRECTION ( 'NONE',  ( 1.000000000000000000, -0.000000000000000000, -0.000000000000000000 ) ) ;
#25181=ORIENTED_EDGE ( 'NONE', *, *, #3861, .F. ) ;
#25183=EDGE_CURVE ( 'NONE', #30137, #12997, #31961, .T. ) ;
#25184=CARTESIAN_POINT ( 'NONE',  ( -10.00000000000000000, 0.000000000000000000, 0.000000000000000000 ) ) ;
#25186=ORIENTED_EDGE ( 'NONE', *, *, #32174, .T. ) ;
#25190=DIRECTION ( 'NONE',  ( 0.000000000000000000, 0.1564344650402311743, -0.9876883405951376593 ) ) ;
#25191=CARTESIAN_POINT ( 'NONE',  ( 0.000000000000000000, -40.65526001592663619, 71.21200624218782593 ) ) ;
#25194=DIRECTION ( 'NONE',  ( 0.000000000000000000, 0.000000000000000000, 1.000000000000000000 ) ) ;
#25197=AXIS2_PLACEMENT_3D ( 'NONE', #32919, #17756, #36832 ) ;
#25204=CARTESIAN_POINT ( 'NONE',  ( 11.99999999999999822, -41.76106447765443619, -62.50884508063471401 ) ) ;
#25210=VECTOR ( 'NONE', #1666, 1000.000000000000000 ) ;
#25215=VECTOR ( 'NONE', #26604, 1000.000000000000000 ) ;
#25216=EDGE_CURVE ( 'NONE', #28563, #9076, #44318, .T. ) ;
#25218=CYLINDRICAL_SURFACE ( 'NONE', #24267, 31.99999999999998579 ) ;
#25220=CARTESIAN_POINT ( 'NONE',  ( 11.99999999999999822, 17.28742895386189460, -75.54627589209927407 ) ) ;
#25223=CARTESIAN_POINT ( 'NONE',  ( 15.00000000000000000, -13.04903810567646971, 19.60159698893442481 ) ) ;
#25225=ORIENTED_EDGE ( 'NONE', *, *, #13544, .F. ) ;
#25228=EDGE_CURVE ( 'NONE', #20542, #17607, #82, .T. ) ;
#25232=FACE_OUTER_BOUND ( 'NONE', #43491, .T. ) ;
#25238=ORIENTED_EDGE ( 'NONE', *, *, #31456, .F. ) ;
#25242=DIRECTION ( 'NONE',  ( 0.000000000000000000, 0.000000000000000000, -1.000000000000000000 ) ) ;
#25244=CARTESIAN_POINT ( 'NONE',  ( 11.99999999999999822, -81.34940948281328588, -10.30890764327469356 ) ) ;
#25252=ORIENTED_EDGE ( 'NONE', *, *, #35231, .T. ) ;
#25253=CARTESIAN_POINT ( 'NONE',  ( 11.99999999999999822, 50.23322058963348979, 64.81221759200361987 ) ) ;
#25255=DIRECTION ( 'NONE',  ( -1.000000000000000000, 0.000000000000000000, -0.000000000000000000 ) ) ;
#25260=CARTESIAN_POINT ( 'NONE',  ( 0.000000000000000000, 0.000000000000000000, 0.000000000000000000 ) ) ;
#25269=AXIS2_PLACEMENT_3D ( 'NONE', #532, #45081, #755 ) ;
#25270=DIRECTION ( 'NONE',  ( 0.000000000000000000, 0.000000000000000000, 1.000000000000000000 ) ) ;
#25271=AXIS2_PLACEMENT_3D ( 'NONE', #39206, #43366, #46305 ) ;
#25272=CARTESIAN_POINT ( 'NONE',  ( 11.99999999999999822, -8.830959090342926032, 74.65491531819115778 ) ) ;
#25275=EDGE_CURVE ( 'NONE', #2410, #46211, #10142, .T. ) ;
#25277=DIRECTION ( 'NONE',  ( 0.000000000000000000, 0.3826834323650904479, -0.9238795325112865164 ) ) ;
#25279=EDGE_CURVE ( 'NONE', #22205, #37953, #36525, .T. ) ;
#25283=ORIENTED_EDGE ( 'NONE', *, *, #33825, .F. ) ;
#25286=CIRCLE ( 'NONE', #29988, 31.99999999999998579 ) ;
#25287=DIRECTION ( 'NONE',  ( -1.000000000000000000, 0.000000000000000000, 0.000000000000000000 ) ) ;
#25290=DIRECTION ( 'NONE',  ( 0.000000000000000000, 0.000000000000000000, 1.000000000000000000 ) ) ;
#25291=EDGE_CURVE ( 'NONE', #1684, #5172, #29469, .T. ) ;
#25292=ORIENTED_EDGE ( 'NONE', *, *, #4041, .F. ) ;
#25294=EDGE_CURVE ( 'NONE', #18715, #40885, #13087, .T. ) ;
#25304=CIRCLE ( 'NONE', #24564, 31.99999999999998579 ) ;
#25305=DIRECTION ( 'NONE',  ( 0.000000000000000000, 0.9510565162951544194, -0.3090169943749446757 ) ) ;
#25307=DIRECTION ( 'NONE',  ( 0.000000000000000000, 0.000000000000000000, 1.000000000000000000 ) ) ;
#25312=AXIS2_PLACEMENT_3D ( 'NONE', #29932, #23077, #45337 ) ;
#25313=DIRECTION ( 'NONE',  ( -1.000000000000000000, 0.000000000000000000, 0.000000000000000000 ) ) ;
#25317=ORIENTED_EDGE ( 'NONE', *, *, #9765, .F. ) ;
#25321=CARTESIAN_POINT ( 'NONE',  ( 11.99999999999999822, 75.11725578898467859, 2.956366410620910656 ) ) ;
#25323=CIRCLE ( 'NONE', #15183, 31.99999999999998579 ) ;
#25324=CARTESIAN_POINT ( 'NONE',  ( 11.99999999999999822, -74.65491531819111515, -8.830959090343204920 ) ) ;
#25327=AXIS2_PLACEMENT_3D ( 'NONE', #11000, #48200, #2502 ) ;
#25329=AXIS2_PLACEMENT_3D ( 'NONE', #43477, #8969, #38847 ) ;
#25331=VERTEX_POINT ( 'NONE', #22119 ) ;
#25332=ORIENTED_EDGE ( 'NONE', *, *, #8820, .T. ) ;
#25340=EDGE_CURVE ( 'NONE', #4586, #39044, #22375, .T. ) ;
#25343=EDGE_CURVE ( 'NONE', #42347, #15440, #12302, .T. ) ;
#25353=ORIENTED_EDGE ( 'NONE', *, *, #16352, .T. ) ;
#25356=CARTESIAN_POINT ( 'NONE',  ( 11.99999999999999822, 0.000000000000000000, 0.000000000000000000 ) ) ;
#25360=LINE ( 'NONE', #40319, #41534 ) ;
#25362=VERTEX_POINT ( 'NONE', #25065 ) ;
#25363=ORIENTED_EDGE ( 'NONE', *, *, #6543, .T. ) ;
#25366=VECTOR ( 'NONE', #10910, 1000.000000000000000 ) ;
#25375=EDGE_CURVE ( 'NONE', #31941, #48222, #40013, .T. ) ;
#25377=VECTOR ( 'NONE', #1352, 1000.000000000000000 ) ;
#25383=VECTOR ( 'NONE', #2741, 1000.000000000000000 ) ;
#25386=DIRECTION ( 'NONE',  ( -1.000000000000000000, -0.000000000000000000, 0.000000000000000000 ) ) ;
#25389=CARTESIAN_POINT ( 'NONE',  ( 15.00000000000000000, 6.762365576493647445, 25.66652317338391498 ) ) ;
#25391=LINE ( 'NONE', #33701, #22212 ) ;
#25392=VERTEX_POINT ( 'NONE', #8627 ) ;
#25395=ORIENTED_EDGE ( 'NONE', *, *, #36151, .F. ) ;
#25397=ORIENTED_EDGE ( 'NONE', *, *, #38472, .F. ) ;
#25403=CIRCLE ( 'NONE', #1168, 82.00000000000000000 ) ;
#25407=ORIENTED_EDGE ( 'NONE', *, *, #29006, .F. ) ;
#25412=EDGE_CURVE ( 'NONE', #19576, #461, #26525, .T. ) ;
#25415=VERTEX_POINT ( 'NONE', #44882 ) ;
#25416=CARTESIAN_POINT ( 'NONE',  ( 11.99999999999999822, 0.000000000000000000, 0.000000000000000000 ) ) ;
#25420=DIRECTION ( 'NONE',  ( 0.000000000000000000, -0.3090169943749349613, -0.9510565162951576390 ) ) ;
#25425=ADVANCED_FACE ( 'NONE', ( #38263 ), #578, .F. ) ;
#25433=LINE ( 'NONE', #29364, #33953 ) ;
#25435=DIRECTION ( 'NONE',  ( 0.000000000000000000, 0.000000000000000000, 1.000000000000000000 ) ) ;
#25440=EDGE_LOOP ( 'NONE', ( #26006, #39086, #20617, #43766 ) ) ;
#25450=VERTEX_POINT ( 'NONE', #26288 ) ;
#25457=AXIS2_PLACEMENT_3D ( 'NONE', #40010, #17721, #32884 ) ;
#25458=VECTOR ( 'NONE', #22399, 1000.000000000000000 ) ;
#25466=CARTESIAN_POINT ( 'NONE',  ( 11.99999999999999822, 74.74816331893477184, -33.71516098798660011 ) ) ;
#25473=CIRCLE ( 'NONE', #42724, 31.99999999999998579 ) ;
#25474=CARTESIAN_POINT ( 'NONE',  ( 15.00000000000000000, 18.84667830672579569, -18.68964196561269375 ) ) ;
#25476=ORIENTED_EDGE ( 'NONE', *, *, #25043, .T. ) ;
#25482=ORIENTED_EDGE ( 'NONE', *, *, #23760, .F. ) ;
#25492=VERTEX_POINT ( 'NONE', #1044 ) ;
#25495=CARTESIAN_POINT ( 'NONE',  ( 11.99999999999999822, -20.40083707022935400, 72.35432306680478121 ) ) ;
#25496=EDGE_LOOP ( 'NONE', ( #45017, #9051, #30188, #32686 ) ) ;
#25498=CIRCLE ( 'NONE', #27054, 77.49900000000000944 ) ;
#25503=AXIS2_PLACEMENT_3D ( 'NONE', #34822, #15988, #1305 ) ;
#25505=LINE ( 'NONE', #40928, #39182 ) ;
#25508=LINE ( 'NONE', #3224, #463 ) ;
#25511=LINE ( 'NONE', #21110, #23171 ) ;
#25515=CARTESIAN_POINT ( 'NONE',  ( 12.00000000000000000, 23.49999999999999645, 1.499999999999995337 ) ) ;
#25516=ORIENTED_EDGE ( 'NONE', *, *, #31861, .F. ) ;
#25517=CYLINDRICAL_SURFACE ( 'NONE', #11315, 31.99999999999998579 ) ;
#25523=CARTESIAN_POINT ( 'NONE',  ( 0.000000000000000000, -71.21200624218825226, 40.65526001592589722 ) ) ;
#25528=EDGE_LOOP ( 'NONE', ( #12382, #16903, #33338, #9022 ) ) ;
#25529=EDGE_CURVE ( 'NONE', #8125, #7607, #21090, .T. ) ;
#25530=CIRCLE ( 'NONE', #12284, 82.00000000000000000 ) ;
#25534=CARTESIAN_POINT ( 'NONE',  ( 11.99999999999999822, -23.16143007188376757, -73.95703589263997912 ) ) ;
#25535=LINE ( 'NONE', #6944, #32454 ) ;
#25537=ORIENTED_EDGE ( 'NONE', *, *, #44470, .T. ) ;
#25540=VECTOR ( 'NONE', #19192, 1000.000000000000114 ) ;
#25545=AXIS2_PLACEMENT_3D ( 'NONE', #33670, #33442, #29762 ) ;
#25549=ORIENTED_EDGE ( 'NONE', *, *, #1337, .F. ) ;
#25552=DIRECTION ( 'NONE',  ( 0.000000000000000000, 0.000000000000000000, 1.000000000000000000 ) ) ;
#25556=CARTESIAN_POINT ( 'NONE',  ( 11.99999999999999822, -15.33399622253425321, -80.55351364060605590 ) ) ;
#25563=CARTESIAN_POINT ( 'NONE',  ( 0.000000000000000000, -14.66109333815513160, 73.73191006444567108 ) ) ;
#25568=AXIS2_PLACEMENT_3D ( 'NONE', #2115, #27335, #42031 ) ;
#25576=EDGE_CURVE ( 'NONE', #526, #29716, #24063, .T. ) ;
#25580=AXIS2_PLACEMENT_3D ( 'NONE', #47576, #36803, #14556 ) ;
#25581=ORIENTED_EDGE ( 'NONE', *, *, #20730, .T. ) ;
#25582=ADVANCED_FACE ( 'NONE', ( #39483 ), #13519, .F. ) ;
#25588=EDGE_LOOP ( 'NONE', ( #38604, #30803, #31835, #8497 ) ) ;
#25591=CARTESIAN_POINT ( 'NONE',  ( 11.99999999999999822, -65.64334221924937651, 41.19522573413711797 ) ) ;
#25592=DIRECTION ( 'NONE',  ( -1.000000000000000000, 0.000000000000000000, 0.000000000000000000 ) ) ;
#25594=ORIENTED_EDGE ( 'NONE', *, *, #16087, .F. ) ;
#25598=VERTEX_POINT ( 'NONE', #13284 ) ;
#25602=DIRECTION ( 'NONE',  ( 0.000000000000000000, 0.000000000000000000, 1.000000000000000000 ) ) ;
#25603=ORIENTED_EDGE ( 'NONE', *, *, #30051, .F. ) ;
#25604=EDGE_LOOP ( 'NONE', ( #26997, #29294, #35951, #17956 ) ) ;
#25607=LINE ( 'NONE', #37597, #33979 ) ;
#25610=ORIENTED_EDGE ( 'NONE', *, *, #30116, .F. ) ;
#25613=CARTESIAN_POINT ( 'NONE',  ( -10.00000000000000000, 0.000000000000000000, 0.000000000000000000 ) ) ;
#25616=LINE ( 'NONE', #37121, #21214 ) ;
#25619=ORIENTED_EDGE ( 'NONE', *, *, #11402, .F. ) ;
#25622=VECTOR ( 'NONE', #41420, 1000.000000000000000 ) ;
#25626=AXIS2_PLACEMENT_3D ( 'NONE', #43500, #44450, #40315 ) ;
#25635=ADVANCED_FACE ( 'NONE', ( #20616 ), #20140, .F. ) ;
#25636=EDGE_CURVE ( 'NONE', #9618, #26872, #12803, .T. ) ;
#25639=ORIENTED_EDGE ( 'NONE', *, *, #16357, .T. ) ;
#25640=DIRECTION ( 'NONE',  ( 0.000000000000000000, 0.000000000000000000, -1.000000000000000000 ) ) ;
#25642=ORIENTED_EDGE ( 'NONE', *, *, #26979, .T. ) ;
#25650=CARTESIAN_POINT ( 'NONE',  ( 11.99999999999999822, -74.65374052328644439, -8.840884882375878107 ) ) ;
#25653=CARTESIAN_POINT ( 'NONE',  ( 11.99999999999999822, 51.02545421589402252, -55.20638768913705263 ) ) ;
#25655=DIRECTION ( 'NONE',  ( 0.000000000000000000, 0.000000000000000000, 1.000000000000000000 ) ) ;
#25656=ORIENTED_EDGE ( 'NONE', *, *, #15695, .T. ) ;
#25659=DIRECTION ( 'NONE',  ( 0.000000000000000000, -0.4539904997395541875, 0.8910065241883641241 ) ) ;
#25665=DIRECTION ( 'NONE',  ( 0.000000000000000000, 0.9510565162951544194, -0.3090169943749446757 ) ) ;
#25673=CARTESIAN_POINT ( 'NONE',  ( 0.000000000000000000, -81.96053171279903893, 2.543863470248101333 ) ) ;
#25675=DIRECTION ( 'NONE',  ( 0.000000000000000000, 0.1564344650402312020, -0.9876883405951376593 ) ) ;
#25678=ORIENTED_EDGE ( 'NONE', *, *, #24048, .T. ) ;
#25680=DIRECTION ( 'NONE',  ( -1.000000000000000000, -0.000000000000000000, -0.000000000000000000 ) ) ;
#25681=CARTESIAN_POINT ( 'NONE',  ( 11.99999999999999822, -28.89263327155693517, -71.91182617369219088 ) ) ;
#25691=DIRECTION ( 'NONE',  ( 0.000000000000000000, 0.07845909572783797692, 0.9969173337331285190 ) ) ;
#25695=ORIENTED_EDGE ( 'NONE', *, *, #6695, .T. ) ;
#25700=VERTEX_POINT ( 'NONE', #43855 ) ;
#25701=EDGE_LOOP ( 'NONE', ( #44543, #24772, #2914, #12135 ) ) ;
#25704=VERTEX_POINT ( 'NONE', #21335 ) ;
#25705=CARTESIAN_POINT ( 'NONE',  ( 11.99999999999999822, 70.52718814184260054, 26.02418014898334420 ) ) ;
#25706=CIRCLE ( 'NONE', #14802, 31.99999999999998579 ) ;
#25709=VERTEX_POINT ( 'NONE', #11052 ) ;
#25712=CIRCLE ( 'NONE', #30323, 31.99999999999998579 ) ;
#25713=CARTESIAN_POINT ( 'NONE',  ( 15.00000000000000000, 24.81905959214260804, -9.408202855044828894 ) ) ;
#25714=ORIENTED_EDGE ( 'NONE', *, *, #17224, .F. ) ;
#25717=ORIENTED_EDGE ( 'NONE', *, *, #45460, .T. ) ;
#25718=LINE ( 'NONE', #21587, #43007 ) ;
#25721=ORIENTED_EDGE ( 'NONE', *, *, #26550, .F. ) ;
#25725=DIRECTION ( 'NONE',  ( 0.000000000000000000, 0.000000000000000000, 1.000000000000000000 ) ) ;
#25726=DIRECTION ( 'NONE',  ( -1.000000000000000000, 0.000000000000000000, 0.000000000000000000 ) ) ;
#25727=ORIENTED_EDGE ( 'NONE', *, *, #9455, .T. ) ;
#25729=CARTESIAN_POINT ( 'NONE',  ( 11.99999999999999822, -0.8261519478425843888, -77.49459641780887864 ) ) ;
#25731=CARTESIAN_POINT ( 'NONE',  ( 0.000000000000000000, 0.000000000000000000, 0.000000000000000000 ) ) ;
#25734=EDGE_CURVE ( 'NONE', #16268, #36912, #37238, .T. ) ;
#25737=FACE_OUTER_BOUND ( 'NONE', #42604, .T. ) ;
#25744=CARTESIAN_POINT ( 'NONE',  ( 11.99999999999999822, -69.42325613327466272, 34.44570377933573724 ) ) ;
#25745=CARTESIAN_POINT ( 'NONE',  ( 0.000000000000000000, -29.01471420065616513, 76.69515212746007649 ) ) ;
#25762=ADVANCED_FACE ( 'NONE', ( #17902 ), #32827, .T. ) ;
#25765=VERTEX_POINT ( 'NONE', #988 ) ;
#25770=DIRECTION ( 'NONE',  ( -1.000000000000000000, 0.000000000000000000, 0.000000000000000000 ) ) ;
#25781=DIRECTION ( 'NONE',  ( 0.000000000000000000, 0.000000000000000000, -1.000000000000000000 ) ) ;
#25788=CYLINDRICAL_SURFACE ( 'NONE', #21118, 31.99999999999998579 ) ;
#25789=DIRECTION ( 'NONE',  ( 0.000000000000000000, 0.000000000000000000, 1.000000000000000000 ) ) ;
#25791=CARTESIAN_POINT ( 'NONE',  ( 11.99999999999999822, 68.26794271651307611, -31.47745569255064169 ) ) ;
#25792=LINE ( 'NONE', #3042, #10359 ) ;
#25794=LINE ( 'NONE', #40737, #17254 ) ;
#25795=AXIS2_PLACEMENT_3D ( 'NONE', #8635, #19645, #38511 ) ;
#25796=CARTESIAN_POINT ( 'NONE',  ( 0.000000000000000000, 0.000000000000000000, 0.000000000000000000 ) ) ;
#25797=DIRECTION ( 'NONE',  ( 0.000000000000000000, 0.9723699203976756689, 0.2334453638559095823 ) ) ;
#25799=DIRECTION ( 'NONE',  ( 0.000000000000000000, 0.000000000000000000, 1.000000000000000000 ) ) ;
#25801=EDGE_CURVE ( 'NONE', #44508, #47223, #15456, .T. ) ;
#25809=CARTESIAN_POINT ( 'NONE',  ( 11.99999999999999822, 75.16055320797057959, -18.89407956138179046 ) ) ;
#25811=ORIENTED_EDGE ( 'NONE', *, *, #11770, .T. ) ;
#25814=AXIS2_PLACEMENT_3D ( 'NONE', #19500, #12432, #45722 ) ;
#25815=ORIENTED_EDGE ( 'NONE', *, *, #9664, .F. ) ;
#25820=EDGE_LOOP ( 'NONE', ( #22530, #21361, #914, #2533 ) ) ;
#25822=AXIS2_PLACEMENT_3D ( 'NONE', #20879, #25014, #48010 ) ;
#25823=EDGE_CURVE ( 'NONE', #44743, #33355, #4527, .T. ) ;
#25824=DIRECTION ( 'NONE',  ( 0.000000000000000000, 0.000000000000000000, 1.000000000000000000 ) ) ;
#25826=CARTESIAN_POINT ( 'NONE',  ( 5.999999999999999112, -27.74655509720617630, -77.16300072079690153 ) ) ;
#25828=ORIENTED_EDGE ( 'NONE', *, *, #29993, .F. ) ;
#25832=ORIENTED_EDGE ( 'NONE', *, *, #17370, .T. ) ;
#25835=DIRECTION ( 'NONE',  ( 0.000000000000000000, 0.000000000000000000, 1.000000000000000000 ) ) ;
#25842=DIRECTION ( 'NONE',  ( 0.000000000000000000, -0.3090169943749350168, -0.9510565162951576390 ) ) ;
#25854=VECTOR ( 'NONE', #37647, 999.9999999999998863 ) ;
#25856=ADVANCED_FACE ( 'NONE', ( #34276 ), #23032, .T. ) ;
#25857=ORIENTED_EDGE ( 'NONE', *, *, #20953, .T. ) ;
#25858=CIRCLE ( 'NONE', #1631, 77.49899999999999523 ) ;
#25863=DIRECTION ( 'NONE',  ( -1.000000000000000000, -0.000000000000000000, 0.000000000000000000 ) ) ;
#25867=AXIS2_PLACEMENT_3D ( 'NONE', #37489, #34773, #38715 ) ;
#25872=FACE_OUTER_BOUND ( 'NONE', #37485, .T. ) ;
#25877=ORIENTED_EDGE ( 'NONE', *, *, #35756, .F. ) ;
#25880=CARTESIAN_POINT ( 'NONE',  ( 0.000000000000000000, 34.94270380257741238, -74.18225833017852722 ) ) ;
#25881=CARTESIAN_POINT ( 'NONE',  ( 11.99999999999999822, 0.000000000000000000, 0.000000000000000000 ) ) ;
#25884=VECTOR ( 'NONE', #14012, 1000.000000000000000 ) ;
#25890=EDGE_CURVE ( 'NONE', #44445, #47105, #34985, .T. ) ;
#25891=ORIENTED_EDGE ( 'NONE', *, *, #2072, .T. ) ;
#25895=DIRECTION ( 'NONE',  ( 0.000000000000000000, -1.000000000000000000, -1.040834085586084730E-14 ) ) ;
#25899=VERTEX_POINT ( 'NONE', #30877 ) ;
#25902=CIRCLE ( 'NONE', #31450, 82.00000000000000000 ) ;
#25903=CYLINDRICAL_SURFACE ( 'NONE', #48104, 77.49899999999999523 ) ;
#25909=ORIENTED_EDGE ( 'NONE', *, *, #7636, .T. ) ;
#25910=DIRECTION ( 'NONE',  ( -1.000000000000000000, 0.000000000000000000, 0.000000000000000000 ) ) ;
#25912=ORIENTED_EDGE ( 'NONE', *, *, #36893, .F. ) ;
#25919=FACE_OUTER_BOUND ( 'NONE', #11418, .T. ) ;
#25920=CYLINDRICAL_SURFACE ( 'NONE', #41743, 31.99999999999998579 ) ;
#25922=CARTESIAN_POINT ( 'NONE',  ( 11.99999999999999822, -68.67312586195022561, 35.91791733033451806 ) ) ;
#25923=ADVANCED_FACE ( 'NONE', ( #12745 ), #35010, .T. ) ;
#25924=CARTESIAN_POINT ( 'NONE',  ( 11.99999999999999822, 34.44570377933693806, -69.42325613327405165 ) ) ;
#25925=AXIS2_PLACEMENT_3D ( 'NONE', #20321, #31613, #35507 ) ;
#25926=AXIS2_PLACEMENT_3D ( 'NONE', #34097, #15505, #19398 ) ;
#25928=DIRECTION ( 'NONE',  ( -1.000000000000000000, 0.000000000000000000, 0.000000000000000000 ) ) ;
#25929=ORIENTED_EDGE ( 'NONE', *, *, #20494, .F. ) ;
#25931=CARTESIAN_POINT ( 'NONE',  ( 11.99999999999999822, -73.95703589263958122, -23.16143007188505010 ) ) ;
#25935=VERTEX_POINT ( 'NONE', #29050 ) ;
#25937=DIRECTION ( 'NONE',  ( -1.000000000000000000, -0.000000000000000000, -0.000000000000000000 ) ) ;
#25939=LINE ( 'NONE', #13969, #11247 ) ;
#25940=ORIENTED_EDGE ( 'NONE', *, *, #22756, .T. ) ;
#25941=EDGE_CURVE ( 'NONE', #19231, #3822, #47521, .T. ) ;
#25942=LINE ( 'NONE', #11279, #4702 ) ;
#25944=DIRECTION ( 'NONE',  ( 0.000000000000000000, 0.000000000000000000, 1.000000000000000000 ) ) ;
#25945=EDGE_CURVE ( 'NONE', #24044, #17161, #42864, .T. ) ;
#25949=DIRECTION ( 'NONE',  ( -1.000000000000000000, 0.000000000000000000, 0.000000000000000000 ) ) ;
#25954=ORIENTED_EDGE ( 'NONE', *, *, #351, .F. ) ;
#25960=AXIS2_PLACEMENT_3D ( 'NONE', #33868, #19652, #34582 ) ;
#25964=CARTESIAN_POINT ( 'NONE',  ( 0.000000000000000000, 22.90783923731740401, -78.73519480814930205 ) ) ;
#25968=VERTEX_POINT ( 'NONE', #35497 ) ;
#25970=ORIENTED_EDGE ( 'NONE', *, *, #3491, .F. ) ;
#25974=PLANE ( 'NONE',  #33010 ) ;
#25980=LINE ( 'NONE', #41644, #21398 ) ;
#25982=DIRECTION ( 'NONE',  ( 0.000000000000000000, 0.000000000000000000, 1.000000000000000000 ) ) ;
#25986=ORIENTED_EDGE ( 'NONE', *, *, #6427, .T. ) ;
#25989=DIRECTION ( 'NONE',  ( 0.000000000000000000, -0.3826834323650969427, 0.9238795325112837409 ) ) ;
#25995=ORIENTED_EDGE ( 'NONE', *, *, #33257, .F. ) ;
#26004=CYLINDRICAL_SURFACE ( 'NONE', #6521, 82.00000000000000000 ) ;
#26005=AXIS2_PLACEMENT_3D ( 'NONE', #24554, #5968, #36695 ) ;
#26006=ORIENTED_EDGE ( 'NONE', *, *, #30462, .F. ) ;
#26010=FACE_OUTER_BOUND ( 'NONE', #24204, .T. ) ;
#26012=EDGE_LOOP ( 'NONE', ( #31796, #1695, #47190, #45245 ) ) ;
#26018=CYLINDRICAL_SURFACE ( 'NONE', #39480, 31.99999999999998579 ) ;
#26023=ORIENTED_EDGE ( 'NONE', *, *, #16983, .T. ) ;
#26027=CYLINDRICAL_SURFACE ( 'NONE', #36857, 31.99999999999998579 ) ;
#26029=FACE_OUTER_BOUND ( 'NONE', #9775, .T. ) ;
#26030=ORIENTED_EDGE ( 'NONE', *, *, #22985, .T. ) ;
#26037=CIRCLE ( 'NONE', #5743, 31.99999999999998934 ) ;
#26041=LINE ( 'NONE', #37306, #34444 ) ;
#26051=DIRECTION ( 'NONE',  ( 0.000000000000000000, 0.000000000000000000, -1.000000000000000000 ) ) ;
#26053=DIRECTION ( 'NONE',  ( -1.000000000000000000, -0.000000000000000000, 0.000000000000000000 ) ) ;
#26055=AXIS2_PLACEMENT_3D ( 'NONE', #21065, #9563, #42646 ) ;
#26063=DIRECTION ( 'NONE',  ( 0.000000000000000000, 0.000000000000000000, 1.000000000000000000 ) ) ;
#26064=DIRECTION ( 'NONE',  ( 0.000000000000000000, -0.3090169943749549453, 0.9510565162951511997 ) ) ;
#26066=VERTEX_POINT ( 'NONE', #5170 ) ;
#26072=EDGE_CURVE ( 'NONE', #10055, #16517, #28151, .T. ) ;
#26073=CARTESIAN_POINT ( 'NONE',  ( 0.000000000000000000, 67.80270845531956070, -46.11716303203111522 ) ) ;
#26074=VERTEX_POINT ( 'NONE', #18521 ) ;
#26079=EDGE_CURVE ( 'NONE', #44863, #13341, #11182, .T. ) ;
#26081=CARTESIAN_POINT ( 'NONE',  ( 0.000000000000000000, 64.81221759200342092, 50.23322058963371006 ) ) ;
#26084=ORIENTED_EDGE ( 'NONE', *, *, #4762, .T. ) ;
#26087=ORIENTED_EDGE ( 'NONE', *, *, #28474, .F. ) ;
#26091=DIRECTION ( 'NONE',  ( -1.000000000000000000, -0.000000000000000000, 0.000000000000000000 ) ) ;
#26095=ORIENTED_EDGE ( 'NONE', *, *, #40843, .F. ) ;
#26100=DIRECTION ( 'NONE',  ( 0.000000000000000000, 0.8660254037844432595, 0.4999999999999919509 ) ) ;
#26101=CARTESIAN_POINT ( 'NONE',  ( 11.99999999999999822, -77.16300072079641836, -27.74655509720752633 ) ) ;
#26104=CYLINDRICAL_SURFACE ( 'NONE', #45650, 82.00000000000000000 ) ;
#26107=CARTESIAN_POINT ( 'NONE',  ( 11.99999999999999822, 34.44570377933598593, 69.42325613327452061 ) ) ;
#26110=ADVANCED_FACE ( 'NONE', ( #7015 ), #10707, .F. ) ;
#26117=CIRCLE ( 'NONE', #44067, 31.99999999999998579 ) ;
#26122=DIRECTION ( 'NONE',  ( 0.000000000000000000, 0.9510565162951510887, -0.3090169943749551673 ) ) ;
#26125=AXIS2_PLACEMENT_3D ( 'NONE', #14391, #37384, #33466 ) ;
#26127=CARTESIAN_POINT ( 'NONE',  ( 11.99999999999999822, -26.02418014898260878, -70.52718814184285634 ) ) ;
#26129=ORIENTED_EDGE ( 'NONE', *, *, #35683, .T. ) ;
#26130=VECTOR ( 'NONE', #22003, 1000.000000000000000 ) ;
#26132=DIRECTION ( 'NONE',  ( 0.000000000000000000, 0.000000000000000000, 1.000000000000000000 ) ) ;
#26137=ORIENTED_EDGE ( 'NONE', *, *, #41921, .F. ) ;
#26139=EDGE_CURVE ( 'NONE', #15938, #20902, #24093, .T. ) ;
#26140=DIRECTION ( 'NONE',  ( 0.000000000000000000, 0.9969173337331281859, -0.07845909572784168229 ) ) ;
#26142=ORIENTED_EDGE ( 'NONE', *, *, #34619, .T. ) ;
#26156=DIRECTION ( 'NONE',  ( -1.000000000000000000, 0.000000000000000000, 0.000000000000000000 ) ) ;
#26160=AXIS2_PLACEMENT_3D ( 'NONE', #42939, #9883, #39025 ) ;
#26164=AXIS2_PLACEMENT_3D ( 'NONE', #7009, #30270, #45190 ) ;
#26167=EDGE_CURVE ( 'NONE', #18579, #36121, #41289, .T. ) ;
#26172=DIRECTION ( 'NONE',  ( 0.000000000000000000, 0.07845909572783797692, 0.9969173337331285190 ) ) ;
#26174=DIRECTION ( 'NONE',  ( -1.000000000000000000, 0.000000000000000000, -0.000000000000000000 ) ) ;
#26177=CARTESIAN_POINT ( 'NONE',  ( 11.99999999999999822, 0.000000000000000000, 0.000000000000000000 ) ) ;
#26178=DIRECTION ( 'NONE',  ( -1.000000000000000000, 0.000000000000000000, 0.000000000000000000 ) ) ;
#26180=DIRECTION ( 'NONE',  ( 0.000000000000000000, 0.000000000000000000, 1.000000000000000000 ) ) ;
#26191=CIRCLE ( 'NONE', #17583, 31.99999999999998934 ) ;
#26192=AXIS2_PLACEMENT_3D ( 'NONE', #18819, #221, #33754 ) ;
#26193=PRODUCT_DEFINITION_CONTEXT ( 'detailed design', #45743, 'design' ) ;
#26195=VECTOR ( 'NONE', #35377, 1000.000000000000000 ) ;
#26197=EDGE_CURVE ( 'NONE', #34678, #3459, #12361, .T. ) ;
#26198=CARTESIAN_POINT ( 'NONE',  ( 15.00000000000000000, 5.835314593368777558, 22.81335362449846471 ) ) ;
#26199=AXIS2_PLACEMENT_3D ( 'NONE', #2797, #10386, #25305 ) ;
#26201=ADVANCED_FACE ( 'NONE', ( #6789 ), #26104, .T. ) ;
#26204=EDGE_LOOP ( 'NONE', ( #22537, #41893, #45864, #30741 ) ) ;
#26205=FACE_OUTER_BOUND ( 'NONE', #37474, .T. ) ;
#26206=ORIENTED_EDGE ( 'NONE', *, *, #14729, .F. ) ;
#26212=LINE ( 'NONE', #11528, #44116 ) ;
#26214=DIRECTION ( 'NONE',  ( 0.000000000000000000, 0.000000000000000000, 1.000000000000000000 ) ) ;
#26216=EDGE_LOOP ( 'NONE', ( #29159, #5094, #19672, #36666 ) ) ;
#26217=LINE ( 'NONE', #19340, #4048 ) ;
#26222=ORIENTED_EDGE ( 'NONE', *, *, #6063, .F. ) ;
#26224=DIRECTION ( 'NONE',  ( 0.000000000000000000, 0.5877852522924797984, 0.8090169943749426773 ) ) ;
#26225=VERTEX_POINT ( 'NONE', #40796 ) ;
#26226=CYLINDRICAL_SURFACE ( 'NONE', #2330, 82.00000000000000000 ) ;
#26229=CIRCLE ( 'NONE', #31703, 77.49900000000002365 ) ;
#26235=CARTESIAN_POINT ( 'NONE',  ( 0.000000000000000000, 70.52718814184260054, 26.02418014898334420 ) ) ;
#26237=AXIS2_PLACEMENT_3D ( 'NONE', #33628, #3280, #18212 ) ;
#26240=CIRCLE ( 'NONE', #5138, 77.49899999999999523 ) ;
#26244=EDGE_CURVE ( 'NONE', #25968, #29983, #43970, .T. ) ;
#26249=DIRECTION ( 'NONE',  ( -1.000000000000000000, -0.000000000000000000, -0.000000000000000000 ) ) ;
#26253=DIRECTION ( 'NONE',  ( 0.000000000000000000, 0.000000000000000000, -1.000000000000000000 ) ) ;
#26254=DIRECTION ( 'NONE',  ( -1.000000000000000000, -0.000000000000000000, -0.000000000000000000 ) ) ;
#26262=LINE ( 'NONE', #775, #5863 ) ;
#26268=EDGE_CURVE ( 'NONE', #5700, #13430, #29235, .T. ) ;
#26269=EDGE_CURVE ( 'NONE', #36359, #33795, #44075, .T. ) ;
#26271=DIRECTION ( 'NONE',  ( -1.000000000000000000, 0.000000000000000000, -0.000000000000000000 ) ) ;
#26281=AXIS2_PLACEMENT_3D ( 'NONE', #2757, #6685, #10107 ) ;
#26283=DIRECTION ( 'NONE',  ( 0.000000000000000000, -0.5224985647159559043, 0.8526401643540879594 ) ) ;
#26284=DIRECTION ( 'NONE',  ( -1.000000000000000000, 0.000000000000000000, 0.000000000000000000 ) ) ;
#26286=CARTESIAN_POINT ( 'NONE',  ( 11.99999999999999822, -36.73666225445845157, -65.58780272294114866 ) ) ;
#26288=CARTESIAN_POINT ( 'NONE',  ( 11.99999999999999822, 71.21200624218852226, -40.65526001592539984 ) ) ;
#26289=ORIENTED_EDGE ( 'NONE', *, *, #32067, .T. ) ;
#26298=CYLINDRICAL_SURFACE ( 'NONE', #31331, 77.49899999999999523 ) ;
#26303=DIRECTION ( 'NONE',  ( -1.000000000000000000, 0.000000000000000000, -0.000000000000000000 ) ) ;
#26306=EDGE_CURVE ( 'NONE', #39373, #15331, #26786, .T. ) ;
#26309=LINE ( 'NONE', #47833, #45615 ) ;
#26311=LINE ( 'NONE', #41003, #19212 ) ;
#26318=CYLINDRICAL_SURFACE ( 'NONE', #25197, 31.99999999999998579 ) ;
#26342=VERTEX_POINT ( 'NONE', #19959 ) ;
#26344=VERTEX_POINT ( 'NONE', #1374 ) ;
#26345=LINE ( 'NONE', #44223, #2881 ) ;
#26351=CYLINDRICAL_SURFACE ( 'NONE', #31408, 77.49899999999999523 ) ;
#26354=CARTESIAN_POINT ( 'NONE',  ( 11.99999999999999822, -26.01480285779885904, 70.53064760720306481 ) ) ;
#26355=DIRECTION ( 'NONE',  ( 1.000000000000000000, -0.000000000000000000, -0.000000000000000000 ) ) ;
#26356=CARTESIAN_POINT ( 'NONE',  ( 0.000000000000000000, -74.65374052328644439, -8.840884882375878107 ) ) ;
#26357=ORIENTED_EDGE ( 'NONE', *, *, #22001, .F. ) ;
#26358=AXIS2_PLACEMENT_3D ( 'NONE', #46415, #46669, #27832 ) ;
#26359=LINE ( 'NONE', #43986, #22018 ) ;
#26360=ORIENTED_EDGE ( 'NONE', *, *, #27600, .T. ) ;
#26363=ORIENTED_EDGE ( 'NONE', *, *, #43823, .T. ) ;
#26374=ORIENTED_EDGE ( 'NONE', *, *, #3265, .T. ) ;
#26375=DIRECTION ( 'NONE',  ( -1.000000000000000000, 0.000000000000000000, 0.000000000000000000 ) ) ;
#26379=DIRECTION ( 'NONE',  ( 0.000000000000000000, 0.000000000000000000, 1.000000000000000000 ) ) ;
#26388=CARTESIAN_POINT ( 'NONE',  ( 0.000000000000000000, 0.000000000000000000, 0.000000000000000000 ) ) ;
#26390=VERTEX_POINT ( 'NONE', #6252 ) ;
#26394=DIRECTION ( 'NONE',  ( -1.000000000000000000, -0.000000000000000000, 0.000000000000000000 ) ) ;
#26397=CYLINDRICAL_SURFACE ( 'NONE', #17800, 31.99999999999998579 ) ;
#26406=LINE ( 'NONE', #4127, #43150 ) ;
#26408=CYLINDRICAL_SURFACE ( 'NONE', #976, 31.99999999999998579 ) ;
#26410=ORIENTED_EDGE ( 'NONE', *, *, #11999, .T. ) ;
#26411=ORIENTED_EDGE ( 'NONE', *, *, #12310, .F. ) ;
#26419=ORIENTED_EDGE ( 'NONE', *, *, #14591, .F. ) ;
#26420=DIRECTION ( 'NONE',  ( 0.000000000000000000, 0.8910065241883655673, 0.4539904997395510233 ) ) ;
#26424=EDGE_CURVE ( 'NONE', #17817, #15931, #1858, .T. ) ;
#26426=FACE_OUTER_BOUND ( 'NONE', #3592, .T. ) ;
#26430=CARTESIAN_POINT ( 'NONE',  ( 11.99999999999999822, 62.50884508063427347, 41.76106447765511831 ) ) ;
#26432=EDGE_CURVE ( 'NONE', #1046, #2861, #13843, .T. ) ;
#26436=ORIENTED_EDGE ( 'NONE', *, *, #4041, .T. ) ;
#26438=DIRECTION ( 'NONE',  ( -1.000000000000000000, -0.000000000000000000, 0.000000000000000000 ) ) ;
#26440=DIRECTION ( 'NONE',  ( -1.000000000000000000, -0.000000000000000000, 0.000000000000000000 ) ) ;
#26441=DIRECTION ( 'NONE',  ( 1.000000000000000000, 0.000000000000000000, 0.000000000000000000 ) ) ;
#26443=ORIENTED_EDGE ( 'NONE', *, *, #43315, .F. ) ;
#26445=DIRECTION ( 'NONE',  ( 1.000000000000000000, 0.000000000000000000, -0.000000000000000000 ) ) ;
#26456=ORIENTED_EDGE ( 'NONE', *, *, #7215, .T. ) ;
#26464=ORIENTED_EDGE ( 'NONE', *, *, #2390, .T. ) ;
#26466=CARTESIAN_POINT ( 'NONE',  ( 15.00000000000000000, 16.83928648764945635, 16.46020748918027010 ) ) ;
#26467=EDGE_LOOP ( 'NONE', ( #12693, #2904, #25721, #27182 ) ) ;
#26469=EDGE_LOOP ( 'NONE', ( #43757, #48042, #7977, #12649 ) ) ;
#26473=ORIENTED_EDGE ( 'NONE', *, *, #41491, .F. ) ;
#26474=CIRCLE ( 'NONE', #47556, 31.99999999999998579 ) ;
#26478=CIRCLE ( 'NONE', #5371, 77.49900000000000944 ) ;
#26483=EDGE_CURVE ( 'NONE', #23779, #36359, #17738, .T. ) ;
#26484=CARTESIAN_POINT ( 'NONE',  ( -10.00000000000000000, 0.000000000000000000, 0.000000000000000000 ) ) ;
#26487=DIRECTION ( 'NONE',  ( 0.000000000000000000, 0.000000000000000000, 1.000000000000000000 ) ) ;
#26488=DIRECTION ( 'NONE',  ( 1.000000000000000000, -0.000000000000000000, 0.000000000000000000 ) ) ;
#26493=CYLINDRICAL_SURFACE ( 'NONE', #4530, 31.99999999999998579 ) ;
#26498=DIRECTION ( 'NONE',  ( -1.000000000000000000, -0.000000000000000000, -0.000000000000000000 ) ) ;
#26499=ORIENTED_EDGE ( 'NONE', *, *, #40301, .T. ) ;
#26505=CARTESIAN_POINT ( 'NONE',  ( 11.99999999999999822, -59.03342792756231461, -46.54456581323868392 ) ) ;
#26506=VECTOR ( 'NONE', #40048, 1000.000000000000000 ) ;
#26514=CYLINDRICAL_SURFACE ( 'NONE', #36715, 77.49899999999999523 ) ;
#26520=CARTESIAN_POINT ( 'NONE',  ( 12.00000000000000000, 5.835314593368470248, -22.81335362449854642 ) ) ;
#26522=CARTESIAN_POINT ( 'NONE',  ( 11.99999999999999822, 2.956366410621684260, -75.11725578898465017 ) ) ;
#26524=ORIENTED_EDGE ( 'NONE', *, *, #32101, .T. ) ;
#26525=LINE ( 'NONE', #34326, #27957 ) ;
#26526=ORIENTED_EDGE ( 'NONE', *, *, #22026, .T. ) ;
#26535=FACE_OUTER_BOUND ( 'NONE', #41485, .T. ) ;
#26539=DIRECTION ( 'NONE',  ( 0.000000000000000000, -0.7071067811865389130, -0.7071067811865562325 ) ) ;
#26541=AXIS2_PLACEMENT_3D ( 'NONE', #5650, #9797, #35748 ) ;
#26542=AXIS2_PLACEMENT_3D ( 'NONE', #9701, #19737, #28307 ) ;
#26544=CARTESIAN_POINT ( 'NONE',  ( -10.00000000000000000, 0.000000000000000000, 0.000000000000000000 ) ) ;
#26549=DIRECTION ( 'NONE',  ( 0.000000000000000000, 0.000000000000000000, 1.000000000000000000 ) ) ;
#26550=EDGE_CURVE ( 'NONE', #12857, #43286, #25792, .T. ) ;
#26558=ORIENTED_EDGE ( 'NONE', *, *, #21006, .F. ) ;
#26563=CYLINDRICAL_SURFACE ( 'NONE', #22235, 77.49899999999999523 ) ;
#26566=DIRECTION ( 'NONE',  ( -1.000000000000000000, 0.000000000000000000, 0.000000000000000000 ) ) ;
#26574=AXIS2_PLACEMENT_3D ( 'NONE', #20987, #2374, #17301 ) ;
#26576=CARTESIAN_POINT ( 'NONE',  ( 0.000000000000000000, -65.64334221924882229, -41.19522573413803457 ) ) ;
#26578=ORIENTED_EDGE ( 'NONE', *, *, #21722, .T. ) ;
#26582=CARTESIAN_POINT ( 'NONE',  ( 11.99999999999999822, 73.95703589264006439, -23.16143007188350822 ) ) ;
#26583=ORIENTED_EDGE ( 'NONE', *, *, #23519, .F. ) ;
#26589=DIRECTION ( 'NONE',  ( 0.000000000000000000, 0.000000000000000000, 1.000000000000000000 ) ) ;
#26596=DIRECTION ( 'NONE',  ( -1.000000000000000000, 0.000000000000000000, 0.000000000000000000 ) ) ;
#26604=DIRECTION ( 'NONE',  ( -1.000000000000000000, -0.000000000000000000, -0.000000000000000000 ) ) ;
#26609=ORIENTED_EDGE ( 'NONE', *, *, #38639, .F. ) ;
#26610=CARTESIAN_POINT ( 'NONE',  ( -10.00000000000000000, 0.000000000000000000, 0.000000000000000000 ) ) ;
#26614=AXIS2_PLACEMENT_3D ( 'NONE', #242, #34026, #26214 ) ;
#26615=DIRECTION ( 'NONE',  ( 0.000000000000000000, -0.1564344650402381687, 0.9876883405951365491 ) ) ;
#26616=EDGE_LOOP ( 'NONE', ( #27365, #6228, #41400, #4835 ) ) ;
#26619=ORIENTED_EDGE ( 'NONE', *, *, #18822, .F. ) ;
#26621=DIRECTION ( 'NONE',  ( -1.000000000000000000, 0.000000000000000000, 0.000000000000000000 ) ) ;
#26626=ORIENTED_EDGE ( 'NONE', *, *, #24273, .T. ) ;
#26627=EDGE_CURVE ( 'NONE', #5583, #25081, #33060, .T. ) ;
#26628=EDGE_CURVE ( 'NONE', #40230, #28665, #3363, .T. ) ;
#26629=DIRECTION ( 'NONE',  ( -1.000000000000000000, -0.000000000000000000, 0.000000000000000000 ) ) ;
#26633=DIRECTION ( 'NONE',  ( -1.000000000000000000, -0.000000000000000000, -0.000000000000000000 ) ) ;
#26644=DIRECTION ( 'NONE',  ( 0.000000000000000000, 0.000000000000000000, 1.000000000000000000 ) ) ;
#26648=ADVANCED_FACE ( 'NONE', ( #45140 ), #38272, .F. ) ;
#26653=VECTOR ( 'NONE', #24183, 1000.000000000000000 ) ;
#26656=DIRECTION ( 'NONE',  ( 0.000000000000000000, -0.8526401643540970632, 0.5224985647159410274 ) ) ;
#26657=ORIENTED_EDGE ( 'NONE', *, *, #37189, .F. ) ;
#26664=DIRECTION ( 'NONE',  ( 0.000000000000000000, 0.3826834323650840086, 0.9238795325112891810 ) ) ;
#26668=DIRECTION ( 'NONE',  ( 0.000000000000000000, 0.9510565162951544194, -0.3090169943749446757 ) ) ;
#26673=ORIENTED_EDGE ( 'NONE', *, *, #14405, .T. ) ;
#26675=ADVANCED_FACE ( 'NONE', ( #22854 ), #11609, .T. ) ;
#26679=CIRCLE ( 'NONE', #39993, 31.99999999999998579 ) ;
#26681=DIRECTION ( 'NONE',  ( -1.000000000000000000, 0.000000000000000000, -0.000000000000000000 ) ) ;
#26682=VERTEX_POINT ( 'NONE', #38040 ) ;
#26684=ORIENTED_EDGE ( 'NONE', *, *, #21709, .F. ) ;
#26685=ADVANCED_FACE ( 'NONE', ( #26535 ), #4738, .T. ) ;
#26694=ORIENTED_EDGE ( 'NONE', *, *, #26079, .T. ) ;
#26697=ORIENTED_EDGE ( 'NONE', *, *, #27987, .T. ) ;
#26699=EDGE_LOOP ( 'NONE', ( #19401, #36969, #5646, #24679 ) ) ;
#26700=DIRECTION ( 'NONE',  ( 0.000000000000000000, 0.000000000000000000, 1.000000000000000000 ) ) ;
#26709=AXIS2_PLACEMENT_3D ( 'NONE', #33609, #30670, #8155 ) ;
#26721=CIRCLE ( 'NONE', #15782, 82.00000000000000000 ) ;
#26722=CARTESIAN_POINT ( 'NONE',  ( -10.00000000000000000, 0.000000000000000000, 0.000000000000000000 ) ) ;
#26727=CYLINDRICAL_SURFACE ( 'NONE', #32529, 82.00000000000000000 ) ;
#26733=VERTEX_POINT ( 'NONE', #12573 ) ;
#26734=ORIENTED_EDGE ( 'NONE', *, *, #37982, .F. ) ;
#26735=CARTESIAN_POINT ( 'NONE',  ( 12.00000000000000000, -10.45096189432314127, 21.10159698893440350 ) ) ;
#26736=EDGE_LOOP ( 'NONE', ( #4826, #27803, #43835, #48233 ) ) ;
#26737=CARTESIAN_POINT ( 'NONE',  ( 0.000000000000000000, 0.000000000000000000, 0.000000000000000000 ) ) ;
#26740=ORIENTED_EDGE ( 'NONE', *, *, #667, .F. ) ;
#26742=ADVANCED_FACE ( 'NONE', ( #27508 ), #8891, .T. ) ;
#26747=AXIS2_PLACEMENT_3D ( 'NONE', #30689, #15761, #26539 ) ;
#26750=CARTESIAN_POINT ( 'NONE',  ( 11.99999999999999822, 6.903761155838878061, -77.19088730480517313 ) ) ;
#26755=ORIENTED_EDGE ( 'NONE', *, *, #33571, .F. ) ;
#26758=DIRECTION ( 'NONE',  ( 0.000000000000000000, 0.1045284632676449221, -0.9945218953682741780 ) ) ;
#26763=EDGE_LOOP ( 'NONE', ( #2122, #24631, #46709, #9672 ) ) ;
#26766=DIRECTION ( 'NONE',  ( -1.000000000000000000, 0.000000000000000000, 0.000000000000000000 ) ) ;
#26769=DIRECTION ( 'NONE',  ( 0.000000000000000000, 0.6494480483301848794, -0.7604059656000299317 ) ) ;
#26772=CARTESIAN_POINT ( 'NONE',  ( 12.00000000000000000, 16.83928648764945635, 16.46020748918027010 ) ) ;
#26773=VECTOR ( 'NONE', #8647, 1000.000000000000000 ) ;
#26775=DIRECTION ( 'NONE',  ( 1.000000000000000000, 0.000000000000000000, 0.000000000000000000 ) ) ;
#26776=DIRECTION ( 'NONE',  ( 1.000000000000000000, -0.000000000000000000, 0.000000000000000000 ) ) ;
#26779=AXIS2_PLACEMENT_3D ( 'NONE', #13935, #28855, #48188 ) ;
#26780=CARTESIAN_POINT ( 'NONE',  ( 11.99999999999999822, -75.16055320797043748, 18.89407956138231270 ) ) ;
#26781=DIRECTION ( 'NONE',  ( 0.000000000000000000, 0.000000000000000000, 1.000000000000000000 ) ) ;
#26782=CARTESIAN_POINT ( 'NONE',  ( 11.99999999999999822, -74.65491531819111515, -8.830959090343204920 ) ) ;
#26785=DIRECTION ( 'NONE',  ( -1.000000000000000000, -0.000000000000000000, 0.000000000000000000 ) ) ;
#26786=CIRCLE ( 'NONE', #11169, 82.00000000000000000 ) ;
#26790=EDGE_CURVE ( 'NONE', #43952, #19231, #9140, .T. ) ;
#26792=LINE ( 'NONE', #4042, #32280 ) ;
#26794=ORIENTED_EDGE ( 'NONE', *, *, #2758, .T. ) ;
#26795=VERTEX_POINT ( 'NONE', #39239 ) ;
#26797=AXIS2_PLACEMENT_3D ( 'NONE', #7164, #22086, #37020 ) ;
#26801=ADVANCED_FACE ( 'NONE', ( #5707 ), #39494, .T. ) ;
#26804=DIRECTION ( 'NONE',  ( -1.000000000000000000, -0.000000000000000000, 0.000000000000000000 ) ) ;
#26806=AXIS2_PLACEMENT_3D ( 'NONE', #23882, #31240, #5520 ) ;
#26812=EDGE_LOOP ( 'NONE', ( #47679, #10262, #15146, #25594 ) ) ;
#26815=DIRECTION ( 'NONE',  ( -1.000000000000000000, -0.000000000000000000, -0.000000000000000000 ) ) ;
#26817=VECTOR ( 'NONE', #9859, 1000.000000000000000 ) ;
#26820=CARTESIAN_POINT ( 'NONE',  ( 0.000000000000000000, -51.02545421589363883, 55.20638768913742922 ) ) ;
#26821=VERTEX_POINT ( 'NONE', #32385 ) ;
#26831=DIRECTION ( 'NONE',  ( 0.000000000000000000, 0.000000000000000000, 1.000000000000000000 ) ) ;
#26833=DIRECTION ( 'NONE',  ( -1.000000000000000000, -0.000000000000000000, 0.000000000000000000 ) ) ;
#26840=CARTESIAN_POINT ( 'NONE',  ( 0.000000000000000000, 62.20884554314020676, 46.21855187248652896 ) ) ;
#26841=EDGE_CURVE ( 'NONE', #16242, #975, #5463, .T. ) ;
#26846=FACE_OUTER_BOUND ( 'NONE', #26216, .T. ) ;
#26850=VECTOR ( 'NONE', #39201, 1000.000000000000000 ) ;
#26851=EDGE_CURVE ( 'NONE', #32445, #1298, #20380, .T. ) ;
#26852=CIRCLE ( 'NONE', #35442, 31.99999999999999289 ) ;
#26853=ORIENTED_EDGE ( 'NONE', *, *, #10498, .T. ) ;
#26855=AXIS2_PLACEMENT_3D ( 'NONE', #8708, #16312, #27095 ) ;
#26859=CIRCLE ( 'NONE', #24514, 82.00000000000000000 ) ;
#26865=FACE_OUTER_BOUND ( 'NONE', #14409, .T. ) ;
#26866=ORIENTED_EDGE ( 'NONE', *, *, #33218, .T. ) ;
#26868=ADVANCED_FACE ( 'NONE', ( #47313 ), #20630, .T. ) ;
#26872=VERTEX_POINT ( 'NONE', #43156 ) ;
#26880=CARTESIAN_POINT ( 'NONE',  ( 15.00000000000000000, -3.948201729842032215, 23.21447184625297666 ) ) ;
#26884=ORIENTED_EDGE ( 'NONE', *, *, #20567, .F. ) ;
#26890=CARTESIAN_POINT ( 'NONE',  ( 12.00000000000000000, -4.261787119644963262, 26.19803753235780164 ) ) ;
#26892=ORIENTED_EDGE ( 'NONE', *, *, #1644, .F. ) ;
#26898=VERTEX_POINT ( 'NONE', #40675 ) ;
#26901=ORIENTED_EDGE ( 'NONE', *, *, #43592, .T. ) ;
#26903=CARTESIAN_POINT ( 'NONE',  ( 0.000000000000000000, 60.67117009219135326, 55.16347631943062169 ) ) ;
#26906=CARTESIAN_POINT ( 'NONE',  ( 0.000000000000000000, -59.75363087400114637, 56.15606465354937171 ) ) ;
#26911=CARTESIAN_POINT ( 'NONE',  ( 0.000000000000000000, 76.69515212746057387, -29.01471420065479379 ) ) ;
#26912=LINE ( 'NONE', #4628, #9817 ) ;
#26915=DIRECTION ( 'NONE',  ( -1.000000000000000000, 0.000000000000000000, -0.000000000000000000 ) ) ;
#26918=EDGE_CURVE ( 'NONE', #30740, #13430, #28110, .T. ) ;
#26921=VECTOR ( 'NONE', #2926, 1000.000000000000000 ) ;
#26930=EDGE_CURVE ( 'NONE', #4565, #42647, #14801, .T. ) ;
#26936=CARTESIAN_POINT ( 'NONE',  ( 15.00000000000000000, 22.07842321921480888, -8.187992925817425771 ) ) ;
#26937=CIRCLE ( 'NONE', #33181, 82.00000000000000000 ) ;
#26942=VECTOR ( 'NONE', #46654, 1000.000000000000000 ) ;
#26946=ORIENTED_EDGE ( 'NONE', *, *, #35523, .T. ) ;
#26948=ORIENTED_EDGE ( 'NONE', *, *, #18333, .T. ) ;
#26955=ORIENTED_EDGE ( 'NONE', *, *, #25801, .F. ) ;
#26958=CARTESIAN_POINT ( 'NONE',  ( 11.99999999999999822, 62.20884554314020676, 46.21855187248652896 ) ) ;
#26959=EDGE_LOOP ( 'NONE', ( #23853, #32374, #18528, #22383 ) ) ;
#26962=CARTESIAN_POINT ( 'NONE',  ( 0.000000000000000000, -73.73191006444582740, 14.66109333815435889 ) ) ;
#26966=AXIS2_PLACEMENT_3D ( 'NONE', #11338, #45833, #34303 ) ;
#26970=CARTESIAN_POINT ( 'NONE',  ( 0.000000000000000000, -73.73191006444561424, -14.66109333815538918 ) ) ;
#26971=DIRECTION ( 'NONE',  ( 0.000000000000000000, 0.000000000000000000, 1.000000000000000000 ) ) ;
#26974=VECTOR ( 'NONE', #29692, 1000.000000000000000 ) ;
#26979=EDGE_CURVE ( 'NONE', #22916, #1311, #32766, .T. ) ;
#26981=EDGE_CURVE ( 'NONE', #1470, #24537, #17926, .T. ) ;
#26985=DIRECTION ( 'NONE',  ( -1.000000000000000000, 0.000000000000000000, -0.000000000000000000 ) ) ;
#26988=VERTEX_POINT ( 'NONE', #7392 ) ;
#26990=FACE_BOUND ( 'NONE', #48302, .T. ) ;
#26993=EDGE_CURVE ( 'NONE', #5309, #17850, #29431, .T. ) ;
#26997=ORIENTED_EDGE ( 'NONE', *, *, #21744, .T. ) ;
#26999=ORIENTED_EDGE ( 'NONE', *, *, #44755, .T. ) ;
#27006=ORIENTED_EDGE ( 'NONE', *, *, #42432, .T. ) ;
#27012=CARTESIAN_POINT ( 'NONE',  ( 12.00000000000000000, -20.55727247249725664, 16.78983467731313084 ) ) ;
#27014=EDGE_CURVE ( 'NONE', #31086, #29937, #38276, .T. ) ;
#27022=ORIENTED_EDGE ( 'NONE', *, *, #36151, .T. ) ;
#27029=CARTESIAN_POINT ( 'NONE',  ( 11.99999999999999822, 51.03279382321088065, 55.19960302592086521 ) ) ;
#27030=DIRECTION ( 'NONE',  ( 0.000000000000000000, 0.000000000000000000, 1.000000000000000000 ) ) ;
#27033=CARTESIAN_POINT ( 'NONE',  ( 11.99999999999999822, -73.44644590900043113, -24.73286445877782924 ) ) ;
#27037=DIRECTION ( 'NONE',  ( -1.000000000000000000, -0.000000000000000000, 0.000000000000000000 ) ) ;
#27038=DIRECTION ( 'NONE',  ( -1.000000000000000000, -0.000000000000000000, -0.000000000000000000 ) ) ;
#27041=CARTESIAN_POINT ( 'NONE',  ( 11.99999999999999822, -73.95703589263990807, 23.16143007188399139 ) ) ;
#27043=VECTOR ( 'NONE', #26156, 1000.000000000000000 ) ;
#27047=VERTEX_POINT ( 'NONE', #4209 ) ;
#27050=DIRECTION ( 'NONE',  ( 1.000000000000000000, -0.000000000000000000, -0.000000000000000000 ) ) ;
#27054=AXIS2_PLACEMENT_3D ( 'NONE', #9090, #20326, #27951 ) ;
#27058=EDGE_LOOP ( 'NONE', ( #990, #511, #10077, #17263 ) ) ;
#27062=LINE ( 'NONE', #19219, #25377 ) ;
#27063=ORIENTED_EDGE ( 'NONE', *, *, #10899, .T. ) ;
#27066=AXIS2_PLACEMENT_3D ( 'NONE', #47379, #6493, #18215 ) ;
#27072=ORIENTED_EDGE ( 'NONE', *, *, #6802, .T. ) ;
#27075=VERTEX_POINT ( 'NONE', #15465 ) ;
#27088=CARTESIAN_POINT ( 'NONE',  ( 6.000000000000000000, 80.55351364060611274, -15.33399622253396899 ) ) ;
#27089=VERTEX_POINT ( 'NONE', #42132 ) ;
#27093=CARTESIAN_POINT ( 'NONE',  ( 11.99999999999999822, -41.76937507738831812, 62.50329211542423025 ) ) ;
#27095=DIRECTION ( 'NONE',  ( 0.000000000000000000, 0.2334453638558989796, 0.9723699203976782224 ) ) ;
#27097=VECTOR ( 'NONE', #37962, 1000.000000000000000 ) ;
#27098=EDGE_CURVE ( 'NONE', #46297, #25935, #42960, .T. ) ;
#27106=EDGE_CURVE ( 'NONE', #17899, #6838, #729, .T. ) ;
#27111=ORIENTED_EDGE ( 'NONE', *, *, #44436, .F. ) ;
#27113=CIRCLE ( 'NONE', #18494, 31.99999999999998579 ) ;
#27116=CIRCLE ( 'NONE', #1291, 77.49900000000000944 ) ;
#27118=ORIENTED_EDGE ( 'NONE', *, *, #21286, .T. ) ;
#27125=LINE ( 'NONE', #7780, #46812 ) ;
#27135=DIRECTION ( 'NONE',  ( -1.000000000000000000, -0.000000000000000000, 0.000000000000000000 ) ) ;
#27137=ORIENTED_EDGE ( 'NONE', *, *, #5996, .T. ) ;
#27138=DIRECTION ( 'NONE',  ( 0.000000000000000000, 0.000000000000000000, 1.000000000000000000 ) ) ;
#27140=EDGE_CURVE ( 'NONE', #22304, #36859, #18870, .T. ) ;
#27141=ORIENTED_EDGE ( 'NONE', *, *, #31861, .T. ) ;
#27142=ORIENTED_EDGE ( 'NONE', *, *, #16850, .F. ) ;
#27144=( NAMED_UNIT ( * ) SI_UNIT ( $, .STERADIAN. ) SOLID_ANGLE_UNIT ( ) );
#27145=CARTESIAN_POINT ( 'NONE',  ( 0.000000000000000000, -66.50666863322028632, 39.78640506895582973 ) ) ;
#27146=AXIS2_PLACEMENT_3D ( 'NONE', #2314, #23875, #5282 ) ;
#27152=CYLINDRICAL_SURFACE ( 'NONE', #30820, 82.00000000000000000 ) ;
#27154=DIRECTION ( 'NONE',  ( 0.000000000000000000, 0.000000000000000000, 1.000000000000000000 ) ) ;
#27160=CYLINDRICAL_SURFACE ( 'NONE', #2045, 31.99999999999998579 ) ;
#27166=DIRECTION ( 'NONE',  ( -1.000000000000000000, -0.000000000000000000, -0.000000000000000000 ) ) ;
#27168=CARTESIAN_POINT ( 'NONE',  ( 15.00000000000000000, -11.95096189432312350, 23.69967320028773372 ) ) ;
#27169=DIRECTION ( 'NONE',  ( -1.000000000000000000, -0.000000000000000000, -0.000000000000000000 ) ) ;
#27170=ORIENTED_EDGE ( 'NONE', *, *, #32329, .F. ) ;
#27176=ORIENTED_EDGE ( 'NONE', *, *, #27257, .T. ) ;
#27177=ORIENTED_EDGE ( 'NONE', *, *, #30195, .T. ) ;
#27179=DIRECTION ( 'NONE',  ( -1.000000000000000000, 0.000000000000000000, -0.000000000000000000 ) ) ;
#27182=ORIENTED_EDGE ( 'NONE', *, *, #33692, .T. ) ;
#27183=LINE ( 'NONE', #46025, #11426 ) ;
#27186=ORIENTED_EDGE ( 'NONE', *, *, #29689, .T. ) ;
#27188=DIRECTION ( 'NONE',  ( -1.000000000000000000, -0.000000000000000000, -0.000000000000000000 ) ) ;
#27189=CARTESIAN_POINT ( 'NONE',  ( 11.99999999999999822, 0.000000000000000000, 0.000000000000000000 ) ) ;
#27190=EDGE_CURVE ( 'NONE', #31053, #42577, #31226, .T. ) ;
#27192=PLANE ( 'NONE',  #3212 ) ;
#27194=CIRCLE ( 'NONE', #8424, 82.00000000000000000 ) ;
#27196=CYLINDRICAL_SURFACE ( 'NONE', #45394, 82.00000000000000000 ) ;
#27197=ORIENTED_EDGE ( 'NONE', *, *, #36362, .T. ) ;
#27199=VERTEX_POINT ( 'NONE', #35981 ) ;
#27200=ORIENTED_EDGE ( 'NONE', *, *, #16790, .T. ) ;
#27208=EDGE_CURVE ( 'NONE', #46458, #19020, #31370, .T. ) ;
#27209=FACE_OUTER_BOUND ( 'NONE', #39595, .T. ) ;
#27214=EDGE_CURVE ( 'NONE', #30440, #48354, #47618, .T. ) ;
#27217=ORIENTED_EDGE ( 'NONE', *, *, #15315, .T. ) ;
#27223=EDGE_CURVE ( 'NONE', #24537, #23027, #11688, .T. ) ;
#27225=DIRECTION ( 'NONE',  ( 0.000000000000000000, 0.000000000000000000, 1.000000000000000000 ) ) ;
#27230=ORIENTED_EDGE ( 'NONE', *, *, #26918, .T. ) ;
#27233=CARTESIAN_POINT ( 'NONE',  ( 11.99999999999999822, -20.41045688087772092, -72.35160999960838524 ) ) ;
#27235=FACE_OUTER_BOUND ( 'NONE', #18011, .T. ) ;
#27238=ORIENTED_EDGE ( 'NONE', *, *, #36476, .F. ) ;
#27240=ORIENTED_EDGE ( 'NONE', *, *, #33329, .F. ) ;
#27242=EDGE_CURVE ( 'NONE', #1046, #39954, #14025, .T. ) ;
#27243=CIRCLE ( 'NONE', #677, 31.99999999999999289 ) ;
#27256=VERTEX_POINT ( 'NONE', #21049 ) ;
#27257=EDGE_CURVE ( 'NONE', #5571, #47807, #9314, .T. ) ;
#27260=CARTESIAN_POINT ( 'NONE',  ( 15.00000000000000000, 5.835314593368470248, -22.81335362449854642 ) ) ;
#27262=FACE_OUTER_BOUND ( 'NONE', #45951, .T. ) ;
#27266=CYLINDRICAL_SURFACE ( 'NONE', #14932, 82.00000000000000000 ) ;
#27268=VECTOR ( 'NONE', #33818, 1000.000000000000000 ) ;
#27272=EDGE_CURVE ( 'NONE', #47811, #31605, #17139, .T. ) ;
#27274=DIRECTION ( 'NONE',  ( -1.000000000000000000, -0.000000000000000000, -0.000000000000000000 ) ) ;
#27282=CIRCLE ( 'NONE', #23453, 82.00000000000000000 ) ;
#27283=ORIENTED_EDGE ( 'NONE', *, *, #25945, .F. ) ;
#27284=VERTEX_POINT ( 'NONE', #9085 ) ;
#27287=VECTOR ( 'NONE', #41096, 1000.000000000000000 ) ;
#27290=EDGE_CURVE ( 'NONE', #41381, #410, #20094, .T. ) ;
#27292=ORIENTED_EDGE ( 'NONE', *, *, #2118, .T. ) ;
#27293=ORIENTED_EDGE ( 'NONE', *, *, #6854, .F. ) ;
#27296=DIRECTION ( 'NONE',  ( -1.000000000000000000, 0.000000000000000000, 0.000000000000000000 ) ) ;
#27302=ORIENTED_EDGE ( 'NONE', *, *, #45644, .T. ) ;
#27305=CARTESIAN_POINT ( 'NONE',  ( 0.000000000000000000, -70.53064760720336324, 26.01480285779810231 ) ) ;
#27308=VECTOR ( 'NONE', #8108, 1000.000000000000000 ) ;
#27311=AXIS2_PLACEMENT_3D ( 'NONE', #13145, #35662, #16568 ) ;
#27313=ORIENTED_EDGE ( 'NONE', *, *, #9650, .T. ) ;
#27316=AXIS2_PLACEMENT_3D ( 'NONE', #33474, #40823, #18550 ) ;
#27317=CYLINDRICAL_SURFACE ( 'NONE', #32692, 31.99999999999998579 ) ;
#27320=DIRECTION ( 'NONE',  ( 0.000000000000000000, 0.9510565162951536422, 0.3090169943749471182 ) ) ;
#27321=DIRECTION ( 'NONE',  ( -1.000000000000000000, 0.000000000000000000, 0.000000000000000000 ) ) ;
#27323=ORIENTED_EDGE ( 'NONE', *, *, #31152, .F. ) ;
#27325=CARTESIAN_POINT ( 'NONE',  ( 0.000000000000000000, -76.66974797899844418, 11.30684508768314522 ) ) ;
#27326=CARTESIAN_POINT ( 'NONE',  ( 11.99999999999999822, 8.840884882375075193, 74.65374052328651544 ) ) ;
#27332=CARTESIAN_POINT ( 'NONE',  ( 0.000000000000000000, -69.42325613327415113, -34.44570377933671779 ) ) ;
#27335=DIRECTION ( 'NONE',  ( -1.000000000000000000, 0.000000000000000000, 0.000000000000000000 ) ) ;
#27339=CARTESIAN_POINT ( 'NONE',  ( 6.000000000000000000, 22.90783923731740401, -78.73519480814930205 ) ) ;
#27340=VERTEX_POINT ( 'NONE', #25673 ) ;
#27342=ORIENTED_EDGE ( 'NONE', *, *, #37409, .T. ) ;
#27343=AXIS2_PLACEMENT_3D ( 'NONE', #9953, #6054, #36845 ) ;
#27346=DIRECTION ( 'NONE',  ( -1.000000000000000000, -0.000000000000000000, -0.000000000000000000 ) ) ;
#27353=DIRECTION ( 'NONE',  ( -1.000000000000000000, -0.000000000000000000, -0.000000000000000000 ) ) ;
#27359=ORIENTED_EDGE ( 'NONE', *, *, #45225, .T. ) ;
#27363=PLANE ( 'NONE',  #20037 ) ;
#27364=ORIENTED_EDGE ( 'NONE', *, *, #25062, .F. ) ;
#27365=ORIENTED_EDGE ( 'NONE', *, *, #32701, .F. ) ;
#27366=EDGE_CURVE ( 'NONE', #5777, #39278, #32061, .T. ) ;
#27367=LINE ( 'NONE', #8749, #9346 ) ;
#27385=EDGE_CURVE ( 'NONE', #19503, #36132, #34368, .T. ) ;
#27398=VERTEX_POINT ( 'NONE', #25922 ) ;
#27403=DIRECTION ( 'NONE',  ( 0.000000000000000000, 0.000000000000000000, -1.000000000000000000 ) ) ;
#27404=EDGE_LOOP ( 'NONE', ( #11875, #40776, #42324, #45984 ) ) ;
#27411=ORIENTED_EDGE ( 'NONE', *, *, #41777, .F. ) ;
#27414=AXIS2_PLACEMENT_3D ( 'NONE', #12570, #8887, #5235 ) ;
#27425=ORIENTED_EDGE ( 'NONE', *, *, #36893, .T. ) ;
#27426=COLOUR_RGB ( '', 0.72549020, 0.75294118, 0.79215686) ;
#27429=VERTEX_POINT ( 'NONE', #28872 ) ;
#27435=ORIENTED_EDGE ( 'NONE', *, *, #41782, .F. ) ;
#27437=DIRECTION ( 'NONE',  ( -1.000000000000000000, -0.000000000000000000, -0.000000000000000000 ) ) ;
#27438=VERTEX_POINT ( 'NONE', #43807 ) ;
#27445=DIRECTION ( 'NONE',  ( 0.000000000000000000, -0.07845909572785224328, 0.9969173337331274087 ) ) ;
#27448=CYLINDRICAL_SURFACE ( 'NONE', #21970, 31.99999999999998579 ) ;
#27450=CIRCLE ( 'NONE', #44662, 31.99999999999998579 ) ;
#27454=DIRECTION ( 'NONE',  ( 1.000000000000000000, 0.000000000000000000, 0.000000000000000000 ) ) ;
#27456=AXIS2_PLACEMENT_3D ( 'NONE', #35722, #21257, #24712 ) ;
#27464=CIRCLE ( 'NONE', #19606, 77.49899999999999523 ) ;
#27473=DIRECTION ( 'NONE',  ( 0.000000000000000000, 0.3826834323650904479, -0.9238795325112865164 ) ) ;
#27479=EDGE_CURVE ( 'NONE', #25392, #43802, #938, .T. ) ;
#27482=ORIENTED_EDGE ( 'NONE', *, *, #8126, .T. ) ;
#27493=DIRECTION ( 'NONE',  ( -1.000000000000000000, 0.000000000000000000, 0.000000000000000000 ) ) ;
#27502=DIRECTION ( 'NONE',  ( 0.000000000000000000, 0.6691306063588569053, -0.7431448254773954654 ) ) ;
#27503=DIRECTION ( 'NONE',  ( -1.000000000000000000, -0.000000000000000000, 0.000000000000000000 ) ) ;
#27507=DIRECTION ( 'NONE',  ( 0.000000000000000000, -0.7604059656000226042, -0.6494480483301934282 ) ) ;
#27508=FACE_OUTER_BOUND ( 'NONE', #5538, .T. ) ;
#27516=CARTESIAN_POINT ( 'NONE',  ( 0.000000000000000000, 0.000000000000000000, 0.000000000000000000 ) ) ;
#27519=ORIENTED_EDGE ( 'NONE', *, *, #19317, .F. ) ;
#27525=CIRCLE ( 'NONE', #25960, 82.00000000000000000 ) ;
#27531=EDGE_CURVE ( 'NONE', #48354, #33766, #42186, .T. ) ;
#27532=PLANE ( 'NONE',  #44052 ) ;
#27533=ADVANCED_FACE ( 'NONE', ( #26426 ), #19526, .T. ) ;
#27534=LINE ( 'NONE', #2080, #46907 ) ;
#27535=FACE_OUTER_BOUND ( 'NONE', #15562, .T. ) ;
#27537=ORIENTED_EDGE ( 'NONE', *, *, #41565, .F. ) ;
#27543=VECTOR ( 'NONE', #16078, 1000.000000000000114 ) ;
#27550=AXIS2_PLACEMENT_3D ( 'NONE', #29352, #44277, #25655 ) ;
#27551=CARTESIAN_POINT ( 'NONE',  ( 0.000000000000000000, -68.26794271651239399, -31.47745569255214093 ) ) ;
#27552=CARTESIAN_POINT ( 'NONE',  ( 11.99999999999999822, -70.52718814184240159, -26.02418014898383802 ) ) ;
#27555=CARTESIAN_POINT ( 'NONE',  ( 11.99999999999999822, 28.89263327155746097, 71.91182617369197771 ) ) ;
#27558=ORIENTED_EDGE ( 'NONE', *, *, #36246, .T. ) ;
#27559=CARTESIAN_POINT ( 'NONE',  ( 15.00000000000000000, -13.04903810567675393, -19.60159698893424718 ) ) ;
#27564=ORIENTED_EDGE ( 'NONE', *, *, #31339, .F. ) ;
#27568=LINE ( 'NONE', #4346, #6515 ) ;
#27571=VERTEX_POINT ( 'NONE', #8046 ) ;
#27578=ORIENTED_EDGE ( 'NONE', *, *, #32920, .T. ) ;
#27580=DIRECTION ( 'NONE',  ( -1.000000000000000000, 0.000000000000000000, -0.000000000000000000 ) ) ;
#27581=EDGE_CURVE ( 'NONE', #15507, #27199, #38162, .T. ) ;
#27585=VERTEX_POINT ( 'NONE', #22173 ) ;
#27586=CIRCLE ( 'NONE', #22887, 31.99999999999998579 ) ;
#27587=VECTOR ( 'NONE', #33728, 1000.000000000000114 ) ;
#27590=AXIS2_PLACEMENT_3D ( 'NONE', #29549, #3103, #41069 ) ;
#27592=CARTESIAN_POINT ( 'NONE',  ( 15.00000000000000000, -22.32062822937469093, 14.36278369418830181 ) ) ;
#27594=FACE_OUTER_BOUND ( 'NONE', #33709, .T. ) ;
#27596=ORIENTED_EDGE ( 'NONE', *, *, #39351, .T. ) ;
#27600=EDGE_CURVE ( 'NONE', #24540, #27912, #20294, .T. ) ;
#27603=CARTESIAN_POINT ( 'NONE',  ( 0.000000000000000000, 80.28980883073758434, 16.65972982744962749 ) ) ;
#27607=FACE_OUTER_BOUND ( 'NONE', #21759, .T. ) ;
#27611=DIRECTION ( 'NONE',  ( -1.000000000000000000, -0.000000000000000000, 0.000000000000000000 ) ) ;
#27614=ORIENTED_EDGE ( 'NONE', *, *, #30133, .T. ) ;
#27619=CARTESIAN_POINT ( 'NONE',  ( 6.000000000000000000, -29.01471420065616513, 76.69515212746007649 ) ) ;
#27634=CARTESIAN_POINT ( 'NONE',  ( 11.99999999999999822, 0.000000000000000000, 0.000000000000000000 ) ) ;
#27641=CIRCLE ( 'NONE', #33878, 31.99999999999998579 ) ;
#27642=ORIENTED_EDGE ( 'NONE', *, *, #43118, .F. ) ;
#27647=DIRECTION ( 'NONE',  ( 0.000000000000000000, 0.3826834323650841752, 0.9238795325112891810 ) ) ;
#27651=DIRECTION ( 'NONE',  ( 0.000000000000000000, 0.000000000000000000, 1.000000000000000000 ) ) ;
#27660=CIRCLE ( 'NONE', #11240, 31.99999999999998579 ) ;
#27661=CIRCLE ( 'NONE', #32388, 77.49900000000000944 ) ;
#27665=VECTOR ( 'NONE', #13006, 1000.000000000000000 ) ;
#27671=EDGE_LOOP ( 'NONE', ( #40852, #31044, #27435, #11681 ) ) ;
#27672=CARTESIAN_POINT ( 'NONE',  ( 11.99999999999999822, 0.000000000000000000, 77.49899999999999523 ) ) ;
#27678=CARTESIAN_POINT ( 'NONE',  ( 0.000000000000000000, 0.000000000000000000, 0.000000000000000000 ) ) ;
#27680=ORIENTED_EDGE ( 'NONE', *, *, #20213, .T. ) ;
#27681=DIRECTION ( 'NONE',  ( 0.000000000000000000, 0.5877852522924689183, -0.8090169943749504489 ) ) ;
#27683=EDGE_CURVE ( 'NONE', #41443, #42392, #37100, .T. ) ;
#27684=CYLINDRICAL_SURFACE ( 'NONE', #45676, 82.00000000000000000 ) ;
#27685=DIRECTION ( 'NONE',  ( -1.000000000000000000, 0.000000000000000000, 0.000000000000000000 ) ) ;
#27686=DIRECTION ( 'NONE',  ( -1.000000000000000000, 0.000000000000000000, -0.000000000000000000 ) ) ;
#27688=DIRECTION ( 'NONE',  ( 0.000000000000000000, -0.5877852522924779111, -0.8090169943749440096 ) ) ;
#27690=AXIS2_PLACEMENT_3D ( 'NONE', #44978, #11461, #26379 ) ;
#27691=CARTESIAN_POINT ( 'NONE',  ( 0.000000000000000000, -62.20884554314051229, 46.21855187248609553 ) ) ;
#27697=VECTOR ( 'NONE', #13060, 1000.000000000000000 ) ;
#27699=PLANE ( 'NONE',  #17429 ) ;
#27700=DIRECTION ( 'NONE',  ( 0.000000000000000000, -0.8090169943749530024, 0.5877852522924653655 ) ) ;
#27702=CARTESIAN_POINT ( 'NONE',  ( 11.99999999999999822, -74.65491531819111515, 23.16904090965678265 ) ) ;
#27706=VERTEX_POINT ( 'NONE', #10191 ) ;
#27716=DIRECTION ( 'NONE',  ( -1.000000000000000000, -0.000000000000000000, -0.000000000000000000 ) ) ;
#27717=CIRCLE ( 'NONE', #8172, 31.99999999999997868 ) ;
#27718=VERTEX_POINT ( 'NONE', #36610 ) ;
#27720=DIRECTION ( 'NONE',  ( 0.000000000000000000, 0.8090169943749445647, 0.5877852522924770229 ) ) ;
#27721=EDGE_CURVE ( 'NONE', #352, #14857, #43961, .T. ) ;
#27729=CARTESIAN_POINT ( 'NONE',  ( 15.00000000000000000, 5.835314593368777558, 22.81335362449846471 ) ) ;
#27733=DIRECTION ( 'NONE',  ( 0.000000000000000000, 0.000000000000000000, 1.000000000000000000 ) ) ;
#27735=CARTESIAN_POINT ( 'NONE',  ( 11.99999999999999822, 64.81221759200417409, -50.23322058963275794 ) ) ;
#27738=DIRECTION ( 'NONE',  ( -1.000000000000000000, -0.000000000000000000, 0.000000000000000000 ) ) ;
#27749=VERTEX_POINT ( 'NONE', #38079 ) ;
#27750=EDGE_CURVE ( 'NONE', #33596, #17439, #34375, .T. ) ;
#27756=DIRECTION ( 'NONE',  ( -1.000000000000000000, 0.000000000000000000, -0.000000000000000000 ) ) ;
#27757=EDGE_CURVE ( 'NONE', #37621, #44069, #38309, .T. ) ;
#27760=DIRECTION ( 'NONE',  ( 1.000000000000000000, 0.000000000000000000, 0.000000000000000000 ) ) ;
#27765=DIRECTION ( 'NONE',  ( -1.000000000000000000, -0.000000000000000000, 0.000000000000000000 ) ) ;
#27766=CARTESIAN_POINT ( 'NONE',  ( 12.00000000000000000, 26.49999999999999645, 1.499999999999995781 ) ) ;
#27767=CARTESIAN_POINT ( 'NONE',  ( 0.000000000000000000, -75.16055320797016748, -18.89407956138335365 ) ) ;
#27775=AXIS2_PLACEMENT_3D ( 'NONE', #10387, #10644, #25552 ) ;
#27776=CARTESIAN_POINT ( 'NONE',  ( 0.000000000000000000, 0.000000000000000000, 0.000000000000000000 ) ) ;
#27777=ORIENTED_EDGE ( 'NONE', *, *, #42164, .F. ) ;
#27780=CIRCLE ( 'NONE', #6662, 31.99999999999999289 ) ;
#27784=AXIS2_PLACEMENT_3D ( 'NONE', #20198, #31476, #12868 ) ;
#27794=ORIENTED_EDGE ( 'NONE', *, *, #33696, .T. ) ;
#27802=ORIENTED_EDGE ( 'NONE', *, *, #7204, .F. ) ;
#27803=ORIENTED_EDGE ( 'NONE', *, *, #35555, .T. ) ;
#27811=DIRECTION ( 'NONE',  ( 0.000000000000000000, 0.5877852522924797984, 0.8090169943749426773 ) ) ;
#27815=ORIENTED_EDGE ( 'NONE', *, *, #39649, .F. ) ;
#27818=DIRECTION ( 'NONE',  ( 1.000000000000000000, -0.000000000000000000, -0.000000000000000000 ) ) ;
#27826=CARTESIAN_POINT ( 'NONE',  ( 12.00000000000000000, -13.04903810567675393, -19.60159698893424718 ) ) ;
#27827=EDGE_CURVE ( 'NONE', #28563, #45738, #46941, .T. ) ;
#27832=DIRECTION ( 'NONE',  ( 0.000000000000000000, 0.000000000000000000, 1.000000000000000000 ) ) ;
#27833=CARTESIAN_POINT ( 'NONE',  ( 0.000000000000000000, 77.19088730480524418, 6.903761155838049390 ) ) ;
#27835=ORIENTED_EDGE ( 'NONE', *, *, #22543, .F. ) ;
#27837=AXIS2_PLACEMENT_3D ( 'NONE', #42223, #13100, #31957 ) ;
#27848=CARTESIAN_POINT ( 'NONE',  ( 0.000000000000000000, -50.23322058963393744, 64.81221759200325039 ) ) ;
#27854=DIRECTION ( 'NONE',  ( -1.000000000000000000, 0.000000000000000000, -0.000000000000000000 ) ) ;
#27855=ORIENTED_EDGE ( 'NONE', *, *, #21438, .F. ) ;
#27857=ORIENTED_EDGE ( 'NONE', *, *, #10774, .F. ) ;
#27862=ORIENTED_EDGE ( 'NONE', *, *, #23862, .F. ) ;
#27867=ORIENTED_EDGE ( 'NONE', *, *, #34817, .F. ) ;
#27868=CARTESIAN_POINT ( 'NONE',  ( 11.99999999999999822, 73.44644590900061587, 24.73286445877730699 ) ) ;
#27869=CARTESIAN_POINT ( 'NONE',  ( 11.99999999999999822, 74.65491531819105830, 8.830959090343693418 ) ) ;
#27872=CIRCLE ( 'NONE', #34092, 77.49900000000000944 ) ;
#27875=CARTESIAN_POINT ( 'NONE',  ( 15.00000000000000000, -23.29833615347104470, 3.418703333116808629 ) ) ;
#27879=EDGE_CURVE ( 'NONE', #38615, #13555, #21904, .T. ) ;
#27885=ORIENTED_EDGE ( 'NONE', *, *, #140, .F. ) ;
#27886=EDGE_CURVE ( 'NONE', #34677, #43252, #42209, .T. ) ;
#27891=CARTESIAN_POINT ( 'NONE',  ( 11.99999999999999822, 22.90783923731740401, -78.73519480814930205 ) ) ;
#27897=AXIS2_PLACEMENT_3D ( 'NONE', #43506, #39834, #28320 ) ;
#27903=LINE ( 'NONE', #1944, #9631 ) ;
#27910=ORIENTED_EDGE ( 'NONE', *, *, #1973, .F. ) ;
#27912=VERTEX_POINT ( 'NONE', #28508 ) ;
#27919=EDGE_CURVE ( 'NONE', #5925, #21150, #22682, .T. ) ;
#27932=ORIENTED_EDGE ( 'NONE', *, *, #8824, .T. ) ;
#27943=CARTESIAN_POINT ( 'NONE',  ( 11.99999999999999822, -70.53064760720336324, 26.01480285779810231 ) ) ;
#27944=DIRECTION ( 'NONE',  ( 0.000000000000000000, 0.000000000000000000, 1.000000000000000000 ) ) ;
#27946=LINE ( 'NONE', #3102, #32202 ) ;
#27948=DIRECTION ( 'NONE',  ( 0.000000000000000000, 0.000000000000000000, 1.000000000000000000 ) ) ;
#27951=DIRECTION ( 'NONE',  ( 0.000000000000000000, -0.9969173337331270757, -0.07845909572785580988 ) ) ;
#27957=VECTOR ( 'NONE', #34101, 1000.000000000000000 ) ;
#27960=VECTOR ( 'NONE', #21486, 1000.000000000000000 ) ;
#27969=CIRCLE ( 'NONE', #11541, 77.49899999999999523 ) ;
#27970=DIRECTION ( 'NONE',  ( 0.000000000000000000, 0.000000000000000000, 1.000000000000000000 ) ) ;
#27978=FACE_OUTER_BOUND ( 'NONE', #45120, .T. ) ;
#27987=EDGE_CURVE ( 'NONE', #38298, #42647, #43820, .T. ) ;
#27991=ADVANCED_FACE ( 'NONE', ( #24828 ), #31464, .T. ) ;
#27992=DIRECTION ( 'NONE',  ( -1.000000000000000000, -0.000000000000000000, 0.000000000000000000 ) ) ;
#27993=DIRECTION ( 'NONE',  ( -1.000000000000000000, 0.000000000000000000, 0.000000000000000000 ) ) ;
#27995=CARTESIAN_POINT ( 'NONE',  ( 11.99999999999999822, 17.28742895386189460, -75.54627589209927407 ) ) ;
#27997=FACE_OUTER_BOUND ( 'NONE', #40134, .T. ) ;
#27998=DIRECTION ( 'NONE',  ( 0.000000000000000000, 0.3090169943749480064, -0.9510565162951534202 ) ) ;
#27999=PLANE ( 'NONE',  #13004 ) ;
#28004=PLANE ( 'NONE',  #41741 ) ;
#28011=DIRECTION ( 'NONE',  ( -1.000000000000000000, 0.000000000000000000, 0.000000000000000000 ) ) ;
#28013=EDGE_CURVE ( 'NONE', #16230, #36455, #13568, .T. ) ;
#28014=EDGE_CURVE ( 'NONE', #20184, #18, #6232, .T. ) ;
#28018=ORIENTED_EDGE ( 'NONE', *, *, #32701, .T. ) ;
#28030=ADVANCED_FACE ( 'NONE', ( #48319 ), #26298, .T. ) ;
#28031=ADVANCED_FACE ( 'NONE', ( #7689 ), #29717, .T. ) ;
#28034=DIRECTION ( 'NONE',  ( 1.000000000000000000, -0.000000000000000000, -0.000000000000000000 ) ) ;
#28038=CARTESIAN_POINT ( 'NONE',  ( 11.99999999999999822, -65.58780272294100655, 36.73666225445870737 ) ) ;
#28047=ORIENTED_EDGE ( 'NONE', *, *, #19217, .T. ) ;
#28053=DIRECTION ( 'NONE',  ( 0.000000000000000000, 0.9876883405951371042, 0.1564344650402346715 ) ) ;
#28066=CARTESIAN_POINT ( 'NONE',  ( -10.00000000000000000, 0.000000000000000000, 0.000000000000000000 ) ) ;
#28070=VERTEX_POINT ( 'NONE', #7922 ) ;
#28071=EDGE_CURVE ( 'NONE', #11938, #35871, #48083, .T. ) ;
#28074=EDGE_CURVE ( 'NONE', #6779, #5309, #22710, .T. ) ;
#28075=CARTESIAN_POINT ( 'NONE',  ( 11.99999999999999822, -33.71516098798793593, 74.74816331893418919 ) ) ;
#28088=ORIENTED_EDGE ( 'NONE', *, *, #36195, .F. ) ;
#28099=ADVANCED_FACE ( 'NONE', ( #4278 ), #15292, .T. ) ;
#28103=ORIENTED_EDGE ( 'NONE', *, *, #15031, .F. ) ;
#28104=DIRECTION ( 'NONE',  ( -1.000000000000000000, 0.000000000000000000, 0.000000000000000000 ) ) ;
#28110=CIRCLE ( 'NONE', #24193, 31.99999999999998579 ) ;
#28119=ORIENTED_EDGE ( 'NONE', *, *, #7480, .F. ) ;
#28120=AXIS2_PLACEMENT_3D ( 'NONE', #38761, #4723, #15990 ) ;
#28121=ORIENTED_EDGE ( 'NONE', *, *, #14609, .T. ) ;
#28123=CARTESIAN_POINT ( 'NONE',  ( 11.99999999999999822, 20.41045688087930898, -72.35160999960793049 ) ) ;
#28125=ORIENTED_EDGE ( 'NONE', *, *, #33376, .T. ) ;
#28127=EDGE_CURVE ( 'NONE', #35715, #25450, #25794, .T. ) ;
#28130=ORIENTED_EDGE ( 'NONE', *, *, #39202, .F. ) ;
#28140=ORIENTED_EDGE ( 'NONE', *, *, #7328, .T. ) ;
#28145=EDGE_LOOP ( 'NONE', ( #29096, #2139, #10990, #23249 ) ) ;
#28149=EDGE_CURVE ( 'NONE', #35932, #36740, #1625, .T. ) ;
#28151=LINE ( 'NONE', #43085, #41295 ) ;
#28153=AXIS2_PLACEMENT_3D ( 'NONE', #35790, #39951, #20613 ) ;
#28163=ADVANCED_FACE ( 'NONE', ( #34840 ), #23106, .T. ) ;
#28164=DIRECTION ( 'NONE',  ( -1.000000000000000000, -0.000000000000000000, -0.000000000000000000 ) ) ;
#28168=LINE ( 'NONE', #39441, #24892 ) ;
#28169=CARTESIAN_POINT ( 'NONE',  ( -10.00000000000000000, 0.000000000000000000, 0.000000000000000000 ) ) ;
#28170=DIRECTION ( 'NONE',  ( 1.000000000000000000, 0.000000000000000000, 0.000000000000000000 ) ) ;
#28171=VERTEX_POINT ( 'NONE', #26772 ) ;
#28175=EDGE_CURVE ( 'NONE', #38262, #43952, #38372, .T. ) ;
#28182=ADVANCED_FACE ( 'NONE', ( #31433 ), #27266, .T. ) ;
#28187=ORIENTED_EDGE ( 'NONE', *, *, #4641, .F. ) ;
#28195=VERTEX_POINT ( 'NONE', #23834 ) ;
#28196=VERTEX_POINT ( 'NONE', #34337 ) ;
#28201=CIRCLE ( 'NONE', #45386, 77.49899999999999523 ) ;
#28209=DIRECTION ( 'NONE',  ( 0.000000000000000000, -0.2334453638559126909, 0.9723699203976748917 ) ) ;
#28210=VECTOR ( 'NONE', #30445, 1000.000000000000000 ) ;
#28213=CARTESIAN_POINT ( 'NONE',  ( 0.000000000000000000, 3.894527615419050903, -81.90746397400384637 ) ) ;
#28214=FACE_OUTER_BOUND ( 'NONE', #46067, .T. ) ;
#28217=DIRECTION ( 'NONE',  ( -1.000000000000000000, 0.000000000000000000, 0.000000000000000000 ) ) ;
#28218=AXIS2_PLACEMENT_3D ( 'NONE', #20082, #27437, #15683 ) ;
#28223=AXIS2_PLACEMENT_3D ( 'NONE', #33497, #22254, #24948 ) ;
#28224=DIRECTION ( 'NONE',  ( 0.000000000000000000, 0.7604059656000277112, 0.6494480483301875440 ) ) ;
#28240=AXIS2_PLACEMENT_3D ( 'NONE', #3964, #18871, #33804 ) ;
#28242=EDGE_CURVE ( 'NONE', #22951, #33006, #836, .T. ) ;
#28245=CARTESIAN_POINT ( 'NONE',  ( 11.99999999999999822, 44.88180994100376608, 63.18004540533043922 ) ) ;
#28246=EDGE_LOOP ( 'NONE', ( #1154, #6212, #21268, #18601 ) ) ;
#28248=VERTEX_POINT ( 'NONE', #38518 ) ;
#28258=ORIENTED_EDGE ( 'NONE', *, *, #15878, .T. ) ;
#28271=CARTESIAN_POINT ( 'NONE',  ( 11.99999999999999822, 72.35160999960844208, -20.41045688087747223 ) ) ;
#28275=CARTESIAN_POINT ( 'NONE',  ( 0.000000000000000000, 14.67089635893819377, -73.72996012237423713 ) ) ;
#28276=EDGE_CURVE ( 'NONE', #26988, #34677, #25046, .T. ) ;
#28287=DIRECTION ( 'NONE',  ( -1.000000000000000000, 0.000000000000000000, -0.000000000000000000 ) ) ;
#28294=CARTESIAN_POINT ( 'NONE',  ( 11.99999999999999822, -71.91182617369167929, -28.89263327155821059 ) ) ;
#28298=VERTEX_POINT ( 'NONE', #10099 ) ;
#28301=EDGE_CURVE ( 'NONE', #31941, #15671, #28201, .T. ) ;
#28306=VECTOR ( 'NONE', #37799, 999.9999999999998863 ) ;
#28307=DIRECTION ( 'NONE',  ( 0.000000000000000000, 0.000000000000000000, 1.000000000000000000 ) ) ;
#28312=VERTEX_POINT ( 'NONE', #32386 ) ;
#28314=VECTOR ( 'NONE', #15042, 1000.000000000000000 ) ;
#28320=DIRECTION ( 'NONE',  ( 0.000000000000000000, 0.000000000000000000, -1.000000000000000000 ) ) ;
#28321=FACE_OUTER_BOUND ( 'NONE', #23031, .T. ) ;
#28323=AXIS2_PLACEMENT_3D ( 'NONE', #36363, #2829, #46675 ) ;
#28324=CARTESIAN_POINT ( 'NONE',  ( 0.000000000000000000, -62.50329211542465657, 41.76937507738766442 ) ) ;
#28325=DIRECTION ( 'NONE',  ( -1.000000000000000000, -0.000000000000000000, -0.000000000000000000 ) ) ;
#28326=CARTESIAN_POINT ( 'NONE',  ( 11.99999999999999822, 0.000000000000000000, 0.000000000000000000 ) ) ;
#28332=LINE ( 'NONE', #13174, #17347 ) ;
#28334=ADVANCED_FACE ( 'NONE', ( #39974 ), #28712, .F. ) ;
#28336=CARTESIAN_POINT ( 'NONE',  ( 6.000000000000000000, 2.543863470249533965, -81.96053171279901051 ) ) ;
#28338=DIRECTION ( 'NONE',  ( -1.000000000000000000, 0.000000000000000000, 0.000000000000000000 ) ) ;
#28339=EDGE_CURVE ( 'NONE', #32136, #11391, #43635, .T. ) ;
#28340=FACE_OUTER_BOUND ( 'NONE', #22454, .T. ) ;
#28341=DIRECTION ( 'NONE',  ( -1.000000000000000000, -0.000000000000000000, -0.000000000000000000 ) ) ;
#28343=EDGE_LOOP ( 'NONE', ( #9688, #6122, #24341, #23978 ) ) ;
#28345=DIRECTION ( 'NONE',  ( 0.000000000000000000, 0.5224985647159441360, 0.8526401643540952868 ) ) ;
#28348=AXIS2_PLACEMENT_3D ( 'NONE', #31542, #23443, #46462 ) ;
#28356=EDGE_LOOP ( 'NONE', ( #11351, #12449, #36069, #39028 ) ) ;
#28359=VECTOR ( 'NONE', #43892, 1000.000000000000000 ) ;
#28366=ORIENTED_EDGE ( 'NONE', *, *, #35912, .F. ) ;
#28367=ORIENTED_EDGE ( 'NONE', *, *, #16583, .F. ) ;
#28368=ORIENTED_EDGE ( 'NONE', *, *, #2628, .T. ) ;
#28370=AXIS2_PLACEMENT_3D ( 'NONE', #1491, #15689, #23280 ) ;
#28375=CARTESIAN_POINT ( 'NONE',  ( 0.000000000000000000, 77.32052557432849937, -5.256550761632002633 ) ) ;
#28383=VERTEX_POINT ( 'NONE', #17912 ) ;
#28384=CARTESIAN_POINT ( 'NONE',  ( 11.99999999999999822, 0.000000000000000000, 0.000000000000000000 ) ) ;
#28387=ORIENTED_EDGE ( 'NONE', *, *, #20264, .F. ) ;
#28390=DIRECTION ( 'NONE',  ( -1.000000000000000000, 0.000000000000000000, 0.000000000000000000 ) ) ;
#28391=ORIENTED_EDGE ( 'NONE', *, *, #782, .T. ) ;
#28397=CARTESIAN_POINT ( 'NONE',  ( 15.00000000000000000, 9.615535125378766423, -24.73947219025917121 ) ) ;
#28398=EDGE_CURVE ( 'NONE', #45904, #15507, #32613, .T. ) ;
#28402=CARTESIAN_POINT ( 'NONE',  ( 0.000000000000000000, -26.02418014898359289, 70.52718814184250107 ) ) ;
#28403=CARTESIAN_POINT ( 'NONE',  ( 12.00000000000000000, -23.29833615347104470, 3.418703333116808629 ) ) ;
#28407=DIRECTION ( 'NONE',  ( 0.000000000000000000, 0.2079116908177532363, -0.9781476007338069101 ) ) ;
#28410=EDGE_CURVE ( 'NONE', #35941, #5623, #38410, .T. ) ;
#28414=ORIENTED_EDGE ( 'NONE', *, *, #26841, .T. ) ;
#28415=DIRECTION ( 'NONE',  ( -1.000000000000000000, -0.000000000000000000, -0.000000000000000000 ) ) ;
#28421=AXIS2_PLACEMENT_3D ( 'NONE', #44276, #10506, #48418 ) ;
#28422=LINE ( 'NONE', #35279, #4189 ) ;
#28427=CIRCLE ( 'NONE', #14345, 31.99999999999998224 ) ;
#28431=DIRECTION ( 'NONE',  ( -1.000000000000000000, 0.000000000000000000, -0.000000000000000000 ) ) ;
#28437=ORIENTED_EDGE ( 'NONE', *, *, #6794, .F. ) ;
#28441=CARTESIAN_POINT ( 'NONE',  ( 11.99999999999999822, -41.76937507738745836, -62.50329211542482710 ) ) ;
#28443=VECTOR ( 'NONE', #32736, 1000.000000000000000 ) ;
#28446=CARTESIAN_POINT ( 'NONE',  ( 0.000000000000000000, 35.91791733033570466, -68.67312586194960033 ) ) ;
#28447=VERTEX_POINT ( 'NONE', #13065 ) ;
#28451=ADVANCED_FACE ( 'NONE', ( #27997 ), #39737, .T. ) ;
#28453=CARTESIAN_POINT ( 'NONE',  ( 12.00000000000000000, 26.49999999999999645, 1.499999999999995781 ) ) ;
#28454=CIRCLE ( 'NONE', #1085, 31.99999999999999289 ) ;
#28455=ADVANCED_FACE ( 'NONE', ( #25737 ), #11065, .F. ) ;
#28460=CARTESIAN_POINT ( 'NONE',  ( 11.99999999999999822, 75.11725578898467859, 2.956366410620910656 ) ) ;
#28463=EDGE_CURVE ( 'NONE', #12730, #2585, #10594, .T. ) ;
#28472=DIRECTION ( 'NONE',  ( -1.000000000000000000, 0.000000000000000000, 0.000000000000000000 ) ) ;
#28474=EDGE_CURVE ( 'NONE', #48127, #13412, #25505, .T. ) ;
#28481=CIRCLE ( 'NONE', #9742, 82.00000000000000000 ) ;
#28486=DIRECTION ( 'NONE',  ( -1.000000000000000000, -0.000000000000000000, -0.000000000000000000 ) ) ;
#28488=ORIENTED_EDGE ( 'NONE', *, *, #43550, .T. ) ;
#28489=ADVANCED_FACE ( 'NONE', ( #7635 ), #33341, .T. ) ;
#28503=AXIS2_PLACEMENT_3D ( 'NONE', #36641, #6799, #29313 ) ;
#28508=CARTESIAN_POINT ( 'NONE',  ( 0.000000000000000000, 81.34940948281351325, -10.30890764327295450 ) ) ;
#28509=EDGE_LOOP ( 'NONE', ( #18177, #45969, #12171, #1209 ) ) ;
#28516=ORIENTED_EDGE ( 'NONE', *, *, #3265, .F. ) ;
#28522=DIRECTION ( 'NONE',  ( -1.000000000000000000, 0.000000000000000000, -0.000000000000000000 ) ) ;
#28523=DIRECTION ( 'NONE',  ( 0.000000000000000000, 0.000000000000000000, -1.000000000000000000 ) ) ;
#28530=CARTESIAN_POINT ( 'NONE',  ( 11.99999999999999822, -44.88180994100419952, 63.18004540533013369 ) ) ;
#28538=CARTESIAN_POINT ( 'NONE',  ( 11.99999999999999822, -59.03961581697367933, -46.53671651294010303 ) ) ;
#28543=ORIENTED_EDGE ( 'NONE', *, *, #39208, .T. ) ;
#28549=ORIENTED_EDGE ( 'NONE', *, *, #6913, .T. ) ;
#28554=DIRECTION ( 'NONE',  ( -1.000000000000000000, 0.000000000000000000, -0.000000000000000000 ) ) ;
#28555=ORIENTED_EDGE ( 'NONE', *, *, #43492, .F. ) ;
#28556=ORIENTED_EDGE ( 'NONE', *, *, #7394, .T. ) ;
#28557=CIRCLE ( 'NONE', #2018, 77.49900000000000944 ) ;
#28561=LINE ( 'NONE', #24160, #34736 ) ;
#28563=VERTEX_POINT ( 'NONE', #18410 ) ;
#28566=CARTESIAN_POINT ( 'NONE',  ( 0.000000000000000000, 0.000000000000000000, 0.000000000000000000 ) ) ;
#28568=DIRECTION ( 'NONE',  ( 0.000000000000000000, -0.9510565162951543083, -0.3090169943749448977 ) ) ;
#28575=CYLINDRICAL_SURFACE ( 'NONE', #32784, 31.99999999999998579 ) ;
#28580=EDGE_CURVE ( 'NONE', #28248, #20499, #14986, .T. ) ;
#28582=CIRCLE ( 'NONE', #24668, 31.99999999999999289 ) ;
#28586=ADVANCED_FACE ( 'NONE', ( #27209 ), #27448, .T. ) ;
#28589=CARTESIAN_POINT ( 'NONE',  ( 11.99999999999999822, -74.18225833017864090, -34.94270380257717790 ) ) ;
#28591=EDGE_LOOP ( 'NONE', ( #46623, #47569, #16530, #4449 ) ) ;
#28596=EDGE_CURVE ( 'NONE', #24462, #2149, #27450, .T. ) ;
#28612=CIRCLE ( 'NONE', #16110, 21.00000000000000000 ) ;
#28613=LINE ( 'NONE', #28837, #6936 ) ;
#28622=ORIENTED_EDGE ( 'NONE', *, *, #4645, .F. ) ;
#28623=CIRCLE ( 'NONE', #30175, 31.99999999999998224 ) ;
#28627=ORIENTED_EDGE ( 'NONE', *, *, #3798, .T. ) ;
#28628=CARTESIAN_POINT ( 'NONE',  ( -10.00000000000000000, 0.000000000000000000, 0.000000000000000000 ) ) ;
#28631=DIRECTION ( 'NONE',  ( -1.000000000000000000, -0.000000000000000000, 0.000000000000000000 ) ) ;
#28633=EDGE_LOOP ( 'NONE', ( #20547, #24117, #38265, #11912 ) ) ;
#28638=CARTESIAN_POINT ( 'NONE',  ( 11.99999999999999822, -23.16143007188479430, 73.95703589263968070 ) ) ;
#28639=CARTESIAN_POINT ( 'NONE',  ( 15.00000000000000000, -18.13022148937263012, -15.02647892043543898 ) ) ;
#28640=VERTEX_POINT ( 'NONE', #37981 ) ;
#28642=PLANE ( 'NONE',  #29132 ) ;
#28647=CIRCLE ( 'NONE', #31000, 31.99999999999998579 ) ;
#28649=CYLINDRICAL_SURFACE ( 'NONE', #7353, 82.00000000000000000 ) ;
#28651=EDGE_CURVE ( 'NONE', #40154, #16137, #33684, .T. ) ;
#28656=CARTESIAN_POINT ( 'NONE',  ( 15.00000000000000000, 22.07842321921492612, 8.187992925817123790 ) ) ;
#28659=CARTESIAN_POINT ( 'NONE',  ( 11.99999999999999822, -64.81221759200380461, 50.23322058963326242 ) ) ;
#28665=VERTEX_POINT ( 'NONE', #34055 ) ;
#28667=FACE_OUTER_BOUND ( 'NONE', #48232, .T. ) ;
#28669=FACE_OUTER_BOUND ( 'NONE', #8439, .T. ) ;
#28673=CIRCLE ( 'NONE', #4430, 77.49899999999999523 ) ;
#28682=ADVANCED_FACE ( 'NONE', ( #45311 ), #11789, .T. ) ;
#28689=ORIENTED_EDGE ( 'NONE', *, *, #10868, .T. ) ;
#28697=CARTESIAN_POINT ( 'NONE',  ( 0.000000000000000000, 72.35160999960844208, -20.41045688087747223 ) ) ;
#28699=ORIENTED_EDGE ( 'NONE', *, *, #33866, .F. ) ;
#28702=VERTEX_POINT ( 'NONE', #33222 ) ;
#28704=CYLINDRICAL_SURFACE ( 'NONE', #24699, 82.00000000000000000 ) ;
#28706=CYLINDRICAL_SURFACE ( 'NONE', #307, 77.49899999999999523 ) ;
#28707=FACE_OUTER_BOUND ( 'NONE', #1550, .T. ) ;
#28710=DIRECTION ( 'NONE',  ( -1.000000000000000000, -0.000000000000000000, -0.000000000000000000 ) ) ;
#28712=PLANE ( 'NONE',  #47008 ) ;
#28717=DIRECTION ( 'NONE',  ( -1.000000000000000000, 0.000000000000000000, 0.000000000000000000 ) ) ;
#28723=VERTEX_POINT ( 'NONE', #48149 ) ;
#28724=DIRECTION ( 'NONE',  ( -1.000000000000000000, -0.000000000000000000, -0.000000000000000000 ) ) ;
#28725=AXIS2_PLACEMENT_3D ( 'NONE', #22807, #33811, #44598 ) ;
#28728=CARTESIAN_POINT ( 'NONE',  ( 11.99999999999999822, 0.000000000000000000, 0.000000000000000000 ) ) ;
#28743=VERTEX_POINT ( 'NONE', #24245 ) ;
#28745=DIRECTION ( 'NONE',  ( -1.000000000000000000, -0.000000000000000000, -0.000000000000000000 ) ) ;
#28749=EDGE_CURVE ( 'NONE', #22296, #38875, #27946, .T. ) ;
#28751=ORIENTED_EDGE ( 'NONE', *, *, #15469, .F. ) ;
#28757=DIRECTION ( 'NONE',  ( 0.000000000000000000, 0.000000000000000000, 1.000000000000000000 ) ) ;
#28760=FACE_OUTER_BOUND ( 'NONE', #15407, .T. ) ;
#28762=FACE_OUTER_BOUND ( 'NONE', #15019, .T. ) ;
#28767=ORIENTED_EDGE ( 'NONE', *, *, #27098, .T. ) ;
#28769=FACE_OUTER_BOUND ( 'NONE', #8340, .T. ) ;
#28774=DIRECTION ( 'NONE',  ( -0.000000000000000000, 0.9781476007338067991, 0.2079116908177533474 ) ) ;
#28778=AXIS2_PLACEMENT_3D ( 'NONE', #33101, #48033, #15960 ) ;
#28780=CARTESIAN_POINT ( 'NONE',  ( 12.00000000000000000, -19.89357724625003598, -12.59942793731059041 ) ) ;
#28781=ORIENTED_EDGE ( 'NONE', *, *, #45056, .F. ) ;
#28784=EDGE_CURVE ( 'NONE', #25492, #22951, #7025, .T. ) ;
#28785=ORIENTED_EDGE ( 'NONE', *, *, #28301, .T. ) ;
#28786=EDGE_CURVE ( 'NONE', #32136, #39596, #131, .T. ) ;
#28790=CIRCLE ( 'NONE', #20193, 77.49899999999999523 ) ;
#28798=ORIENTED_EDGE ( 'NONE', *, *, #16573, .F. ) ;
#28804=VERTEX_POINT ( 'NONE', #47431 ) ;
#28807=DIRECTION ( 'NONE',  ( -1.000000000000000000, -0.000000000000000000, 0.000000000000000000 ) ) ;
#28808=VERTEX_POINT ( 'NONE', #28821 ) ;
#28809=CARTESIAN_POINT ( 'NONE',  ( 11.99999999999999822, 12.93880638057426502, -76.41127070299258150 ) ) ;
#28811=LINE ( 'NONE', #32491, #11231 ) ;
#28821=CARTESIAN_POINT ( 'NONE',  ( 11.99999999999999822, -80.55351364060578589, -15.33399622253569383 ) ) ;
#28823=LINE ( 'NONE', #17084, #38531 ) ;
#28827=CARTESIAN_POINT ( 'NONE',  ( 11.99999999999999822, 6.903761155838878061, -77.19088730480517313 ) ) ;
#28829=CARTESIAN_POINT ( 'NONE',  ( -10.00000000000000000, 0.000000000000000000, 0.000000000000000000 ) ) ;
#28835=CIRCLE ( 'NONE', #31978, 77.49899999999999523 ) ;
#28837=CARTESIAN_POINT ( 'NONE',  ( 11.99999999999999822, 55.38113227695858143, -54.21277698773617715 ) ) ;
#28840=AXIS2_PLACEMENT_3D ( 'NONE', #10866, #26284, #7673 ) ;
#28845=ORIENTED_EDGE ( 'NONE', *, *, #41012, .F. ) ;
#28855=DIRECTION ( 'NONE',  ( -1.000000000000000000, 0.000000000000000000, 0.000000000000000000 ) ) ;
#28857=DIRECTION ( 'NONE',  ( 0.000000000000000000, 0.000000000000000000, 1.000000000000000000 ) ) ;
#28860=DIRECTION ( 'NONE',  ( 1.000000000000000000, 0.000000000000000000, 0.000000000000000000 ) ) ;
#28862=VECTOR ( 'NONE', #3565, 1000.000000000000000 ) ;
#28869=DIRECTION ( 'NONE',  ( -1.000000000000000000, 0.000000000000000000, 0.000000000000000000 ) ) ;
#28872=CARTESIAN_POINT ( 'NONE',  ( 0.000000000000000000, 74.74816331893430288, 33.71516098798768724 ) ) ;
#28873=CARTESIAN_POINT ( 'NONE',  ( 11.99999999999999822, 0.000000000000000000, 0.000000000000000000 ) ) ;
#28884=CARTESIAN_POINT ( 'NONE',  ( 0.000000000000000000, -50.95692526931372157, 58.39081064771733054 ) ) ;
#28887=LINE ( 'NONE', #39697, #45587 ) ;
#28890=ORIENTED_EDGE ( 'NONE', *, *, #47138, .F. ) ;
#28892=EDGE_CURVE ( 'NONE', #13449, #30895, #11451, .T. ) ;
#28898=AXIS2_PLACEMENT_3D ( 'NONE', #119, #37573, #41492 ) ;
#28901=CIRCLE ( 'NONE', #33700, 31.99999999999998579 ) ;
#28904=CIRCLE ( 'NONE', #35160, 82.00000000000000000 ) ;
#28908=ORIENTED_EDGE ( 'NONE', *, *, #42116, .T. ) ;
#28909=CARTESIAN_POINT ( 'NONE',  ( 11.99999999999999822, 39.78640506895604290, 66.50666863322015843 ) ) ;
#28912=CARTESIAN_POINT ( 'NONE',  ( 15.00000000000000000, -22.67460108101782978, -6.353146135317906840 ) ) ;
#28920=ORIENTED_EDGE ( 'NONE', *, *, #32325, .T. ) ;
#28927=EDGE_LOOP ( 'NONE', ( #632, #48234, #18504, #42940 ) ) ;
#28932=EDGE_CURVE ( 'NONE', #12123, #40106, #158, .T. ) ;
#28933=CARTESIAN_POINT ( 'NONE',  ( 15.00000000000000000, -1.278221433540507546, -26.51162292216071492 ) ) ;
#28942=DIRECTION ( 'NONE',  ( -1.000000000000000000, -0.000000000000000000, 0.000000000000000000 ) ) ;
#28947=CIRCLE ( 'NONE', #24270, 31.99999999999997868 ) ;
#28950=DIRECTION ( 'NONE',  ( -1.000000000000000000, 0.000000000000000000, 0.000000000000000000 ) ) ;
#28956=DIRECTION ( 'NONE',  ( 0.000000000000000000, 0.000000000000000000, 1.000000000000000000 ) ) ;
#28971=CARTESIAN_POINT ( 'NONE',  ( 11.99999999999999822, 74.65491531819118620, -8.830959090342659579 ) ) ;
#28980=ORIENTED_EDGE ( 'NONE', *, *, #11617, .T. ) ;
#28989=LINE ( 'NONE', #32440, #31314 ) ;
#29001=AXIS2_PLACEMENT_3D ( 'NONE', #9369, #24306, #9604 ) ;
#29005=EDGE_LOOP ( 'NONE', ( #30375, #2537, #31763, #31265 ) ) ;
#29006=EDGE_CURVE ( 'NONE', #45331, #43377, #45935, .T. ) ;
#29008=CIRCLE ( 'NONE', #12595, 77.49899999999999523 ) ;
#29009=VECTOR ( 'NONE', #16343, 1000.000000000000000 ) ;
#29010=CARTESIAN_POINT ( 'NONE',  ( 0.000000000000000000, -36.73666225445940370, 65.58780272294062286 ) ) ;
#29015=AXIS2_PLACEMENT_3D ( 'NONE', #27943, #46533, #27445 ) ;
#29020=ORIENTED_EDGE ( 'NONE', *, *, #14032, .T. ) ;
#29027=EDGE_LOOP ( 'NONE', ( #27006, #13102, #44796, #3954 ) ) ;
#29031=ORIENTED_EDGE ( 'NONE', *, *, #37952, .F. ) ;
#29033=CARTESIAN_POINT ( 'NONE',  ( 15.00000000000000000, -22.32062822937489344, -14.36278369418800160 ) ) ;
#29035=ADVANCED_FACE ( 'NONE', ( #23896 ), #16798, .T. ) ;
#29037=ORIENTED_EDGE ( 'NONE', *, *, #41565, .T. ) ;
#29038=VECTOR ( 'NONE', #37939, 1000.000000000000000 ) ;
#29043=AXIS2_PLACEMENT_3D ( 'NONE', #44089, #40908, #47994 ) ;
#29044=DIRECTION ( 'NONE',  ( -1.000000000000000000, 0.000000000000000000, 0.000000000000000000 ) ) ;
#29050=CARTESIAN_POINT ( 'NONE',  ( 0.000000000000000000, -77.49459641780886443, 0.8261519478428549501 ) ) ;
#29051=DIRECTION ( 'NONE',  ( -1.000000000000000000, 0.000000000000000000, 0.000000000000000000 ) ) ;
#29058=EDGE_CURVE ( 'NONE', #2304, #5392, #2108, .T. ) ;
#29062=DIRECTION ( 'NONE',  ( 0.000000000000000000, 0.000000000000000000, 1.000000000000000000 ) ) ;
#29065=LINE ( 'NONE', #14387, #44364 ) ;
#29068=CARTESIAN_POINT ( 'NONE',  ( 11.99999999999999822, 46.21855187248630870, 62.20884554314035597 ) ) ;
#29078=DIRECTION ( 'NONE',  ( -1.000000000000000000, 0.000000000000000000, -0.000000000000000000 ) ) ;
#29080=ORIENTED_EDGE ( 'NONE', *, *, #16214, .F. ) ;
#29083=VECTOR ( 'NONE', #39883, 1000.000000000000000 ) ;
#29086=EDGE_CURVE ( 'NONE', #26821, #15059, #23618, .T. ) ;
#29087=EDGE_CURVE ( 'NONE', #11520, #4178, #47824, .T. ) ;
#29092=DIRECTION ( 'NONE',  ( -1.000000000000000000, -0.000000000000000000, -0.000000000000000000 ) ) ;
#29096=ORIENTED_EDGE ( 'NONE', *, *, #31085, .F. ) ;
#29098=CARTESIAN_POINT ( 'NONE',  ( 11.99999999999999822, -34.94270380257585629, -74.18225833017926618 ) ) ;
#29099=CARTESIAN_POINT ( 'NONE',  ( 11.99999999999999822, -74.65491531819111515, -8.830959090343204920 ) ) ;
#29108=CARTESIAN_POINT ( 'NONE',  ( 0.000000000000000000, -81.96053171279901051, -2.543863470249259962 ) ) ;
#29109=CARTESIAN_POINT ( 'NONE',  ( 11.99999999999999822, 55.20638768913831029, -51.02545421589267960 ) ) ;
#29110=FACE_OUTER_BOUND ( 'NONE', #45708, .T. ) ;
#29114=CARTESIAN_POINT ( 'NONE',  ( 11.99999999999999822, 0.000000000000000000, 0.000000000000000000 ) ) ;
#29119=CARTESIAN_POINT ( 'NONE',  ( 11.99999999999999822, 0.000000000000000000, 0.000000000000000000 ) ) ;
#29128=CIRCLE ( 'NONE', #17426, 82.00000000000000000 ) ;
#29129=CYLINDRICAL_SURFACE ( 'NONE', #4235, 77.49899999999999523 ) ;
#29132=AXIS2_PLACEMENT_3D ( 'NONE', #39171, #35740, #27681 ) ;
#29137=CARTESIAN_POINT ( 'NONE',  ( -10.00000000000000000, 0.000000000000000000, 0.000000000000000000 ) ) ;
#29142=DIRECTION ( 'NONE',  ( -1.000000000000000000, 0.000000000000000000, 0.000000000000000000 ) ) ;
#29143=AXIS2_PLACEMENT_3D ( 'NONE', #38776, #4507, #18925 ) ;
#29144=LINE ( 'NONE', #17402, #10210 ) ;
#29153=DIRECTION ( 'NONE',  ( 0.000000000000000000, 0.000000000000000000, -1.000000000000000000 ) ) ;
#29157=VERTEX_POINT ( 'NONE', #47832 ) ;
#29158=DIRECTION ( 'NONE',  ( 0.000000000000000000, 0.000000000000000000, 1.000000000000000000 ) ) ;
#29159=ORIENTED_EDGE ( 'NONE', *, *, #2164, .F. ) ;
#29162=CARTESIAN_POINT ( 'NONE',  ( 11.99999999999999822, -73.72996012237449293, 14.67089635893687571 ) ) ;
#29165=DIRECTION ( 'NONE',  ( 0.000000000000000000, 0.5224985647159500202, -0.8526401643540915121 ) ) ;
#29168=CIRCLE ( 'NONE', #6502, 82.00000000000000000 ) ;
#29170=DIRECTION ( 'NONE',  ( 0.000000000000000000, 0.000000000000000000, 1.000000000000000000 ) ) ;
#29174=AXIS2_PLACEMENT_3D ( 'NONE', #24688, #2629, #17571 ) ;
#29176=CARTESIAN_POINT ( 'NONE',  ( 0.000000000000000000, -0.8261519478425841667, -77.49459641780886443 ) ) ;
#29177=CYLINDRICAL_SURFACE ( 'NONE', #6681, 82.00000000000000000 ) ;
#29184=AXIS2_PLACEMENT_3D ( 'NONE', #30746, #22666, #23154 ) ;
#29187=DIRECTION ( 'NONE',  ( 0.000000000000000000, 0.5224985647159500202, -0.8526401643540915121 ) ) ;
#29191=VERTEX_POINT ( 'NONE', #36587 ) ;
#29193=VECTOR ( 'NONE', #41677, 1000.000000000000000 ) ;
#29198=LINE ( 'NONE', #40231, #13528 ) ;
#29203=CIRCLE ( 'NONE', #3402, 31.99999999999999289 ) ;
#29204=EDGE_LOOP ( 'NONE', ( #38667, #13806, #12947, #3761 ) ) ;
#29217=CIRCLE ( 'NONE', #7343, 82.00000000000000000 ) ;
#29220=DIRECTION ( 'NONE',  ( 1.000000000000000000, 0.000000000000000000, 0.000000000000000000 ) ) ;
#29226=ORIENTED_EDGE ( 'NONE', *, *, #17169, .F. ) ;
#29227=AXIS2_PLACEMENT_3D ( 'NONE', #46191, #12667, #37217 ) ;
#29229=ORIENTED_EDGE ( 'NONE', *, *, #40556, .F. ) ;
#29231=ORIENTED_EDGE ( 'NONE', *, *, #7328, .F. ) ;
#29235=CIRCLE ( 'NONE', #32279, 82.00000000000000000 ) ;
#29239=ORIENTED_EDGE ( 'NONE', *, *, #30351, .T. ) ;
#29241=CIRCLE ( 'NONE', #11255, 77.49899999999999523 ) ;
#29246=DIRECTION ( 'NONE',  ( 0.000000000000000000, 0.7071067811865487940, -0.7071067811865462405 ) ) ;
#29253=EDGE_CURVE ( 'NONE', #5920, #25033, #44659, .T. ) ;
#29256=CARTESIAN_POINT ( 'NONE',  ( 11.99999999999999822, 0.000000000000000000, 0.000000000000000000 ) ) ;
#29262=LINE ( 'NONE', #47606, #11943 ) ;
#29265=AXIS2_PLACEMENT_3D ( 'NONE', #32001, #27854, #46689 ) ;
#29271=DIRECTION ( 'NONE',  ( 0.000000000000000000, 0.000000000000000000, 1.000000000000000000 ) ) ;
#29284=EDGE_CURVE ( 'NONE', #17996, #14039, #46271, .T. ) ;
#29285=ORIENTED_EDGE ( 'NONE', *, *, #11947, .F. ) ;
#29288=CIRCLE ( 'NONE', #18345, 77.49900000000000944 ) ;
#29290=ORIENTED_EDGE ( 'NONE', *, *, #41607, .T. ) ;
#29292=ORIENTED_EDGE ( 'NONE', *, *, #15605, .T. ) ;
#29293=LINE ( 'NONE', #43973, #5242 ) ;
#29294=ORIENTED_EDGE ( 'NONE', *, *, #16163, .F. ) ;
#29300=DIRECTION ( 'NONE',  ( 0.000000000000000000, 0.000000000000000000, -1.000000000000000000 ) ) ;
#29303=EDGE_CURVE ( 'NONE', #3648, #17321, #41594, .T. ) ;
#29304=ADVANCED_FACE ( 'NONE', ( #23114 ), #30227, .T. ) ;
#29310=ADVANCED_FACE ( 'NONE', ( #15527 ), #11133, .T. ) ;
#29311=CARTESIAN_POINT ( 'NONE',  ( 11.99999999999999822, 0.000000000000000000, 0.000000000000000000 ) ) ;
#29312=CIRCLE ( 'NONE', #369, 31.99999999999998934 ) ;
#29313=DIRECTION ( 'NONE',  ( 0.000000000000000000, 0.000000000000000000, 1.000000000000000000 ) ) ;
#29319=EDGE_CURVE ( 'NONE', #42347, #46621, #7210, .T. ) ;
#29320=ORIENTED_EDGE ( 'NONE', *, *, #42243, .T. ) ;
#29324=CYLINDRICAL_SURFACE ( 'NONE', #27690, 31.99999999999998579 ) ;
#29341=ADVANCED_FACE ( 'NONE', ( #19419 ), #41477, .T. ) ;
#29342=CIRCLE ( 'NONE', #15273, 31.99999999999998934 ) ;
#29350=VECTOR ( 'NONE', #39134, 1000.000000000000227 ) ;
#29352=CARTESIAN_POINT ( 'NONE',  ( 0.000000000000000000, 0.000000000000000000, 0.000000000000000000 ) ) ;
#29357=CARTESIAN_POINT ( 'NONE',  ( 11.99999999999999822, -80.28980883073769803, 16.65972982744905551 ) ) ;
#29361=DIRECTION ( 'NONE',  ( -1.000000000000000000, -0.000000000000000000, -0.000000000000000000 ) ) ;
#29363=ORIENTED_EDGE ( 'NONE', *, *, #9402, .T. ) ;
#29364=CARTESIAN_POINT ( 'NONE',  ( 12.00000000000000000, -22.67460108101774452, 6.353146135318220367 ) ) ;
#29370=ADVANCED_FACE ( 'NONE', ( #22395 ), #11618, .T. ) ;
#29372=DIRECTION ( 'NONE',  ( -1.000000000000000000, 0.000000000000000000, 0.000000000000000000 ) ) ;
#29374=CIRCLE ( 'NONE', #19205, 31.99999999999998934 ) ;
#29375=DIRECTION ( 'NONE',  ( -1.000000000000000000, 0.000000000000000000, -0.000000000000000000 ) ) ;
#29379=FACE_OUTER_BOUND ( 'NONE', #27671, .T. ) ;
#29384=DIRECTION ( 'NONE',  ( 1.000000000000000000, -0.000000000000000000, -0.000000000000000000 ) ) ;
#29386=CIRCLE ( 'NONE', #10630, 82.00000000000000000 ) ;
#29391=AXIS2_PLACEMENT_3D ( 'NONE', #30892, #15701, #34529 ) ;
#29395=ORIENTED_EDGE ( 'NONE', *, *, #39871, .F. ) ;
#29400=CIRCLE ( 'NONE', #24720, 77.49899999999999523 ) ;
#29401=ORIENTED_EDGE ( 'NONE', *, *, #24875, .F. ) ;
#29406=VERTEX_POINT ( 'NONE', #38784 ) ;
#29410=DIRECTION ( 'NONE',  ( -1.000000000000000000, 0.000000000000000000, 0.000000000000000000 ) ) ;
#29412=ORIENTED_EDGE ( 'NONE', *, *, #12912, .T. ) ;
#29414=LINE ( 'NONE', #34035, #18485 ) ;
#29415=CARTESIAN_POINT ( 'NONE',  ( 0.000000000000000000, 68.26794271651307611, -31.47745569255064169 ) ) ;
#29420=ORIENTED_EDGE ( 'NONE', *, *, #38855, .F. ) ;
#29429=ORIENTED_EDGE ( 'NONE', *, *, #16227, .T. ) ;
#29431=LINE ( 'NONE', #33086, #30453 ) ;
#29435=CYLINDRICAL_SURFACE ( 'NONE', #17604, 31.99999999999998579 ) ;
#29440=FACE_OUTER_BOUND ( 'NONE', #9836, .T. ) ;
#29449=CARTESIAN_POINT ( 'NONE',  ( 15.00000000000000000, -22.67460108101774452, 6.353146135318220367 ) ) ;
#29453=DIRECTION ( 'NONE',  ( -1.000000000000000000, 0.000000000000000000, 0.000000000000000000 ) ) ;
#29456=AXIS2_PLACEMENT_3D ( 'NONE', #18284, #14141, #6803 ) ;
#29459=EDGE_CURVE ( 'NONE', #5623, #23602, #14269, .T. ) ;
#29462=VERTEX_POINT ( 'NONE', #27766 ) ;
#29466=CARTESIAN_POINT ( 'NONE',  ( -10.00000000000000000, 0.000000000000000000, 0.000000000000000000 ) ) ;
#29467=DIRECTION ( 'NONE',  ( 0.000000000000000000, 0.000000000000000000, -1.000000000000000000 ) ) ;
#29469=CIRCLE ( 'NONE', #8375, 77.49899999999998101 ) ;
#29478=CARTESIAN_POINT ( 'NONE',  ( 11.99999999999999822, 0.000000000000000000, 0.000000000000000000 ) ) ;
#29483=DIRECTION ( 'NONE',  ( 0.000000000000000000, 0.000000000000000000, 1.000000000000000000 ) ) ;
#29488=DIRECTION ( 'NONE',  ( -1.000000000000000000, -0.000000000000000000, -0.000000000000000000 ) ) ;
#29491=DIRECTION ( 'NONE',  ( 0.000000000000000000, 0.000000000000000000, 1.000000000000000000 ) ) ;
#29497=LINE ( 'NONE', #47603, #18277 ) ;
#29498=FACE_OUTER_BOUND ( 'NONE', #33217, .T. ) ;
#29508=AXIS2_PLACEMENT_3D ( 'NONE', #11454, #41784, #8480 ) ;
#29513=EDGE_CURVE ( 'NONE', #17937, #27340, #42191, .T. ) ;
#29524=DIRECTION ( 'NONE',  ( -1.000000000000000000, 0.000000000000000000, -0.000000000000000000 ) ) ;
#29527=AXIS2_PLACEMENT_3D ( 'NONE', #13482, #24749, #47261 ) ;
#29532=ORIENTED_EDGE ( 'NONE', *, *, #21868, .F. ) ;
#29535=CARTESIAN_POINT ( 'NONE',  ( 15.00000000000000000, -3.948201729842355068, -23.21447184625292692 ) ) ;
#29538=DIRECTION ( 'NONE',  ( -1.000000000000000000, 0.000000000000000000, -0.000000000000000000 ) ) ;
#29541=LINE ( 'NONE', #48380, #44670 ) ;
#29542=VECTOR ( 'NONE', #402, 1000.000000000000000 ) ;
#29549=CARTESIAN_POINT ( 'NONE',  ( 0.000000000000000000, 0.000000000000000000, 0.000000000000000000 ) ) ;
#29551=CARTESIAN_POINT ( 'NONE',  ( 0.000000000000000000, -35.91791733033525702, 68.67312586194982771 ) ) ;
#29555=DIRECTION ( 'NONE',  ( 0.000000000000000000, 0.000000000000000000, 1.000000000000000000 ) ) ;
#29563=AXIS2_PLACEMENT_3D ( 'NONE', #19314, #4635, #19538 ) ;
#29567=VERTEX_POINT ( 'NONE', #9615 ) ;
#29573=ORIENTED_EDGE ( 'NONE', *, *, #41782, .T. ) ;
#29579=LINE ( 'NONE', #32999, #27043 ) ;
#29585=EDGE_LOOP ( 'NONE', ( #7319, #46969, #28121, #43626 ) ) ;
#29586=VERTEX_POINT ( 'NONE', #36534 ) ;
#29588=CARTESIAN_POINT ( 'NONE',  ( 0.000000000000000000, 0.000000000000000000, 0.000000000000000000 ) ) ;
#29592=CARTESIAN_POINT ( 'NONE',  ( 0.000000000000000000, 0.000000000000000000, 0.000000000000000000 ) ) ;
#29593=CARTESIAN_POINT ( 'NONE',  ( 0.000000000000000000, 0.000000000000000000, 0.000000000000000000 ) ) ;
#29615=EDGE_CURVE ( 'NONE', #2609, #24762, #16973, .T. ) ;
#29618=VERTEX_POINT ( 'NONE', #31930 ) ;
#29625=ORIENTED_EDGE ( 'NONE', *, *, #41282, .T. ) ;
#29630=AXIS2_PLACEMENT_3D ( 'NONE', #11062, #18407, #48264 ) ;
#29634=ORIENTED_EDGE ( 'NONE', *, *, #14032, .F. ) ;
#29636=VERTEX_POINT ( 'NONE', #39746 ) ;
#29638=LINE ( 'NONE', #28909, #5108 ) ;
#29640=ORIENTED_EDGE ( 'NONE', *, *, #9005, .T. ) ;
#29645=DIRECTION ( 'NONE',  ( 1.000000000000000000, 0.000000000000000000, 0.000000000000000000 ) ) ;
#29661=CARTESIAN_POINT ( 'NONE',  ( 12.00000000000000355, 0.000000000000000000, 0.000000000000000000 ) ) ;
#29667=ADVANCED_FACE ( 'NONE', ( #14020 ), #17920, .T. ) ;
#29676=AXIS2_PLACEMENT_3D ( 'NONE', #26970, #4682, #19836 ) ;
#29677=CARTESIAN_POINT ( 'NONE',  ( 0.000000000000000000, -73.95703589263958122, -23.16143007188505010 ) ) ;
#29681=CARTESIAN_POINT ( 'NONE',  ( 11.99999999999999822, -62.20884554313985149, -46.21855187248698371 ) ) ;
#29687=DIRECTION ( 'NONE',  ( -1.000000000000000000, -0.000000000000000000, 0.000000000000000000 ) ) ;
#29689=EDGE_CURVE ( 'NONE', #28447, #1914, #21304, .T. ) ;
#29692=DIRECTION ( 'NONE',  ( -1.000000000000000000, 0.000000000000000000, 0.000000000000000000 ) ) ;
#29694=CARTESIAN_POINT ( 'NONE',  ( 11.99999999999999822, -72.35432306680498016, 20.40083707022857951 ) ) ;
#29697=CARTESIAN_POINT ( 'NONE',  ( 0.000000000000000000, -41.76106447765533147, 62.50884508063410294 ) ) ;
#29700=EDGE_CURVE ( 'NONE', #36027, #24462, #44757, .T. ) ;
#29707=DIRECTION ( 'NONE',  ( 0.000000000000000000, 0.000000000000000000, 1.000000000000000000 ) ) ;
#29709=FACE_OUTER_BOUND ( 'NONE', #17988, .T. ) ;
#29711=CARTESIAN_POINT ( 'NONE',  ( 11.99999999999999822, -63.18004540532995605, -44.88180994100445531 ) ) ;
#29713=CARTESIAN_POINT ( 'NONE',  ( 11.99999999999999822, -28.89263327155796190, 71.91182617369179297 ) ) ;
#29715=CIRCLE ( 'NONE', #10183, 31.99999999999998579 ) ;
#29716=VERTEX_POINT ( 'NONE', #33347 ) ;
#29717=CYLINDRICAL_SURFACE ( 'NONE', #19588, 82.00000000000000000 ) ;
#29720=AXIS2_PLACEMENT_3D ( 'NONE', #5395, #1726, #31602 ) ;
#29722=FACE_OUTER_BOUND ( 'NONE', #13494, .T. ) ;
#29723=DIRECTION ( 'NONE',  ( -1.000000000000000000, -0.000000000000000000, -0.000000000000000000 ) ) ;
#29729=ORIENTED_EDGE ( 'NONE', *, *, #4919, .T. ) ;
#29732=CARTESIAN_POINT ( 'NONE',  ( 11.99999999999999822, 0.000000000000000000, 0.000000000000000000 ) ) ;
#29734=CARTESIAN_POINT ( 'NONE',  ( 11.99999999999999822, -36.72794159290288718, 65.59268652807197952 ) ) ;
#29740=ORIENTED_EDGE ( 'NONE', *, *, #21864, .F. ) ;
#29741=CIRCLE ( 'NONE', #17986, 31.99999999999998224 ) ;
#29743=CIRCLE ( 'NONE', #30524, 31.99999999999998579 ) ;
#29748=CIRCLE ( 'NONE', #42266, 31.99999999999999289 ) ;
#29749=DIRECTION ( 'NONE',  ( 1.000000000000000000, -0.000000000000000000, 0.000000000000000000 ) ) ;
#29758=DIRECTION ( 'NONE',  ( -1.000000000000000000, 0.000000000000000000, 0.000000000000000000 ) ) ;
#29761=EDGE_LOOP ( 'NONE', ( #3168, #14349, #1032, #45512 ) ) ;
#29762=DIRECTION ( 'NONE',  ( 0.000000000000000000, 0.000000000000000000, 1.000000000000000000 ) ) ;
#29765=EDGE_CURVE ( 'NONE', #1817, #4301, #30688, .T. ) ;
#29767=CARTESIAN_POINT ( 'NONE',  ( 12.00000000000000000, -13.04903810567646971, 19.60159698893442481 ) ) ;
#29775=AXIS2_PLACEMENT_3D ( 'NONE', #41705, #27760, #12816 ) ;
#29778=AXIS2_PLACEMENT_3D ( 'NONE', #35896, #35169, #32241 ) ;
#29779=LINE ( 'NONE', #36405, #10855 ) ;
#29781=VECTOR ( 'NONE', #20797, 1000.000000000000000 ) ;
#29786=VECTOR ( 'NONE', #8760, 1000.000000000000000 ) ;
#29795=DIRECTION ( 'NONE',  ( -1.000000000000000000, -0.000000000000000000, 0.000000000000000000 ) ) ;
#29800=DIRECTION ( 'NONE',  ( -1.000000000000000000, 0.000000000000000000, -0.000000000000000000 ) ) ;
#29803=VECTOR ( 'NONE', #47537, 1000.000000000000114 ) ;
#29813=DIRECTION ( 'NONE',  ( 0.000000000000000000, 0.000000000000000000, 1.000000000000000000 ) ) ;
#29818=ORIENTED_EDGE ( 'NONE', *, *, #21320, .F. ) ;
#29820=CARTESIAN_POINT ( 'NONE',  ( 11.99999999999999822, -27.74655509720725277, 77.16300072079650363 ) ) ;
#29822=ADVANCED_FACE ( 'NONE', ( #37499 ), #41418, .T. ) ;
#29828=CARTESIAN_POINT ( 'NONE',  ( 11.99999999999999822, 0.000000000000000000, 0.000000000000000000 ) ) ;
#29829=EDGE_LOOP ( 'NONE', ( #26095, #3040, #41751, #37724 ) ) ;
#29831=DIRECTION ( 'NONE',  ( -1.000000000000000000, 0.000000000000000000, -0.000000000000000000 ) ) ;
#29836=CYLINDRICAL_SURFACE ( 'NONE', #524, 31.99999999999998579 ) ;
#29837=LINE ( 'NONE', #22264, #31593 ) ;
#29840=ADVANCED_FACE ( 'NONE', ( #12762 ), #35270, .F. ) ;
#29860=CARTESIAN_POINT ( 'NONE',  ( 11.99999999999999822, 0.000000000000000000, 0.000000000000000000 ) ) ;
#29862=ORIENTED_EDGE ( 'NONE', *, *, #32110, .F. ) ;
#29863=FACE_OUTER_BOUND ( 'NONE', #16526, .T. ) ;
#29866=VERTEX_POINT ( 'NONE', #31383 ) ;
#29869=DIRECTION ( 'NONE',  ( 0.000000000000000000, 0.000000000000000000, 1.000000000000000000 ) ) ;
#29872=VERTEX_POINT ( 'NONE', #16431 ) ;
#29875=ORIENTED_EDGE ( 'NONE', *, *, #41931, .F. ) ;
#29876=ADVANCED_FACE ( 'NONE', ( #31137 ), #27699, .F. ) ;
#29881=CIRCLE ( 'NONE', #7241, 31.99999999999998934 ) ;
#29884=CYLINDRICAL_SURFACE ( 'NONE', #23175, 77.49899999999999523 ) ;
#29886=CARTESIAN_POINT ( 'NONE',  ( 11.99999999999999822, 27.74655509720670210, 77.16300072079670258 ) ) ;
#29899=DIRECTION ( 'NONE',  ( 0.000000000000000000, 0.000000000000000000, -1.000000000000000000 ) ) ;
#29901=DIRECTION ( 'NONE',  ( -1.000000000000000000, 0.000000000000000000, 0.000000000000000000 ) ) ;
#29902=EDGE_CURVE ( 'NONE', #32940, #18691, #30720, .T. ) ;
#29903=DIRECTION ( 'NONE',  ( -1.000000000000000000, 0.000000000000000000, 0.000000000000000000 ) ) ;
#29908=DIRECTION ( 'NONE',  ( -1.000000000000000000, -0.000000000000000000, -0.000000000000000000 ) ) ;
#29912=CARTESIAN_POINT ( 'NONE',  ( 0.000000000000000000, 56.15606465355041621, -59.75363087400017292 ) ) ;
#29916=EDGE_LOOP ( 'NONE', ( #7003, #40931, #34615, #43915 ) ) ;
#29926=DIRECTION ( 'NONE',  ( -1.000000000000000000, 0.000000000000000000, 0.000000000000000000 ) ) ;
#29927=ORIENTED_EDGE ( 'NONE', *, *, #3190, .F. ) ;
#29929=FACE_OUTER_BOUND ( 'NONE', #24177, .T. ) ;
#29931=ORIENTED_EDGE ( 'NONE', *, *, #46418, .T. ) ;
#29932=CARTESIAN_POINT ( 'NONE',  ( 11.99999999999999822, 0.000000000000000000, 0.000000000000000000 ) ) ;
#29937=VERTEX_POINT ( 'NONE', #23055 ) ;
#29939=AXIS2_PLACEMENT_3D ( 'NONE', #8062, #22999, #25691 ) ;
#29942=CYLINDRICAL_SURFACE ( 'NONE', #43236, 82.00000000000000000 ) ;
#29943=DIRECTION ( 'NONE',  ( 0.000000000000000000, 0.000000000000000000, 1.000000000000000000 ) ) ;
#29945=FACE_OUTER_BOUND ( 'NONE', #24988, .T. ) ;
#29949=VERTEX_POINT ( 'NONE', #39191 ) ;
#29952=DIRECTION ( 'NONE',  ( -1.000000000000000000, -0.000000000000000000, -0.000000000000000000 ) ) ;
#29954=CYLINDRICAL_SURFACE ( 'NONE', #10963, 77.49899999999999523 ) ;
#29961=LINE ( 'NONE', #18211, #40827 ) ;
#29966=EDGE_CURVE ( 'NONE', #40106, #39158, #46367, .T. ) ;
#29967=PLANE ( 'NONE',  #21640 ) ;
#29969=AXIS2_PLACEMENT_3D ( 'NONE', #16688, #27716, #5431 ) ;
#29970=CARTESIAN_POINT ( 'NONE',  ( 11.99999999999999822, 0.000000000000000000, 0.000000000000000000 ) ) ;
#29971=DIRECTION ( 'NONE',  ( 1.000000000000000000, -0.000000000000000000, -0.000000000000000000 ) ) ;
#29972=CIRCLE ( 'NONE', #42485, 31.99999999999998934 ) ;
#29976=CARTESIAN_POINT ( 'NONE',  ( 11.99999999999999822, 0.000000000000000000, 0.000000000000000000 ) ) ;
#29983=VERTEX_POINT ( 'NONE', #5660 ) ;
#29988=AXIS2_PLACEMENT_3D ( 'NONE', #47415, #32956, #29300 ) ;
#29990=ORIENTED_EDGE ( 'NONE', *, *, #14591, .T. ) ;
#29993=EDGE_CURVE ( 'NONE', #13636, #19576, #231, .T. ) ;
#29996=CARTESIAN_POINT ( 'NONE',  ( 11.99999999999999822, 0.000000000000000000, 0.000000000000000000 ) ) ;
#29999=DIRECTION ( 'NONE',  ( 1.000000000000000000, -0.000000000000000000, -0.000000000000000000 ) ) ;
#30003=ORIENTED_EDGE ( 'NONE', *, *, #28474, .T. ) ;
#30004=ADVANCED_FACE ( 'NONE', ( #47709 ), #2937, .T. ) ;
#30005=ORIENTED_EDGE ( 'NONE', *, *, #17880, .F. ) ;
#30011=CARTESIAN_POINT ( 'NONE',  ( -10.00000000000000000, 0.000000000000000000, 0.000000000000000000 ) ) ;
#30015=ORIENTED_EDGE ( 'NONE', *, *, #23986, .T. ) ;
#30016=EDGE_CURVE ( 'NONE', #410, #2592, #14200, .T. ) ;
#30019=DIRECTION ( 'NONE',  ( -1.000000000000000000, -0.000000000000000000, -0.000000000000000000 ) ) ;
#30020=DIRECTION ( 'NONE',  ( 0.000000000000000000, 0.3090169943749479509, -0.9510565162951534202 ) ) ;
#30022=CARTESIAN_POINT ( 'NONE',  ( 0.000000000000000000, 73.95703589263973754, 23.16143007188452430 ) ) ;
#30026=DIRECTION ( 'NONE',  ( 1.000000000000000000, -0.000000000000000000, 0.000000000000000000 ) ) ;
#30027=ORIENTED_EDGE ( 'NONE', *, *, #12483, .F. ) ;
#30029=AXIS2_PLACEMENT_3D ( 'NONE', #36747, #10092, #25242 ) ;
#30033=VECTOR ( 'NONE', #40286, 1000.000000000000114 ) ;
#30034=CARTESIAN_POINT ( 'NONE',  ( 11.99999999999999822, 70.53064760720278059, 26.01480285779964774 ) ) ;
#30036=DIRECTION ( 'NONE',  ( -1.000000000000000000, 0.000000000000000000, 0.000000000000000000 ) ) ;
#30046=DIRECTION ( 'NONE',  ( -1.000000000000000000, -0.000000000000000000, -0.000000000000000000 ) ) ;
#30048=VECTOR ( 'NONE', #23162, 1000.000000000000000 ) ;
#30049=VERTEX_POINT ( 'NONE', #39438 ) ;
#30051=EDGE_CURVE ( 'NONE', #21369, #410, #10043, .T. ) ;
#30056=CARTESIAN_POINT ( 'NONE',  ( 11.99999999999999822, 62.50884508063487033, -41.76106447765422303 ) ) ;
#30059=AXIS2_PLACEMENT_3D ( 'NONE', #14188, #17364, #18084 ) ;
#30063=VERTEX_POINT ( 'NONE', #24494 ) ;
#30064=VERTEX_POINT ( 'NONE', #2689 ) ;
#30067=EDGE_CURVE ( 'NONE', #15931, #30390, #19763, .T. ) ;
#30084=ORIENTED_EDGE ( 'NONE', *, *, #43604, .T. ) ;
#30096=DIRECTION ( 'NONE',  ( -1.000000000000000000, -0.000000000000000000, 0.000000000000000000 ) ) ;
#30107=( NAMED_UNIT ( * ) PLANE_ANGLE_UNIT ( ) SI_UNIT ( $, .RADIAN. ) );
#30109=EDGE_CURVE ( 'NONE', #127, #20106, #31545, .T. ) ;
#30111=ADVANCED_FACE ( 'NONE', ( #33283 ), #18351, .T. ) ;
#30113=AXIS2_PLACEMENT_3D ( 'NONE', #15056, #18225, #26064 ) ;
#30114=UNCERTAINTY_MEASURE_WITH_UNIT (LENGTH_MEASURE( 1.000000000000000082E-05 ), #4857, 'distance_accuracy_value', 'NONE');
#30116=EDGE_CURVE ( 'NONE', #188, #18133, #22514, .T. ) ;
#30117=CIRCLE ( 'NONE', #14499, 77.49900000000002365 ) ;
#30119=DIRECTION ( 'NONE',  ( 0.000000000000000000, 0.4539904997395413089, 0.8910065241883705633 ) ) ;
#30121=CIRCLE ( 'NONE', #26199, 77.49900000000002365 ) ;
#30122=ORIENTED_EDGE ( 'NONE', *, *, #16262, .T. ) ;
#30123=CIRCLE ( 'NONE', #30163, 77.49899999999999523 ) ;
#30133=EDGE_CURVE ( 'NONE', #4884, #30895, #11998, .T. ) ;
#30137=VERTEX_POINT ( 'NONE', #25931 ) ;
#30140=DIRECTION ( 'NONE',  ( 0.000000000000000000, -0.5877852522924787992, -0.8090169943749434545 ) ) ;
#30143=ORIENTED_EDGE ( 'NONE', *, *, #36362, .F. ) ;
#30144=DIRECTION ( 'NONE',  ( 0.000000000000000000, -0.9510565162951565288, 0.3090169943749382919 ) ) ;
#30145=CARTESIAN_POINT ( 'NONE',  ( 11.99999999999999822, 8.840884882376133902, -74.65374052328640175 ) ) ;
#30146=VERTEX_POINT ( 'NONE', #40399 ) ;
#30151=VECTOR ( 'NONE', #11102, 1000.000000000000000 ) ;
#30160=CARTESIAN_POINT ( 'NONE',  ( -10.00000000000000000, 0.000000000000000000, 0.000000000000000000 ) ) ;
#30163=AXIS2_PLACEMENT_3D ( 'NONE', #10254, #17833, #14667 ) ;
#30173=CARTESIAN_POINT ( 'NONE',  ( 6.000000000000000000, -71.21200624218825226, 40.65526001592589722 ) ) ;
#30175=AXIS2_PLACEMENT_3D ( 'NONE', #25321, #17976, #17751 ) ;
#30186=AXIS2_PLACEMENT_3D ( 'NONE', #12638, #2331, #31977 ) ;
#30188=ORIENTED_EDGE ( 'NONE', *, *, #32695, .F. ) ;
#30189=AXIS2_PLACEMENT_3D ( 'NONE', #10014, #39881, #2421 ) ;
#30190=DIRECTION ( 'NONE',  ( 0.000000000000000000, 0.000000000000000000, 1.000000000000000000 ) ) ;
#30193=CIRCLE ( 'NONE', #32424, 82.00000000000000000 ) ;
#30194=EDGE_CURVE ( 'NONE', #7173, #30536, #7333, .T. ) ;
#30195=EDGE_CURVE ( 'NONE', #5128, #21831, #18229, .T. ) ;
#30199=CARTESIAN_POINT ( 'NONE',  ( 11.99999999999999822, 65.64334221924909230, 41.19522573413756561 ) ) ;
#30201=VECTOR ( 'NONE', #4688, 1000.000000000000000 ) ;
#30202=VECTOR ( 'NONE', #39949, 1000.000000000000000 ) ;
#30205=DIRECTION ( 'NONE',  ( -1.000000000000000000, -0.000000000000000000, 0.000000000000000000 ) ) ;
#30216=CARTESIAN_POINT ( 'NONE',  ( 6.000000000000000000, -80.28980883073769803, 16.65972982744905551 ) ) ;
#30219=DIRECTION ( 'NONE',  ( -1.000000000000000000, -0.000000000000000000, -0.000000000000000000 ) ) ;
#30223=CARTESIAN_POINT ( 'NONE',  ( 5.999999999999999112, 27.74655509720779989, -77.16300072079631889 ) ) ;
#30227=CYLINDRICAL_SURFACE ( 'NONE', #30653, 77.49899999999999523 ) ;
#30241=ORIENTED_EDGE ( 'NONE', *, *, #11341, .F. ) ;
#30247=EDGE_CURVE ( 'NONE', #20016, #7287, #47173, .T. ) ;
#30248=VECTOR ( 'NONE', #37109, 1000.000000000000114 ) ;
#30249=DIRECTION ( 'NONE',  ( -1.000000000000000000, 0.000000000000000000, 0.000000000000000000 ) ) ;
#30254=CIRCLE ( 'NONE', #16176, 77.49900000000000944 ) ;
#30255=DIRECTION ( 'NONE',  ( -1.000000000000000000, 0.000000000000000000, 0.000000000000000000 ) ) ;
#30257=ORIENTED_EDGE ( 'NONE', *, *, #45335, .F. ) ;
#30266=CIRCLE ( 'NONE', #9925, 31.99999999999998224 ) ;
#30268=CARTESIAN_POINT ( 'NONE',  ( 15.00000000000000000, 20.85821328998756385, 10.92862929874494249 ) ) ;
#30270=DIRECTION ( 'NONE',  ( -1.000000000000000000, 0.000000000000000000, -0.000000000000000000 ) ) ;
#30274=DIRECTION ( 'NONE',  ( 0.000000000000000000, 0.000000000000000000, 1.000000000000000000 ) ) ;
#30276=CIRCLE ( 'NONE', #20093, 82.00000000000000000 ) ;
#30277=CARTESIAN_POINT ( 'NONE',  ( 0.000000000000000000, 0.000000000000000000, 0.000000000000000000 ) ) ;
#30278=CARTESIAN_POINT ( 'NONE',  ( 11.99999999999999822, 12.93880638057315657, 76.41127070299278046 ) ) ;
#30283=ORIENTED_EDGE ( 'NONE', *, *, #9252, .F. ) ;
#30287=CARTESIAN_POINT ( 'NONE',  ( 11.99999999999999822, 0.000000000000000000, 0.000000000000000000 ) ) ;
#30293=DIRECTION ( 'NONE',  ( -1.000000000000000000, -0.000000000000000000, -0.000000000000000000 ) ) ;
#30296=EDGE_CURVE ( 'NONE', #17963, #26344, #35432, .T. ) ;
#30303=AXIS2_PLACEMENT_3D ( 'NONE', #11327, #26249, #26487 ) ;
#30307=CARTESIAN_POINT ( 'NONE',  ( 6.000000000000000000, 76.69515212746057387, -29.01471420065479379 ) ) ;
#30308=DIRECTION ( 'NONE',  ( -1.000000000000000000, 0.000000000000000000, -0.000000000000000000 ) ) ;
#30313=ORIENTED_EDGE ( 'NONE', *, *, #24823, .F. ) ;
#30319=DIRECTION ( 'NONE',  ( -0.000000000000000000, -0.9135454576426006446, 0.4067366430758008744 ) ) ;
#30320=ORIENTED_EDGE ( 'NONE', *, *, #1225, .T. ) ;
#30323=AXIS2_PLACEMENT_3D ( 'NONE', #45234, #26629, #39335 ) ;
#30327=ORIENTED_EDGE ( 'NONE', *, *, #26628, .F. ) ;
#30331=ORIENTED_EDGE ( 'NONE', *, *, #22154, .T. ) ;
#30332=EDGE_LOOP ( 'NONE', ( #19273, #21637, #152, #34758 ) ) ;
#30335=DIRECTION ( 'NONE',  ( -1.000000000000000000, 0.000000000000000000, -0.000000000000000000 ) ) ;
#30343=CIRCLE ( 'NONE', #42079, 31.99999999999998579 ) ;
#30346=CARTESIAN_POINT ( 'NONE',  ( 11.99999999999999822, 0.000000000000000000, 0.000000000000000000 ) ) ;
#30349=CARTESIAN_POINT ( 'NONE',  ( 11.99999999999999822, -68.26794271651239399, -31.47745569255214093 ) ) ;
#30350=CYLINDRICAL_SURFACE ( 'NONE', #408, 31.99999999999998579 ) ;
#30351=EDGE_CURVE ( 'NONE', #28723, #39648, #42574, .T. ) ;
#30352=FILL_AREA_STYLE_COLOUR ( '', #40569 ) ;
#30354=ORIENTED_EDGE ( 'NONE', *, *, #4953, .T. ) ;
#30356=DIRECTION ( 'NONE',  ( 0.000000000000000000, -0.9876883405951394357, 0.1564344650402205716 ) ) ;
#30362=AXIS2_PLACEMENT_3D ( 'NONE', #36852, #35895, #14355 ) ;
#30363=ORIENTED_EDGE ( 'NONE', *, *, #1973, .T. ) ;
#30365=CARTESIAN_POINT ( 'NONE',  ( 11.99999999999999822, 0.000000000000000000, 0.000000000000000000 ) ) ;
#30367=ORIENTED_EDGE ( 'NONE', *, *, #351, .T. ) ;
#30370=ORIENTED_EDGE ( 'NONE', *, *, #48028, .T. ) ;
#30375=ORIENTED_EDGE ( 'NONE', *, *, #7687, .F. ) ;
#30376=VERTEX_POINT ( 'NONE', #46488 ) ;
#30378=EDGE_LOOP ( 'NONE', ( #3947, #1252, #33490, #29020 ) ) ;
#30379=DIRECTION ( 'NONE',  ( -1.000000000000000000, 0.000000000000000000, 0.000000000000000000 ) ) ;
#30381=VERTEX_POINT ( 'NONE', #20521 ) ;
#30382=FACE_OUTER_BOUND ( 'NONE', #34382, .T. ) ;
#30383=ORIENTED_EDGE ( 'NONE', *, *, #36575, .F. ) ;
#30387=CARTESIAN_POINT ( 'NONE',  ( 15.00000000000000000, 9.615535125378766423, -24.73947219025917121 ) ) ;
#30390=VERTEX_POINT ( 'NONE', #35934 ) ;
#30398=CARTESIAN_POINT ( 'NONE',  ( 0.000000000000000000, -29.01471420065506379, -76.69515212746047439 ) ) ;
#30402=LINE ( 'NONE', #15468, #22394 ) ;
#30404=CARTESIAN_POINT ( 'NONE',  ( 15.00000000000000000, -14.54903810567676636, -22.19967320028755964 ) ) ;
#30411=EDGE_CURVE ( 'NONE', #12511, #23540, #32045, .T. ) ;
#30412=EDGE_CURVE ( 'NONE', #1469, #13012, #27903, .T. ) ;
#30414=FACE_BOUND ( 'NONE', #13225, .T. ) ;
#30418=CARTESIAN_POINT ( 'NONE',  ( 11.99999999999999822, 0.000000000000000000, 0.000000000000000000 ) ) ;
#30421=DIRECTION ( 'NONE',  ( -1.000000000000000000, 0.000000000000000000, 0.000000000000000000 ) ) ;
#30422=CIRCLE ( 'NONE', #42935, 82.00000000000000000 ) ;
#30433=FACE_OUTER_BOUND ( 'NONE', #45254, .T. ) ;
#30439=ORIENTED_EDGE ( 'NONE', *, *, #43592, .F. ) ;
#30440=VERTEX_POINT ( 'NONE', #10229 ) ;
#30444=CYLINDRICAL_SURFACE ( 'NONE', #35968, 82.00000000000000000 ) ;
#30445=DIRECTION ( 'NONE',  ( -1.000000000000000000, -0.000000000000000000, 0.000000000000000000 ) ) ;
#30447=CARTESIAN_POINT ( 'NONE',  ( 11.99999999999999822, -62.50884508063453637, 41.76106447765467777 ) ) ;
#30450=CARTESIAN_POINT ( 'NONE',  ( -10.00000000000000000, 0.000000000000000000, 0.000000000000000000 ) ) ;
#30451=DIRECTION ( 'NONE',  ( 0.000000000000000000, 0.000000000000000000, 1.000000000000000000 ) ) ;
#30452=CARTESIAN_POINT ( 'NONE',  ( 0.000000000000000000, -59.46389618801929089, -49.70050353004953081 ) ) ;
#30453=VECTOR ( 'NONE', #40212, 1000.000000000000000 ) ;
#30455=CARTESIAN_POINT ( 'NONE',  ( 11.99999999999999822, 75.11764819372149304, -2.946379043146603482 ) ) ;
#30458=CIRCLE ( 'NONE', #43761, 82.00000000000000000 ) ;
#30459=DIRECTION ( 'NONE',  ( -1.000000000000000000, -0.000000000000000000, -0.000000000000000000 ) ) ;
#30462=EDGE_CURVE ( 'NONE', #9384, #6289, #1693, .T. ) ;
#30465=DIRECTION ( 'NONE',  ( -1.000000000000000000, 0.000000000000000000, -0.000000000000000000 ) ) ;
#30471=ORIENTED_EDGE ( 'NONE', *, *, #10893, .F. ) ;
#30472=EDGE_CURVE ( 'NONE', #20366, #45561, #1826, .T. ) ;
#30476=ORIENTED_EDGE ( 'NONE', *, *, #18405, .F. ) ;
#30480=DIRECTION ( 'NONE',  ( 1.000000000000000000, 0.000000000000000000, -0.000000000000000000 ) ) ;
#30482=ORIENTED_EDGE ( 'NONE', *, *, #41234, .F. ) ;
#30483=DIRECTION ( 'NONE',  ( 0.000000000000000000, 0.9238795325112851842, 0.3826834323650937786 ) ) ;
#30487=CARTESIAN_POINT ( 'NONE',  ( 11.99999999999999822, -80.28980883073745645, -16.65972982745018172 ) ) ;
#30492=EDGE_LOOP ( 'NONE', ( #29320, #4364, #9991, #27197 ) ) ;
#30493=FACE_OUTER_BOUND ( 'NONE', #15860, .T. ) ;
#30496=DIRECTION ( 'NONE',  ( 0.000000000000000000, 0.000000000000000000, 1.000000000000000000 ) ) ;
#30497=CARTESIAN_POINT ( 'NONE',  ( 0.000000000000000000, 0.000000000000000000, 0.000000000000000000 ) ) ;
#30498=CARTESIAN_POINT ( 'NONE',  ( -10.00000000000000000, 0.000000000000000000, 0.000000000000000000 ) ) ;
#30502=EDGE_LOOP ( 'NONE', ( #26129, #19801, #31099, #11307 ) ) ;
#30506=CARTESIAN_POINT ( 'NONE',  ( 0.000000000000000000, -71.27951684758045303, 30.41916302227090085 ) ) ;
#30507=DIRECTION ( 'NONE',  ( -1.000000000000000000, 0.000000000000000000, -0.000000000000000000 ) ) ;
#30510=EDGE_CURVE ( 'NONE', #11988, #45060, #11263, .T. ) ;
#30512=DIRECTION ( 'NONE',  ( -1.000000000000000000, -0.000000000000000000, -0.000000000000000000 ) ) ;
#30516=CARTESIAN_POINT ( 'NONE',  ( 11.99999999999999822, -11.30684508768393748, 76.66974797899833050 ) ) ;
#30521=CARTESIAN_POINT ( 'NONE',  ( 11.99999999999999822, 73.44644590900094272, -24.73286445877629802 ) ) ;
#30522=VECTOR ( 'NONE', #47510, 1000.000000000000000 ) ;
#30524=AXIS2_PLACEMENT_3D ( 'NONE', #24352, #9663, #24609 ) ;
#30525=CARTESIAN_POINT ( 'NONE',  ( 0.000000000000000000, -46.11716303203136391, -67.80270845531939017 ) ) ;
#30527=VERTEX_POINT ( 'NONE', #7275 ) ;
#30528=EDGE_CURVE ( 'NONE', #7347, #31342, #47904, .T. ) ;
#30530=ORIENTED_EDGE ( 'NONE', *, *, #9724, .T. ) ;
#30531=ORIENTED_EDGE ( 'NONE', *, *, #36786, .T. ) ;
#30532=CARTESIAN_POINT ( 'NONE',  ( 11.99999999999999822, 71.91182617369190666, 28.89263327155770966 ) ) ;
#30533=CARTESIAN_POINT ( 'NONE',  ( 0.000000000000000000, 0.000000000000000000, 0.000000000000000000 ) ) ;
#30535=LINE ( 'NONE', #7549, #48398 ) ;
#30536=VERTEX_POINT ( 'NONE', #18542 ) ;
#30543=CARTESIAN_POINT ( 'NONE',  ( 5.999999999999999112, 63.97538442413426907, 51.29473840253246664 ) ) ;
#30547=CARTESIAN_POINT ( 'NONE',  ( 11.99999999999999822, 0.000000000000000000, 0.000000000000000000 ) ) ;
#30550=EDGE_CURVE ( 'NONE', #913, #35715, #17503, .T. ) ;
#30551=DIRECTION ( 'NONE',  ( -1.000000000000000000, 0.000000000000000000, 0.000000000000000000 ) ) ;
#30555=AXIS2_PLACEMENT_3D ( 'NONE', #30387, #23030, #11544 ) ;
#30557=CIRCLE ( 'NONE', #29015, 31.99999999999998579 ) ;
#30563=PLANE ( 'NONE',  #21263 ) ;
#30572=FACE_OUTER_BOUND ( 'NONE', #18636, .T. ) ;
#30573=DIRECTION ( 'NONE',  ( -1.000000000000000000, -0.000000000000000000, -0.000000000000000000 ) ) ;
#30585=CIRCLE ( 'NONE', #16548, 82.00000000000000000 ) ;
#30586=DIRECTION ( 'NONE',  ( -1.000000000000000000, -0.000000000000000000, -0.000000000000000000 ) ) ;
#30587=ADVANCED_FACE ( 'NONE', ( #7536 ), #29324, .T. ) ;
#30588=CYLINDRICAL_SURFACE ( 'NONE', #8134, 82.00000000000000000 ) ;
#30591=AXIS2_PLACEMENT_3D ( 'NONE', #41589, #48203, #22002 ) ;
#30594=PLANE ( 'NONE',  #7033 ) ;
#30600=VECTOR ( 'NONE', #37002, 1000.000000000000227 ) ;
#30602=EDGE_LOOP ( 'NONE', ( #32039, #47868, #13663, #24816 ) ) ;
#30605=EDGE_CURVE ( 'NONE', #15986, #37774, #17810, .T. ) ;
#30607=ORIENTED_EDGE ( 'NONE', *, *, #10679, .T. ) ;
#30608=LINE ( 'NONE', #23499, #5140 ) ;
#30611=VERTEX_POINT ( 'NONE', #21730 ) ;
#30614=VECTOR ( 'NONE', #36877, 1000.000000000000000 ) ;
#30617=ORIENTED_EDGE ( 'NONE', *, *, #42987, .T. ) ;
#30622=EDGE_CURVE ( 'NONE', #2200, #5341, #3416, .T. ) ;
#30624=FACE_OUTER_BOUND ( 'NONE', #30502, .T. ) ;
#30629=DIRECTION ( 'NONE',  ( 0.000000000000000000, 0.000000000000000000, 1.000000000000000000 ) ) ;
#30630=CIRCLE ( 'NONE', #15661, 31.99999999999999289 ) ;
#30632=CIRCLE ( 'NONE', #42332, 82.00000000000000000 ) ;
#30634=CYLINDRICAL_SURFACE ( 'NONE', #3656, 31.99999999999998579 ) ;
#30637=DIRECTION ( 'NONE',  ( -1.000000000000000000, 0.000000000000000000, 0.000000000000000000 ) ) ;
#30638=DIRECTION ( 'NONE',  ( -1.000000000000000000, -0.000000000000000000, -0.000000000000000000 ) ) ;
#30639=ORIENTED_EDGE ( 'NONE', *, *, #10779, .T. ) ;
#30642=DIRECTION ( 'NONE',  ( -1.000000000000000000, -0.000000000000000000, 0.000000000000000000 ) ) ;
#30653=AXIS2_PLACEMENT_3D ( 'NONE', #37555, #22623, #33406 ) ;
#30663=ORIENTED_EDGE ( 'NONE', *, *, #18822, .T. ) ;
#30665=ORIENTED_EDGE ( 'NONE', *, *, #28014, .T. ) ;
#30670=DIRECTION ( 'NONE',  ( -1.000000000000000000, -0.000000000000000000, -0.000000000000000000 ) ) ;
#30673=DIRECTION ( 'NONE',  ( 0.000000000000000000, 0.7431448254773878048, -0.6691306063588654540 ) ) ;
#30675=ORIENTED_EDGE ( 'NONE', *, *, #45586, .F. ) ;
#30677=DIRECTION ( 'NONE',  ( 0.000000000000000000, 0.000000000000000000, 1.000000000000000000 ) ) ;
#30683=CARTESIAN_POINT ( 'NONE',  ( 5.999999999999999112, -67.80270845531921964, 46.11716303203162681 ) ) ;
#30688=CIRCLE ( 'NONE', #200, 31.99999999999997868 ) ;
#30689=CARTESIAN_POINT ( 'NONE',  ( 11.99999999999999822, 26.02418014898407961, -70.52718814184231633 ) ) ;
#30691=DIRECTION ( 'NONE',  ( 0.000000000000000000, 0.3826834323650904479, -0.9238795325112865164 ) ) ;
#30697=LINE ( 'NONE', #42192, #41710 ) ;
#30701=ORIENTED_EDGE ( 'NONE', *, *, #14392, .F. ) ;
#30702=CARTESIAN_POINT ( 'NONE',  ( 11.99999999999999822, 0.000000000000000000, 0.000000000000000000 ) ) ;
#30703=DIRECTION ( 'NONE',  ( -1.000000000000000000, 0.000000000000000000, 0.000000000000000000 ) ) ;
#30706=ORIENTED_EDGE ( 'NONE', *, *, #21771, .F. ) ;
#30707=CIRCLE ( 'NONE', #4157, 82.00000000000000000 ) ;
#30709=ORIENTED_EDGE ( 'NONE', *, *, #35136, .F. ) ;
#30712=ORIENTED_EDGE ( 'NONE', *, *, #16202, .T. ) ;
#30713=EDGE_CURVE ( 'NONE', #17850, #1046, #47966, .T. ) ;
#30714=EDGE_LOOP ( 'NONE', ( #19274, #1762, #47309, #28627 ) ) ;
#30715=CARTESIAN_POINT ( 'NONE',  ( 5.999999999999999112, 68.55367621811141987, 44.99326035066079044 ) ) ;
#30720=CIRCLE ( 'NONE', #4133, 77.49900000000000944 ) ;
#30726=CIRCLE ( 'NONE', #20656, 31.99999999999998579 ) ;
#30729=EDGE_LOOP ( 'NONE', ( #41257, #2598, #29395, #16715 ) ) ;
#30730=DIRECTION ( 'NONE',  ( -1.000000000000000000, 0.000000000000000000, 0.000000000000000000 ) ) ;
#30731=VECTOR ( 'NONE', #48371, 1000.000000000000000 ) ;
#30733=AXIS2_PLACEMENT_3D ( 'NONE', #34715, #9260, #46229 ) ;
#30740=VERTEX_POINT ( 'NONE', #19919 ) ;
#30741=ORIENTED_EDGE ( 'NONE', *, *, #13635, .T. ) ;
#30745=CARTESIAN_POINT ( 'NONE',  ( 11.99999999999999822, 62.50329211542435104, 41.76937507738811917 ) ) ;
#30746=CARTESIAN_POINT ( 'NONE',  ( 0.000000000000000000, 46.54456581323888997, -59.03342792756214408 ) ) ;
#30757=EDGE_LOOP ( 'NONE', ( #1043, #15013, #21875, #6351 ) ) ;
#30764=AXIS2_PLACEMENT_3D ( 'NONE', #22744, #3409, #3665 ) ;
#30767=FACE_OUTER_BOUND ( 'NONE', #3809, .T. ) ;
#30770=VECTOR ( 'NONE', #8976, 1000.000000000000000 ) ;
#30773=CYLINDRICAL_SURFACE ( 'NONE', #36146, 31.99999999999998579 ) ;
#30777=EDGE_CURVE ( 'NONE', #39062, #17273, #14372, .T. ) ;
#30787=AXIS2_PLACEMENT_3D ( 'NONE', #15654, #30586, #4640 ) ;
#30803=ORIENTED_EDGE ( 'NONE', *, *, #15031, .T. ) ;
#30813=ORIENTED_EDGE ( 'NONE', *, *, #17459, .F. ) ;
#30820=AXIS2_PLACEMENT_3D ( 'NONE', #16367, #16140, #19304 ) ;
#30821=CARTESIAN_POINT ( 'NONE',  ( 0.000000000000000000, -63.97538442413463855, 51.29473840253199057 ) ) ;
#30823=CIRCLE ( 'NONE', #9696, 31.99999999999997868 ) ;
#30825=LINE ( 'NONE', #23226, #46658 ) ;
#30831=ORIENTED_EDGE ( 'NONE', *, *, #16147, .F. ) ;
#30835=ORIENTED_EDGE ( 'NONE', *, *, #18230, .F. ) ;
#30839=ADVANCED_FACE ( 'NONE', ( #43889 ), #47330, .T. ) ;
#30840=DIRECTION ( 'NONE',  ( -1.000000000000000000, 0.000000000000000000, -0.000000000000000000 ) ) ;
#30844=EDGE_CURVE ( 'NONE', #47607, #1817, #12725, .T. ) ;
#30845=EDGE_CURVE ( 'NONE', #38290, #32306, #29198, .T. ) ;
#30846=AXIS2_PLACEMENT_3D ( 'NONE', #2841, #35663, #5811 ) ;
#30852=ORIENTED_EDGE ( 'NONE', *, *, #16102, .T. ) ;
#30854=ORIENTED_EDGE ( 'NONE', *, *, #3795, .F. ) ;
#30877=CARTESIAN_POINT ( 'NONE',  ( 0.000000000000000000, -74.65491531819111515, 23.16904090965678265 ) ) ;
#30880=AXIS2_PLACEMENT_3D ( 'NONE', #11118, #6959, #25307 ) ;
#30882=ORIENTED_EDGE ( 'NONE', *, *, #23105, .F. ) ;
#30883=DIRECTION ( 'NONE',  ( 1.000000000000000000, -0.000000000000000000, -0.000000000000000000 ) ) ;
#30892=CARTESIAN_POINT ( 'NONE',  ( 11.99999999999999822, 0.000000000000000000, 0.000000000000000000 ) ) ;
#30894=DIRECTION ( 'NONE',  ( 0.000000000000000000, -0.7604059656000227152, -0.6494480483301933171 ) ) ;
#30895=VERTEX_POINT ( 'NONE', #36304 ) ;
#30900=DIRECTION ( 'NONE',  ( 0.000000000000000000, 0.000000000000000000, 1.000000000000000000 ) ) ;
#30906=PLANE ( 'NONE',  #26966 ) ;
#30909=DIRECTION ( 'NONE',  ( -1.000000000000000000, 0.000000000000000000, 0.000000000000000000 ) ) ;
#30911=DIRECTION ( 'NONE',  ( -1.000000000000000000, 0.000000000000000000, 0.000000000000000000 ) ) ;
#30915=EDGE_CURVE ( 'NONE', #42540, #6202, #29128, .T. ) ;
#30919=ORIENTED_EDGE ( 'NONE', *, *, #23662, .F. ) ;
#30923=ORIENTED_EDGE ( 'NONE', *, *, #13487, .F. ) ;
#30924=DIRECTION ( 'NONE',  ( 0.000000000000000000, 0.7071067811865439090, 0.7071067811865512365 ) ) ;
#30925=DIRECTION ( 'NONE',  ( -1.000000000000000000, -0.000000000000000000, 0.000000000000000000 ) ) ;
#30926=ORIENTED_EDGE ( 'NONE', *, *, #21041, .F. ) ;
#30928=AXIS2_PLACEMENT_3D ( 'NONE', #19189, #34115, #37314 ) ;
#30931=AXIS2_PLACEMENT_3D ( 'NONE', #11535, #27188, #4663 ) ;
#30932=DIRECTION ( 'NONE',  ( -1.000000000000000000, -0.000000000000000000, 0.000000000000000000 ) ) ;
#30940=DIRECTION ( 'NONE',  ( -1.000000000000000000, 0.000000000000000000, 0.000000000000000000 ) ) ;
#30945=CYLINDRICAL_SURFACE ( 'NONE', #27414, 31.99999999999998579 ) ;
#30947=DIRECTION ( 'NONE',  ( 0.000000000000000000, -0.7604059656000227152, -0.6494480483301933171 ) ) ;
#30949=DIRECTION ( 'NONE',  ( -1.000000000000000000, -0.000000000000000000, -0.000000000000000000 ) ) ;
#30954=PLANE ( 'NONE',  #2766 ) ;
#30959=VERTEX_POINT ( 'NONE', #22350 ) ;
#30960=EDGE_CURVE ( 'NONE', #16242, #23540, #8133, .T. ) ;
#30962=DIRECTION ( 'NONE',  ( -1.000000000000000000, 0.000000000000000000, 0.000000000000000000 ) ) ;
#30965=ORIENTED_EDGE ( 'NONE', *, *, #46704, .F. ) ;
#30970=DIRECTION ( 'NONE',  ( 0.000000000000000000, 0.5877852522924684742, 0.8090169943749506709 ) ) ;
#30971=CIRCLE ( 'NONE', #2035, 82.00000000000000000 ) ;
#30972=EDGE_LOOP ( 'NONE', ( #45343, #26684, #25225, #42990 ) ) ;
#30973=AXIS2_PLACEMENT_3D ( 'NONE', #29732, #41722, #26063 ) ;
#30974=EDGE_CURVE ( 'NONE', #7137, #25598, #38002, .T. ) ;
#30978=EDGE_CURVE ( 'NONE', #27571, #13807, #40949, .T. ) ;
#30986=ORIENTED_EDGE ( 'NONE', *, *, #36373, .F. ) ;
#30992=LINE ( 'NONE', #16999, #45008 ) ;
#30997=LINE ( 'NONE', #26582, #1323 ) ;
#30999=DIRECTION ( 'NONE',  ( -1.000000000000000000, 0.000000000000000000, 0.000000000000000000 ) ) ;
#31000=AXIS2_PLACEMENT_3D ( 'NONE', #31615, #43808, #39682 ) ;
#31002=DIRECTION ( 'NONE',  ( 0.000000000000000000, 0.8526401643540897357, 0.5224985647159527957 ) ) ;
#31004=DIRECTION ( 'NONE',  ( 0.000000000000000000, 0.6494480483301793283, 0.7604059656000345946 ) ) ;
#31012=ORIENTED_EDGE ( 'NONE', *, *, #25161, .T. ) ;
#31015=CARTESIAN_POINT ( 'NONE',  ( 6.000000000000000000, 10.30890764327382136, 81.34940948281339956 ) ) ;
#31020=ADVANCED_FACE ( 'NONE', ( #11340 ), #40698, .T. ) ;
#31024=CARTESIAN_POINT ( 'NONE',  ( 11.99999999999999822, -77.19088730480518734, -6.903761155838607166 ) ) ;
#31030=EDGE_CURVE ( 'NONE', #17149, #13012, #44614, .T. ) ;
#31031=EDGE_CURVE ( 'NONE', #26821, #22916, #15253, .T. ) ;
#31035=ORIENTED_EDGE ( 'NONE', *, *, #1799, .F. ) ;
#31037=ORIENTED_EDGE ( 'NONE', *, *, #1025, .T. ) ;
#31041=LINE ( 'NONE', #9226, #3067 ) ;
#31044=ORIENTED_EDGE ( 'NONE', *, *, #43410, .F. ) ;
#31048=ORIENTED_EDGE ( 'NONE', *, *, #21551, .F. ) ;
#31049=CIRCLE ( 'NONE', #22449, 77.49900000000002365 ) ;
#31053=VERTEX_POINT ( 'NONE', #7653 ) ;
#31056=CARTESIAN_POINT ( 'NONE',  ( 11.99999999999999822, 65.64334221924909230, 41.19522573413756561 ) ) ;
#31062=EDGE_LOOP ( 'NONE', ( #25995, #47753, #45471, #7776 ) ) ;
#31064=DIRECTION ( 'NONE',  ( 0.000000000000000000, 0.000000000000000000, 1.000000000000000000 ) ) ;
#31073=CIRCLE ( 'NONE', #13072, 77.49900000000000944 ) ;
#31074=DIRECTION ( 'NONE',  ( 0.000000000000000000, 0.000000000000000000, 1.000000000000000000 ) ) ;
#31075=DIRECTION ( 'NONE',  ( -1.000000000000000000, 0.000000000000000000, 0.000000000000000000 ) ) ;
#31077=EDGE_CURVE ( 'NONE', #27912, #42537, #20339, .T. ) ;
#31079=FACE_OUTER_BOUND ( 'NONE', #47673, .T. ) ;
#31084=EDGE_CURVE ( 'NONE', #20902, #27256, #37742, .T. ) ;
#31085=EDGE_CURVE ( 'NONE', #21091, #7113, #34543, .T. ) ;
#31086=VERTEX_POINT ( 'NONE', #46068 ) ;
#31087=CARTESIAN_POINT ( 'NONE',  ( 11.99999999999999822, -36.73666225445940370, 65.58780272294062286 ) ) ;
#31090=CARTESIAN_POINT ( 'NONE',  ( 0.000000000000000000, -51.03279382321125723, 55.19960302592048862 ) ) ;
#31091=ORIENTED_EDGE ( 'NONE', *, *, #28596, .T. ) ;
#31098=VERTEX_POINT ( 'NONE', #35041 ) ;
#31099=ORIENTED_EDGE ( 'NONE', *, *, #33218, .F. ) ;
#31100=CARTESIAN_POINT ( 'NONE',  ( 15.00000000000000000, -26.23277895567251505, -4.042438405569750870 ) ) ;
#31103=ORIENTED_EDGE ( 'NONE', *, *, #44084, .T. ) ;
#31136=VECTOR ( 'NONE', #33816, 1000.000000000000000 ) ;
#31137=FACE_OUTER_BOUND ( 'NONE', #26012, .T. ) ;
#31145=ORIENTED_EDGE ( 'NONE', *, *, #24569, .T. ) ;
#31151=AXIS2_PLACEMENT_3D ( 'NONE', #20331, #20833, #28407 ) ;
#31152=EDGE_CURVE ( 'NONE', #47426, #38615, #12066, .T. ) ;
#31153=ORIENTED_EDGE ( 'NONE', *, *, #21419, .F. ) ;
#31164=AXIS2_PLACEMENT_3D ( 'NONE', #42789, #20015, #5576 ) ;
#31170=FACE_OUTER_BOUND ( 'NONE', #41114, .T. ) ;
#31175=VERTEX_POINT ( 'NONE', #8845 ) ;
#31178=FACE_OUTER_BOUND ( 'NONE', #20174, .T. ) ;
#31183=CARTESIAN_POINT ( 'NONE',  ( 11.99999999999999822, 0.000000000000000000, 0.000000000000000000 ) ) ;
#31190=CARTESIAN_POINT ( 'NONE',  ( 11.99999999999999822, 0.000000000000000000, 0.000000000000000000 ) ) ;
#31197=CYLINDRICAL_SURFACE ( 'NONE', #22940, 82.00000000000000000 ) ;
#31198=EDGE_LOOP ( 'NONE', ( #17443, #45577, #46512, #34364 ) ) ;
#31205=CIRCLE ( 'NONE', #32746, 31.99999999999998579 ) ;
#31206=DIRECTION ( 'NONE',  ( 1.000000000000000000, 0.000000000000000000, 0.000000000000000000 ) ) ;
#31207=ORIENTED_EDGE ( 'NONE', *, *, #45700, .F. ) ;
#31209=ORIENTED_EDGE ( 'NONE', *, *, #27223, .T. ) ;
#31210=VERTEX_POINT ( 'NONE', #6627 ) ;
#31217=CARTESIAN_POINT ( 'NONE',  ( 11.99999999999999822, 0.000000000000000000, 0.000000000000000000 ) ) ;
#31220=CARTESIAN_POINT ( 'NONE',  ( 11.99999999999999822, -62.50884508063453637, 41.76106447765467777 ) ) ;
#31226=CIRCLE ( 'NONE', #32038, 82.00000000000000000 ) ;
#31228=ORIENTED_EDGE ( 'NONE', *, *, #21709, .T. ) ;
#31236=DIRECTION ( 'NONE',  ( -1.000000000000000000, -0.000000000000000000, -0.000000000000000000 ) ) ;
#31239=EDGE_CURVE ( 'NONE', #31422, #43255, #22148, .T. ) ;
#31240=DIRECTION ( 'NONE',  ( -1.000000000000000000, 0.000000000000000000, -0.000000000000000000 ) ) ;
#31245=CARTESIAN_POINT ( 'NONE',  ( 0.000000000000000000, 0.000000000000000000, 0.000000000000000000 ) ) ;
#31254=CARTESIAN_POINT ( 'NONE',  ( 0.000000000000000000, 58.39081064771751528, 50.95692526931350841 ) ) ;
#31255=CARTESIAN_POINT ( 'NONE',  ( 15.00000000000000000, -0.9646360437372099028, 23.52805723605590771 ) ) ;
#31258=DIRECTION ( 'NONE',  ( 0.000000000000000000, 0.000000000000000000, 1.000000000000000000 ) ) ;
#31263=LINE ( 'NONE', #12653, #1773 ) ;
#31265=ORIENTED_EDGE ( 'NONE', *, *, #32346, .T. ) ;
#31270=AXIS2_PLACEMENT_3D ( 'NONE', #5931, #13497, #20849 ) ;
#31272=ORIENTED_EDGE ( 'NONE', *, *, #2324, .F. ) ;
#31276=FACE_OUTER_BOUND ( 'NONE', #40326, .T. ) ;
#31280=ORIENTED_EDGE ( 'NONE', *, *, #1158, .T. ) ;
#31286=ORIENTED_EDGE ( 'NONE', *, *, #38795, .F. ) ;
#31293=ORIENTED_EDGE ( 'NONE', *, *, #25734, .T. ) ;
#31294=CYLINDRICAL_SURFACE ( 'NONE', #32273, 82.00000000000000000 ) ;
#31296=ADVANCED_FACE ( 'NONE', ( #28667 ), #21787, .F. ) ;
#31297=CYLINDRICAL_SURFACE ( 'NONE', #20520, 77.49899999999999523 ) ;
#31300=EDGE_CURVE ( 'NONE', #11246, #5925, #28887, .T. ) ;
#31302=DIRECTION ( 'NONE',  ( -1.000000000000000000, -0.000000000000000000, -0.000000000000000000 ) ) ;
#31312=EDGE_CURVE ( 'NONE', #45678, #20008, #36481, .T. ) ;
#31314=VECTOR ( 'NONE', #43207, 1000.000000000000000 ) ;
#31321=VERTEX_POINT ( 'NONE', #24755 ) ;
#31325=VERTEX_POINT ( 'NONE', #46794 ) ;
#31327=FACE_OUTER_BOUND ( 'NONE', #38709, .T. ) ;
#31329=VERTEX_POINT ( 'NONE', #2944 ) ;
#31331=AXIS2_PLACEMENT_3D ( 'NONE', #341, #15518, #44895 ) ;
#31334=DIRECTION ( 'NONE',  ( -1.000000000000000000, -0.000000000000000000, -0.000000000000000000 ) ) ;
#31337=ORIENTED_EDGE ( 'NONE', *, *, #4641, .T. ) ;
#31339=EDGE_CURVE ( 'NONE', #6663, #30146, #29168, .T. ) ;
#31342=VERTEX_POINT ( 'NONE', #15426 ) ;
#31348=VECTOR ( 'NONE', #1435, 1000.000000000000000 ) ;
#31351=ORIENTED_EDGE ( 'NONE', *, *, #22727, .T. ) ;
#31352=DIRECTION ( 'NONE',  ( -1.000000000000000000, 0.000000000000000000, 0.000000000000000000 ) ) ;
#31358=ORIENTED_EDGE ( 'NONE', *, *, #46906, .F. ) ;
#31363=ORIENTED_EDGE ( 'NONE', *, *, #15133, .T. ) ;
#31369=CARTESIAN_POINT ( 'NONE',  ( 11.99999999999999822, -65.64334221924882229, -41.19522573413803457 ) ) ;
#31370=LINE ( 'NONE', #20821, #16373 ) ;
#31372=EDGE_CURVE ( 'NONE', #42048, #31422, #12765, .T. ) ;
#31374=AXIS2_PLACEMENT_3D ( 'NONE', #23516, #38953, #42370 ) ;
#31380=CIRCLE ( 'NONE', #43860, 31.99999999999998934 ) ;
#31381=CIRCLE ( 'NONE', #27456, 82.00000000000000000 ) ;
#31383=CARTESIAN_POINT ( 'NONE',  ( 0.000000000000000000, -77.19088730480527261, 6.903761155837504049 ) ) ;
#31385=FACE_OUTER_BOUND ( 'NONE', #47355, .T. ) ;
#31390=ORIENTED_EDGE ( 'NONE', *, *, #2390, .F. ) ;
#31392=AXIS2_PLACEMENT_3D ( 'NONE', #7975, #642, #37604 ) ;
#31393=CARTESIAN_POINT ( 'NONE',  ( 6.000000000000000000, 81.34940948281351325, -10.30890764327295450 ) ) ;
#31395=ORIENTED_EDGE ( 'NONE', *, *, #37982, .T. ) ;
#31398=ADVANCED_FACE ( 'NONE', ( #44311 ), #11515, .T. ) ;
#31400=CARTESIAN_POINT ( 'NONE',  ( 11.99999999999999822, 46.21855187248719687, -62.20884554313968806 ) ) ;
#31401=ADVANCED_FACE ( 'NONE', ( #7097 ), #33291, .T. ) ;
#31403=DIRECTION ( 'NONE',  ( -1.000000000000000000, -0.000000000000000000, 0.000000000000000000 ) ) ;
#31407=LINE ( 'NONE', #27729, #44989 ) ;
#31408=AXIS2_PLACEMENT_3D ( 'NONE', #4557, #15568, #30274 ) ;
#31411=VERTEX_POINT ( 'NONE', #18828 ) ;
#31414=EDGE_CURVE ( 'NONE', #28248, #34700, #24497, .T. ) ;
#31416=CARTESIAN_POINT ( 'NONE',  ( 11.99999999999999822, 0.000000000000000000, 0.000000000000000000 ) ) ;
#31422=VERTEX_POINT ( 'NONE', #36945 ) ;
#31424=EDGE_CURVE ( 'NONE', #20505, #1277, #3419, .T. ) ;
#31428=DIRECTION ( 'NONE',  ( 0.000000000000000000, -0.7604059656000369261, 0.6494480483301766638 ) ) ;
#31430=ORIENTED_EDGE ( 'NONE', *, *, #22714, .T. ) ;
#31431=CARTESIAN_POINT ( 'NONE',  ( 11.99999999999999822, 51.29473840253223216, 63.97538442413446091 ) ) ;
#31433=FACE_OUTER_BOUND ( 'NONE', #39163, .T. ) ;
#31436=CARTESIAN_POINT ( 'NONE',  ( 11.99999999999999822, 0.000000000000000000, 0.000000000000000000 ) ) ;
#31446=AXIS2_PLACEMENT_3D ( 'NONE', #20865, #35786, #2250 ) ;
#31450=AXIS2_PLACEMENT_3D ( 'NONE', #35237, #29092, #2908 ) ;
#31451=DIRECTION ( 'NONE',  ( 0.000000000000000000, 1.000000000000000000, 3.469446951953616555E-15 ) ) ;
#31456=EDGE_CURVE ( 'NONE', #32306, #13449, #2664, .T. ) ;
#31458=CARTESIAN_POINT ( 'NONE',  ( 11.99999999999999822, -10.30890764327441289, 81.34940948281332851 ) ) ;
#31459=ADVANCED_FACE ( 'NONE', ( #22750 ), #4165, .T. ) ;
#31462=ORIENTED_EDGE ( 'NONE', *, *, #43057, .T. ) ;
#31463=ORIENTED_EDGE ( 'NONE', *, *, #15191, .F. ) ;
#31464=CYLINDRICAL_SURFACE ( 'NONE', #3966, 31.99999999999998579 ) ;
#31468=DIRECTION ( 'NONE',  ( -0.000000000000000000, 0.6691306063588672304, 0.7431448254773862505 ) ) ;
#31470=EDGE_LOOP ( 'NONE', ( #1527, #26946, #37852, #31293 ) ) ;
#31473=ORIENTED_EDGE ( 'NONE', *, *, #12225, .F. ) ;
#31474=ADVANCED_FACE ( 'NONE', ( #38672 ), #34727, .T. ) ;
#31476=DIRECTION ( 'NONE',  ( -1.000000000000000000, -0.000000000000000000, 0.000000000000000000 ) ) ;
#31478=CARTESIAN_POINT ( 'NONE',  ( 15.00000000000000000, -23.29833615347104470, 3.418703333116808629 ) ) ;
#31480=DIRECTION ( 'NONE',  ( 1.000000000000000000, 0.000000000000000000, 0.000000000000000000 ) ) ;
#31487=CARTESIAN_POINT ( 'NONE',  ( 11.99999999999999822, -26.01480285779785362, -70.53064760720343429 ) ) ;
#31495=DIRECTION ( 'NONE',  ( -1.000000000000000000, 0.000000000000000000, 0.000000000000000000 ) ) ;
#31498=CYLINDRICAL_SURFACE ( 'NONE', #26358, 31.99999999999998579 ) ;
#31501=CARTESIAN_POINT ( 'NONE',  ( 11.99999999999999822, -14.66109333815410487, -73.73191006444587003 ) ) ;
#31502=CIRCLE ( 'NONE', #44748, 77.49899999999999523 ) ;
#31506=DIRECTION ( 'NONE',  ( -1.000000000000000000, -0.000000000000000000, -0.000000000000000000 ) ) ;
#31508=ORIENTED_EDGE ( 'NONE', *, *, #27190, .F. ) ;
#31509=AXIS2_PLACEMENT_3D ( 'NONE', #14449, #34001, #33031 ) ;
#31512=EDGE_CURVE ( 'NONE', #47535, #44620, #43367, .T. ) ;
#31515=AXIS2_PLACEMENT_3D ( 'NONE', #21988, #11484, #15868 ) ;
#31519=VECTOR ( 'NONE', #12460, 1000.000000000000000 ) ;
#31521=VERTEX_POINT ( 'NONE', #4414 ) ;
#31523=FACE_OUTER_BOUND ( 'NONE', #19690, .T. ) ;
#31524=CIRCLE ( 'NONE', #47123, 31.99999999999998579 ) ;
#31525=LINE ( 'NONE', #6287, #2699 ) ;
#31532=ORIENTED_EDGE ( 'NONE', *, *, #9891, .F. ) ;
#31536=CARTESIAN_POINT ( 'NONE',  ( 0.000000000000000000, -75.54627589209955829, 17.28742895386058009 ) ) ;
#31537=DIRECTION ( 'NONE',  ( 0.000000000000000000, -0.9969173337331287410, 0.07845909572783495156 ) ) ;
#31538=ORIENTED_EDGE ( 'NONE', *, *, #30915, .F. ) ;
#31540=CARTESIAN_POINT ( 'NONE',  ( 11.99999999999999822, 0.000000000000000000, 0.000000000000000000 ) ) ;
#31542=CARTESIAN_POINT ( 'NONE',  ( 11.99999999999999822, 0.000000000000000000, 0.000000000000000000 ) ) ;
#31545=CIRCLE ( 'NONE', #31509, 77.49899999999999523 ) ;
#31549=CARTESIAN_POINT ( 'NONE',  ( 6.000000000000000000, -16.65972982744876774, -80.28980883073775487 ) ) ;
#31554=LINE ( 'NONE', #12696, #39603 ) ;
#31555=LINE ( 'NONE', #46478, #1094 ) ;
#31558=CYLINDRICAL_SURFACE ( 'NONE', #11918, 77.49899999999999523 ) ;
#31560=VECTOR ( 'NONE', #37514, 1000.000000000000000 ) ;
#31563=CARTESIAN_POINT ( 'NONE',  ( 0.000000000000000000, -20.41045688087876897, 72.35160999960810102 ) ) ;
#31568=ORIENTED_EDGE ( 'NONE', *, *, #6511, .F. ) ;
#31570=ADVANCED_FACE ( 'NONE', ( #12244 ), #38909, .F. ) ;
#31583=VERTEX_POINT ( 'NONE', #44468 ) ;
#31587=ORIENTED_EDGE ( 'NONE', *, *, #32863, .T. ) ;
#31588=AXIS2_PLACEMENT_3D ( 'NONE', #42888, #31889, #25944 ) ;
#31593=VECTOR ( 'NONE', #45258, 1000.000000000000000 ) ;
#31595=CIRCLE ( 'NONE', #17484, 77.49900000000000944 ) ;
#31602=DIRECTION ( 'NONE',  ( 0.000000000000000000, 0.2334453638558990629, 0.9723699203976782224 ) ) ;
#31605=VERTEX_POINT ( 'NONE', #10939 ) ;
#31607=CARTESIAN_POINT ( 'NONE',  ( 0.000000000000000000, 68.55367621811204515, -44.99326035065983120 ) ) ;
#31609=FACE_OUTER_BOUND ( 'NONE', #9350, .T. ) ;
#31611=DIRECTION ( 'NONE',  ( -1.000000000000000000, -0.000000000000000000, 0.000000000000000000 ) ) ;
#31613=DIRECTION ( 'NONE',  ( -1.000000000000000000, 0.000000000000000000, 0.000000000000000000 ) ) ;
#31615=CARTESIAN_POINT ( 'NONE',  ( 0.000000000000000000, 73.73191006444551476, 14.66109333815590254 ) ) ;
#31617=EDGE_CURVE ( 'NONE', #31521, #7935, #22193, .T. ) ;
#31622=AXIS2_PLACEMENT_3D ( 'NONE', #29256, #36592, #17979 ) ;
#31623=EDGE_CURVE ( 'NONE', #26795, #16364, #3591, .T. ) ;
#31627=LINE ( 'NONE', #23528, #2945 ) ;
#31628=DIRECTION ( 'NONE',  ( 0.000000000000000000, -0.8090169943749433434, 0.5877852522924787992 ) ) ;
#31637=EDGE_CURVE ( 'NONE', #24133, #35935, #28481, .T. ) ;
#31641=ADVANCED_FACE ( 'NONE', ( #18989 ), #37119, .T. ) ;
#31646=CARTESIAN_POINT ( 'NONE',  ( 0.000000000000000000, -8.840884882375609877, 74.65374052328647281 ) ) ;
#31650=VECTOR ( 'NONE', #20562, 999.9999999999998863 ) ;
#31658=FACE_OUTER_BOUND ( 'NONE', #4113, .T. ) ;
#31666=DIRECTION ( 'NONE',  ( -1.000000000000000000, 0.000000000000000000, 0.000000000000000000 ) ) ;
#31668=EDGE_LOOP ( 'NONE', ( #8211, #24085, #36551, #11473 ) ) ;
#31669=AXIS2_PLACEMENT_3D ( 'NONE', #41778, #30512, #1385 ) ;
#31671=CIRCLE ( 'NONE', #46386, 31.99999999999998579 ) ;
#31675=DIRECTION ( 'NONE',  ( 0.000000000000000000, 0.5224985647159440250, 0.8526401643540951758 ) ) ;
#31677=DIRECTION ( 'NONE',  ( 0.000000000000000000, 0.000000000000000000, 1.000000000000000000 ) ) ;
#31681=LINE ( 'NONE', #16730, #9575 ) ;
#31682=DIRECTION ( 'NONE',  ( 0.000000000000000000, 0.000000000000000000, 1.000000000000000000 ) ) ;
#31684=DIRECTION ( 'NONE',  ( -1.000000000000000000, 0.000000000000000000, 0.000000000000000000 ) ) ;
#31689=CARTESIAN_POINT ( 'NONE',  ( 0.000000000000000000, 62.50884508063487033, -41.76106447765422303 ) ) ;
#31690=DIRECTION ( 'NONE',  ( -1.000000000000000000, -0.000000000000000000, 0.000000000000000000 ) ) ;
#31691=EDGE_CURVE ( 'NONE', #24980, #2713, #1145, .T. ) ;
#31692=VERTEX_POINT ( 'NONE', #26107 ) ;
#31694=CARTESIAN_POINT ( 'NONE',  ( 12.00000000000000000, 16.83928648764922542, -16.46020748918050458 ) ) ;
#31698=DIRECTION ( 'NONE',  ( 0.000000000000000000, 0.000000000000000000, 1.000000000000000000 ) ) ;
#31703=AXIS2_PLACEMENT_3D ( 'NONE', #36739, #47523, #39953 ) ;
#31711=EDGE_CURVE ( 'NONE', #1147, #13754, #27717, .T. ) ;
#31712=AXIS2_PLACEMENT_3D ( 'NONE', #22071, #18875, #34717 ) ;
#31713=LINE ( 'NONE', #9396, #40151 ) ;
#31721=DIRECTION ( 'NONE',  ( 0.000000000000000000, 0.000000000000000000, 1.000000000000000000 ) ) ;
#31725=ORIENTED_EDGE ( 'NONE', *, *, #40243, .T. ) ;
#31732=CARTESIAN_POINT ( 'NONE',  ( 11.99999999999999822, -34.44570377933549565, -69.42325613327476219 ) ) ;
#31749=EDGE_CURVE ( 'NONE', #28312, #24194, #15098, .T. ) ;
#31751=FACE_OUTER_BOUND ( 'NONE', #46508, .T. ) ;
#31752=CYLINDRICAL_SURFACE ( 'NONE', #32643, 77.49899999999999523 ) ;
#31762=ORIENTED_EDGE ( 'NONE', *, *, #6794, .T. ) ;
#31763=ORIENTED_EDGE ( 'NONE', *, *, #23607, .T. ) ;
#31764=EDGE_CURVE ( 'NONE', #26074, #127, #23888, .T. ) ;
#31767=ORIENTED_EDGE ( 'NONE', *, *, #47183, .T. ) ;
#31769=CIRCLE ( 'NONE', #10649, 31.99999999999998934 ) ;
#31774=DIRECTION ( 'NONE',  ( -1.000000000000000000, 0.000000000000000000, 0.000000000000000000 ) ) ;
#31776=ORIENTED_EDGE ( 'NONE', *, *, #37000, .T. ) ;
#31783=PLANE ( 'NONE',  #878 ) ;
#31785=EDGE_LOOP ( 'NONE', ( #20189, #14860, #2599, #20231 ) ) ;
#31786=DIRECTION ( 'NONE',  ( -1.000000000000000000, -0.000000000000000000, -0.000000000000000000 ) ) ;
#31789=DIRECTION ( 'NONE',  ( 0.000000000000000000, -0.4539904997395541875, 0.8910065241883641241 ) ) ;
#31792=CARTESIAN_POINT ( 'NONE',  ( 11.99999999999999822, -30.41916302227062019, -71.27951684758059514 ) ) ;
#31793=CARTESIAN_POINT ( 'NONE',  ( 11.99999999999999822, -62.20884554314051229, 46.21855187248609553 ) ) ;
#31794=AXIS2_PLACEMENT_3D ( 'NONE', #6891, #36018, #36262 ) ;
#31796=ORIENTED_EDGE ( 'NONE', *, *, #2324, .T. ) ;
#31797=CYLINDRICAL_SURFACE ( 'NONE', #6325, 82.00000000000000000 ) ;
#31799=CARTESIAN_POINT ( 'NONE',  ( 11.99999999999999822, 59.03961581697465277, -46.53671651293886669 ) ) ;
#31814=EDGE_LOOP ( 'NONE', ( #11670, #43171, #21397, #12356 ) ) ;
#31817=CARTESIAN_POINT ( 'NONE',  ( 11.99999999999999822, 35.91791733033570466, -68.67312586194960033 ) ) ;
#31819=AXIS2_PLACEMENT_3D ( 'NONE', #35750, #2217, #22007 ) ;
#31824=AXIS2_PLACEMENT_3D ( 'NONE', #1194, #46227, #31074 ) ;
#31835=ORIENTED_EDGE ( 'NONE', *, *, #42243, .F. ) ;
#31841=CARTESIAN_POINT ( 'NONE',  ( 0.000000000000000000, 0.000000000000000000, 0.000000000000000000 ) ) ;
#31845=ORIENTED_EDGE ( 'NONE', *, *, #20889, .T. ) ;
#31853=ORIENTED_EDGE ( 'NONE', *, *, #12310, .T. ) ;
#31861=EDGE_CURVE ( 'NONE', #9412, #38298, #18363, .T. ) ;
#31862=DIRECTION ( 'NONE',  ( 0.000000000000000000, 0.000000000000000000, 1.000000000000000000 ) ) ;
#31863=AXIS2_PLACEMENT_3D ( 'NONE', #32911, #47837, #6743 ) ;
#31864=DIRECTION ( 'NONE',  ( -1.000000000000000000, 0.000000000000000000, 0.000000000000000000 ) ) ;
#31868=ORIENTED_EDGE ( 'NONE', *, *, #42329, .T. ) ;
#31870=DIRECTION ( 'NONE',  ( 0.000000000000000000, -0.3826834323650969427, 0.9238795325112837409 ) ) ;
#31882=CARTESIAN_POINT ( 'NONE',  ( 12.00000000000000000, -11.95096189432312350, 23.69967320028773017 ) ) ;
#31889=DIRECTION ( 'NONE',  ( -1.000000000000000000, 0.000000000000000000, -0.000000000000000000 ) ) ;
#31890=VERTEX_POINT ( 'NONE', #40273 ) ;
#31892=AXIS2_PLACEMENT_3D ( 'NONE', #39443, #14205, #22277 ) ;
#31894=DIRECTION ( 'NONE',  ( 0.000000000000000000, 0.000000000000000000, 1.000000000000000000 ) ) ;
#31895=CARTESIAN_POINT ( 'NONE',  ( 15.00000000000000000, -14.54903810567644484, 22.19967320028775504 ) ) ;
#31897=DIRECTION ( 'NONE',  ( -0.000000000000000000, -0.3090169943749572767, -0.9510565162951503115 ) ) ;
#31898=ORIENTED_EDGE ( 'NONE', *, *, #45402, .F. ) ;
#31902=FACE_OUTER_BOUND ( 'NONE', #7619, .T. ) ;
#31910=CARTESIAN_POINT ( 'NONE',  ( 11.99999999999999822, 29.01471420065673712, -76.69515212745983490 ) ) ;
#31911=ORIENTED_EDGE ( 'NONE', *, *, #19761, .F. ) ;
#31913=DIRECTION ( 'NONE',  ( -1.000000000000000000, 0.000000000000000000, 0.000000000000000000 ) ) ;
#31916=ORIENTED_EDGE ( 'NONE', *, *, #8657, .T. ) ;
#31917=FACE_OUTER_BOUND ( 'NONE', #30714, .T. ) ;
#31920=CARTESIAN_POINT ( 'NONE',  ( 5.999999999999999112, -21.60688246758642705, 79.10210256391358996 ) ) ;
#31922=EDGE_CURVE ( 'NONE', #5004, #33903, #13353, .T. ) ;
#31930=CARTESIAN_POINT ( 'NONE',  ( 0.000000000000000000, 71.87247863392413194, 39.47590169984871267 ) ) ;
#31931=CARTESIAN_POINT ( 'NONE',  ( 5.999999999999999112, 71.21200624218795383, 40.65526001592638039 ) ) ;
#31934=ORIENTED_EDGE ( 'NONE', *, *, #8221, .T. ) ;
#31936=EDGE_CURVE ( 'NONE', #14753, #5918, #22287, .T. ) ;
#31938=ORIENTED_EDGE ( 'NONE', *, *, #26790, .T. ) ;
#31941=VERTEX_POINT ( 'NONE', #17244 ) ;
#31942=VECTOR ( 'NONE', #16998, 1000.000000000000000 ) ;
#31948=CARTESIAN_POINT ( 'NONE',  ( 6.000000000000000000, 29.01471420065673712, -76.69515212745984911 ) ) ;
#31957=DIRECTION ( 'NONE',  ( 0.000000000000000000, 0.000000000000000000, 1.000000000000000000 ) ) ;
#31958=CARTESIAN_POINT ( 'NONE',  ( 0.000000000000000000, 0.000000000000000000, 0.000000000000000000 ) ) ;
#31959=VERTEX_POINT ( 'NONE', #20939 ) ;
#31961=LINE ( 'NONE', #43454, #4493 ) ;
#31967=CARTESIAN_POINT ( 'NONE',  ( 6.000000000000000000, 68.55367621811204515, -44.99326035065983120 ) ) ;
#31974=CARTESIAN_POINT ( 'NONE',  ( 15.00000000000000000, 16.83928648764945635, 16.46020748918027010 ) ) ;
#31977=DIRECTION ( 'NONE',  ( 0.000000000000000000, 0.000000000000000000, 1.000000000000000000 ) ) ;
#31978=AXIS2_PLACEMENT_3D ( 'NONE', #35462, #1953, #16874 ) ;
#31984=CARTESIAN_POINT ( 'NONE',  ( 12.00000000000000000, 6.762365576493310826, -25.66652317338400735 ) ) ;
#31987=DIRECTION ( 'NONE',  ( 0.000000000000000000, 0.000000000000000000, 1.000000000000000000 ) ) ;
#31988=DIRECTION ( 'NONE',  ( 0.000000000000000000, -0.4999999999999920064, 0.8660254037844432595 ) ) ;
#31994=ORIENTED_EDGE ( 'NONE', *, *, #25576, .F. ) ;
#32001=CARTESIAN_POINT ( 'NONE',  ( 11.99999999999999822, 0.000000000000000000, 0.000000000000000000 ) ) ;
#32004=ORIENTED_EDGE ( 'NONE', *, *, #18278, .F. ) ;
#32010=CARTESIAN_POINT ( 'NONE',  ( 0.000000000000000000, -75.11725578898470701, 2.956366410620372864 ) ) ;
#32014=ORIENTED_EDGE ( 'NONE', *, *, #14151, .T. ) ;
#32016=ORIENTED_EDGE ( 'NONE', *, *, #45602, .T. ) ;
#32018=DIRECTION ( 'NONE',  ( -1.000000000000000000, -0.000000000000000000, -0.000000000000000000 ) ) ;
#32023=EDGE_CURVE ( 'NONE', #45952, #44798, #25607, .T. ) ;
#32027=ORIENTED_EDGE ( 'NONE', *, *, #46299, .T. ) ;
#32032=CARTESIAN_POINT ( 'NONE',  ( 0.000000000000000000, 0.000000000000000000, 0.000000000000000000 ) ) ;
#32036=CARTESIAN_POINT ( 'NONE',  ( -10.00000000000000000, 0.000000000000000000, 0.000000000000000000 ) ) ;
#32038=AXIS2_PLACEMENT_3D ( 'NONE', #1737, #20565, #8825 ) ;
#32039=ORIENTED_EDGE ( 'NONE', *, *, #16928, .T. ) ;
#32040=PLANE ( 'NONE',  #24711 ) ;
#32043=CARTESIAN_POINT ( 'NONE',  ( 0.000000000000000000, 74.18225833017888249, 34.94270380257665209 ) ) ;
#32045=LINE ( 'NONE', #17319, #34654 ) ;
#32052=EDGE_LOOP ( 'NONE', ( #6829, #5806, #5731, #19556 ) ) ;
#32056=EDGE_CURVE ( 'NONE', #40015, #36455, #23830, .T. ) ;
#32061=CIRCLE ( 'NONE', #4697, 31.99999999999998579 ) ;
#32063=EDGE_CURVE ( 'NONE', #44520, #45891, #22904, .T. ) ;
#32064=CIRCLE ( 'NONE', #16397, 31.99999999999998579 ) ;
#32065=ORIENTED_EDGE ( 'NONE', *, *, #27385, .T. ) ;
#32067=EDGE_CURVE ( 'NONE', #28383, #13636, #41026, .T. ) ;
#32073=DIRECTION ( 'NONE',  ( 0.000000000000000000, 0.07845909572783793529, 0.9969173337331285190 ) ) ;
#32077=LINE ( 'NONE', #28639, #17265 ) ;
#32083=VERTEX_POINT ( 'NONE', #15089 ) ;
#32095=ADVANCED_FACE ( 'NONE', ( #41281 ), #33913, .T. ) ;
#32098=VERTEX_POINT ( 'NONE', #14618 ) ;
#32100=AXIS2_PLACEMENT_3D ( 'NONE', #23612, #38556, #8209 ) ;
#32101=EDGE_CURVE ( 'NONE', #19662, #35253, #36327, .T. ) ;
#32106=CARTESIAN_POINT ( 'NONE',  ( 0.000000000000000000, 0.000000000000000000, 0.000000000000000000 ) ) ;
#32110=EDGE_CURVE ( 'NONE', #5207, #18512, #12904, .T. ) ;
#32120=DIRECTION ( 'NONE',  ( 0.000000000000000000, -0.07845909572783058006, -0.9969173337331290741 ) ) ;
#32125=ORIENTED_EDGE ( 'NONE', *, *, #21320, .T. ) ;
#32131=CARTESIAN_POINT ( 'NONE',  ( -10.00000000000000000, 0.000000000000000000, 0.000000000000000000 ) ) ;
#32132=CARTESIAN_POINT ( 'NONE',  ( 11.99999999999999822, 23.16143007188426850, 73.95703589263983702 ) ) ;
#32136=VERTEX_POINT ( 'NONE', #3330 ) ;
#32138=DIRECTION ( 'NONE',  ( 0.000000000000000000, -1.000000000000000000, -1.047444401652940007E-14 ) ) ;
#32141=LINE ( 'NONE', #32834, #44608 ) ;
#32144=DIRECTION ( 'NONE',  ( 0.000000000000000000, 0.000000000000000000, 1.000000000000000000 ) ) ;
#32162=EDGE_CURVE ( 'NONE', #28196, #2440, #23083, .T. ) ;
#32164=ORIENTED_EDGE ( 'NONE', *, *, #645, .T. ) ;
#32166=AXIS2_PLACEMENT_3D ( 'NONE', #8274, #8995, #5334 ) ;
#32173=ADVANCED_FACE ( 'NONE', ( #23383 ), #42233, .T. ) ;
#32174=EDGE_CURVE ( 'NONE', #47607, #35673, #28582, .T. ) ;
#32176=DIRECTION ( 'NONE',  ( 0.000000000000000000, 0.3090169943749450088, -0.9510565162951543083 ) ) ;
#32179=CARTESIAN_POINT ( 'NONE',  ( 0.000000000000000000, 63.18004540533029001, 44.88180994100398635 ) ) ;
#32183=CARTESIAN_POINT ( 'NONE',  ( 6.000000000000000000, -8.966570791701288456, 81.50828551894223040 ) ) ;
#32186=DIRECTION ( 'NONE',  ( -1.000000000000000000, 0.000000000000000000, 0.000000000000000000 ) ) ;
#32189=ORIENTED_EDGE ( 'NONE', *, *, #31077, .F. ) ;
#32191=EDGE_LOOP ( 'NONE', ( #15308, #36552, #9653, #25815 ) ) ;
#32193=ADVANCED_FACE ( 'NONE', ( #35120 ), #39048, .T. ) ;
#32196=CARTESIAN_POINT ( 'NONE',  ( 0.000000000000000000, 55.19960302592141232, -51.03279382321027668 ) ) ;
#32197=CYLINDRICAL_SURFACE ( 'NONE', #13564, 77.49899999999999523 ) ;
#32202=VECTOR ( 'NONE', #20566, 1000.000000000000000 ) ;
#32208=DIRECTION ( 'NONE',  ( 0.000000000000000000, 0.000000000000000000, 1.000000000000000000 ) ) ;
#32209=AXIS2_PLACEMENT_3D ( 'NONE', #14723, #10806, #7123 ) ;
#32212=CIRCLE ( 'NONE', #22832, 31.99999999999998579 ) ;
#32218=CARTESIAN_POINT ( 'NONE',  ( 0.000000000000000000, 80.55351364060611274, -15.33399622253397609 ) ) ;
#32220=ADVANCED_FACE ( 'NONE', ( #46156 ), #16532, .T. ) ;
#32231=EDGE_CURVE ( 'NONE', #48059, #24460, #34819, .T. ) ;
#32233=CARTESIAN_POINT ( 'NONE',  ( 0.000000000000000000, 77.16300072079660310, 27.74655509720697211 ) ) ;
#32239=CYLINDRICAL_SURFACE ( 'NONE', #17036, 77.49899999999999523 ) ;
#32241=DIRECTION ( 'NONE',  ( 0.000000000000000000, 0.000000000000000000, 1.000000000000000000 ) ) ;
#32247=ORIENTED_EDGE ( 'NONE', *, *, #507, .T. ) ;
#32250=AXIS2_PLACEMENT_3D ( 'NONE', #16560, #45222, #26615 ) ;
#32261=FACE_OUTER_BOUND ( 'NONE', #27404, .T. ) ;
#32266=VECTOR ( 'NONE', #37722, 1000.000000000000000 ) ;
#32268=EDGE_CURVE ( 'NONE', #35892, #40544, #5106, .T. ) ;
#32271=DIRECTION ( 'NONE',  ( 0.000000000000000000, 0.9510565162951523099, 0.3090169943749514481 ) ) ;
#32273=AXIS2_PLACEMENT_3D ( 'NONE', #1428, #12684, #1663 ) ;
#32275=ADVANCED_FACE ( 'NONE', ( #30493 ), #45416, .T. ) ;
#32276=CIRCLE ( 'NONE', #8047, 31.99999999999998579 ) ;
#32279=AXIS2_PLACEMENT_3D ( 'NONE', #37846, #1612, #16538 ) ;
#32280=VECTOR ( 'NONE', #27050, 1000.000000000000000 ) ;
#32282=DIRECTION ( 'NONE',  ( -1.000000000000000000, -0.000000000000000000, -0.000000000000000000 ) ) ;
#32285=EDGE_CURVE ( 'NONE', #17381, #19503, #14060, .T. ) ;
#32288=ORIENTED_EDGE ( 'NONE', *, *, #11066, .T. ) ;
#32291=VECTOR ( 'NONE', #13027, 1000.000000000000000 ) ;
#32298=CARTESIAN_POINT ( 'NONE',  ( 15.00000000000000000, 24.81905959214275370, 9.408202855044498492 ) ) ;
#32299=AXIS2_PLACEMENT_3D ( 'NONE', #22047, #36978, #3450 ) ;
#32301=DIRECTION ( 'NONE',  ( -1.000000000000000000, 0.000000000000000000, 0.000000000000000000 ) ) ;
#32306=VERTEX_POINT ( 'NONE', #36335 ) ;
#32307=DIRECTION ( 'NONE',  ( 0.000000000000000000, -0.4067366430757887730, 0.9135454576426059736 ) ) ;
#32309=AXIS2_PLACEMENT_3D ( 'NONE', #45872, #42426, #23338 ) ;
#32310=ORIENTED_EDGE ( 'NONE', *, *, #24289, .F. ) ;
#32317=CARTESIAN_POINT ( 'NONE',  ( 11.99999999999999822, -46.21855187248585395, -62.20884554314068993 ) ) ;
#32320=CARTESIAN_POINT ( 'NONE',  ( 12.00000000000000000, -26.23277895567245466, 4.042438405570107918 ) ) ;
#32321=AXIS2_PLACEMENT_3D ( 'NONE', #46625, #5999, #12604 ) ;
#32325=EDGE_CURVE ( 'NONE', #42578, #15938, #46642, .T. ) ;
#32329=EDGE_CURVE ( 'NONE', #12921, #31098, #22331, .T. ) ;
#32331=FACE_OUTER_BOUND ( 'NONE', #3629, .T. ) ;
#32332=EDGE_CURVE ( 'NONE', #23927, #5207, #30121, .T. ) ;
#32341=AXIS2_PLACEMENT_3D ( 'NONE', #18518, #7012, #32719 ) ;
#32342=AXIS2_PLACEMENT_3D ( 'NONE', #16438, #23534, #38473 ) ;
#32346=EDGE_CURVE ( 'NONE', #42296, #20697, #16780, .T. ) ;
#32352=EDGE_LOOP ( 'NONE', ( #27867, #30854, #8198, #3329 ) ) ;
#32354=VERTEX_POINT ( 'NONE', #2549 ) ;
#32361=VERTEX_POINT ( 'NONE', #32434 ) ;
#32369=CIRCLE ( 'NONE', #37033, 82.00000000000000000 ) ;
#32371=ORIENTED_EDGE ( 'NONE', *, *, #28127, .F. ) ;
#32374=ORIENTED_EDGE ( 'NONE', *, *, #31922, .F. ) ;
#32375=AXIS2_PLACEMENT_3D ( 'NONE', #37916, #8294, #26420 ) ;
#32376=DIRECTION ( 'NONE',  ( -1.000000000000000000, 0.000000000000000000, -0.000000000000000000 ) ) ;
#32380=CARTESIAN_POINT ( 'NONE',  ( 11.99999999999999822, -8.830959090342926032, 74.65491531819115778 ) ) ;
#32381=DIRECTION ( 'NONE',  ( 0.000000000000000000, 0.8910065241883656784, 0.4539904997395511344 ) ) ;
#32382=ORIENTED_EDGE ( 'NONE', *, *, #37750, .T. ) ;
#32385=CARTESIAN_POINT ( 'NONE',  ( 11.99999999999999822, -2.543863470247810010, -81.96053171279903893 ) ) ;
#32386=CARTESIAN_POINT ( 'NONE',  ( 0.000000000000000000, 44.99326035066149387, -68.55367621811095091 ) ) ;
#32388=AXIS2_PLACEMENT_3D ( 'NONE', #1808, #2281, #9871 ) ;
#32389=CARTESIAN_POINT ( 'NONE',  ( 0.000000000000000000, -71.91182617369167929, -28.89263327155821059 ) ) ;
#32395=CIRCLE ( 'NONE', #21436, 31.99999999999998934 ) ;
#32401=CARTESIAN_POINT ( 'NONE',  ( 12.00000000000000000, 20.85821328998741109, -10.92862929874522671 ) ) ;
#32402=ORIENTED_EDGE ( 'NONE', *, *, #20960, .F. ) ;
#32405=CIRCLE ( 'NONE', #11295, 77.49899999999999523 ) ;
#32407=ORIENTED_EDGE ( 'NONE', *, *, #31414, .T. ) ;
#32418=DIRECTION ( 'NONE',  ( 0.000000000000000000, -0.07845909572785224328, 0.9969173337331274087 ) ) ;
#32419=CIRCLE ( 'NONE', #28503, 82.00000000000000000 ) ;
#32423=LINE ( 'NONE', #47352, #35593 ) ;
#32424=AXIS2_PLACEMENT_3D ( 'NONE', #45541, #1492, #41639 ) ;
#32434=CARTESIAN_POINT ( 'NONE',  ( 15.00000000000000000, 26.50000000000000355, -1.500000000000000000 ) ) ;
#32440=CARTESIAN_POINT ( 'NONE',  ( 11.99999999999999822, 76.66974797899852945, -11.30684508768257679 ) ) ;
#32442=DIRECTION ( 'NONE',  ( 0.000000000000000000, -0.8910065241883722287, 0.4539904997395383113 ) ) ;
#32444=CARTESIAN_POINT ( 'NONE',  ( 11.99999999999999822, 18.89407956138362010, -75.16055320797013906 ) ) ;
#32445=VERTEX_POINT ( 'NONE', #33856 ) ;
#32448=EDGE_CURVE ( 'NONE', #38691, #10422, #21514, .T. ) ;
#32452=EDGE_CURVE ( 'NONE', #9566, #37777, #34012, .T. ) ;
#32454=VECTOR ( 'NONE', #15498, 1000.000000000000000 ) ;
#32458=ORIENTED_EDGE ( 'NONE', *, *, #506, .F. ) ;
#32463=LINE ( 'NONE', #28780, #19711 ) ;
#32464=ORIENTED_EDGE ( 'NONE', *, *, #25216, .T. ) ;
#32468=CARTESIAN_POINT ( 'NONE',  ( 11.99999999999999822, 0.000000000000000000, 0.000000000000000000 ) ) ;
#32470=ORIENTED_EDGE ( 'NONE', *, *, #24318, .F. ) ;
#32485=DIRECTION ( 'NONE',  ( 1.000000000000000000, 0.000000000000000000, 0.000000000000000000 ) ) ;
#32487=DIRECTION ( 'NONE',  ( -1.000000000000000000, -0.000000000000000000, -0.000000000000000000 ) ) ;
#32491=CARTESIAN_POINT ( 'NONE',  ( 12.00000000000000000, 20.85821328998756385, 10.92862929874494249 ) ) ;
#32494=AXIS2_PLACEMENT_3D ( 'NONE', #45865, #30940, #30677 ) ;
#32497=CARTESIAN_POINT ( 'NONE',  ( 11.99999999999999822, 75.11725578898472122, -2.956366410619845730 ) ) ;
#32501=FACE_OUTER_BOUND ( 'NONE', #38849, .T. ) ;
#32508=EDGE_CURVE ( 'NONE', #2713, #4855, #44232, .T. ) ;
#32510=CARTESIAN_POINT ( 'NONE',  ( 11.99999999999999822, -76.41127070299262414, -12.93880638057396304 ) ) ;
#32514=CARTESIAN_POINT ( 'NONE',  ( 5.999999999999999112, -77.16300072079681627, 27.74655509720641433 ) ) ;
#32515=CARTESIAN_POINT ( 'NONE',  ( 0.000000000000000000, 58.39081064771822582, -50.95692526931267707 ) ) ;
#32516=CARTESIAN_POINT ( 'NONE',  ( 0.000000000000000000, 27.74655509720669500, 77.16300072079670258 ) ) ;
#32518=DIRECTION ( 'NONE',  ( -1.000000000000000000, -0.000000000000000000, -0.000000000000000000 ) ) ;
#32521=CIRCLE ( 'NONE', #30189, 31.99999999999998224 ) ;
#32523=DIRECTION ( 'NONE',  ( 0.000000000000000000, 0.000000000000000000, 1.000000000000000000 ) ) ;
#32526=CARTESIAN_POINT ( 'NONE',  ( 11.99999999999999822, 0.000000000000000000, 0.000000000000000000 ) ) ;
#32529=AXIS2_PLACEMENT_3D ( 'NONE', #14994, #30638, #12048 ) ;
#32532=AXIS2_PLACEMENT_3D ( 'NONE', #21287, #32783, #37193 ) ;
#32542=EDGE_CURVE ( 'NONE', #29567, #22296, #4373, .T. ) ;
#32550=ORIENTED_EDGE ( 'NONE', *, *, #34864, .T. ) ;
#32551=DIRECTION ( 'NONE',  ( -1.000000000000000000, -0.000000000000000000, -0.000000000000000000 ) ) ;
#32556=CIRCLE ( 'NONE', #11467, 77.49900000000002365 ) ;
#32557=DIRECTION ( 'NONE',  ( -1.000000000000000000, 0.000000000000000000, -0.000000000000000000 ) ) ;
#32560=ADVANCED_FACE ( 'NONE', ( #23332 ), #34329, .T. ) ;
#32563=ORIENTED_EDGE ( 'NONE', *, *, #15106, .T. ) ;
#32565=CARTESIAN_POINT ( 'NONE',  ( 0.000000000000000000, 21.60688246758586928, 79.10210256391376049 ) ) ;
#32566=CARTESIAN_POINT ( 'NONE',  ( 11.99999999999999822, -75.11764819372149304, 2.946379043146075905 ) ) ;
#32571=ADVANCED_FACE ( 'NONE', ( #581 ), #8630, .T. ) ;
#32572=VECTOR ( 'NONE', #47655, 1000.000000000000000 ) ;
#32580=CIRCLE ( 'NONE', #15410, 31.99999999999998579 ) ;
#32583=CARTESIAN_POINT ( 'NONE',  ( 15.00000000000000000, -3.948201729842355068, -23.21447184625292692 ) ) ;
#32587=ADVANCED_FACE ( 'NONE', ( #23096 ), #4500, .T. ) ;
#32588=CARTESIAN_POINT ( 'NONE',  ( 11.99999999999999822, 0.000000000000000000, 0.000000000000000000 ) ) ;
#32589=ORIENTED_EDGE ( 'NONE', *, *, #47155, .T. ) ;
#32595=VECTOR ( 'NONE', #6498, 1000.000000000000114 ) ;
#32598=CARTESIAN_POINT ( 'NONE',  ( -10.00000000000000000, 0.000000000000000000, 0.000000000000000000 ) ) ;
#32599=EDGE_LOOP ( 'NONE', ( #14533, #9218, #4273, #45821 ) ) ;
#32608=DIRECTION ( 'NONE',  ( -1.000000000000000000, -0.000000000000000000, -0.000000000000000000 ) ) ;
#32610=LINE ( 'NONE', #21098, #27697 ) ;
#32613=LINE ( 'NONE', #32838, #29803 ) ;
#32617=ORIENTED_EDGE ( 'NONE', *, *, #4919, .F. ) ;
#32621=DIRECTION ( 'NONE',  ( -1.000000000000000000, 0.000000000000000000, 0.000000000000000000 ) ) ;
#32628=CYLINDRICAL_SURFACE ( 'NONE', #45682, 31.99999999999998579 ) ;
#32632=FACE_OUTER_BOUND ( 'NONE', #43230, .T. ) ;
#32633=EDGE_LOOP ( 'NONE', ( #31898, #24684, #13814, #45112 ) ) ;
#32636=ORIENTED_EDGE ( 'NONE', *, *, #25228, .T. ) ;
#32640=DIRECTION ( 'NONE',  ( 0.000000000000000000, 0.000000000000000000, 1.000000000000000000 ) ) ;
#32641=FACE_OUTER_BOUND ( 'NONE', #28509, .T. ) ;
#32643=AXIS2_PLACEMENT_3D ( 'NONE', #16801, #35141, #1624 ) ;
#32646=ORIENTED_EDGE ( 'NONE', *, *, #4342, .T. ) ;
#32651=VERTEX_POINT ( 'NONE', #1312 ) ;
#32652=ADVANCED_FACE ( 'NONE', ( #31178 ), #46098, .F. ) ;
#32657=DIRECTION ( 'NONE',  ( -1.000000000000000000, 0.000000000000000000, 0.000000000000000000 ) ) ;
#32670=VERTEX_POINT ( 'NONE', #31910 ) ;
#32678=CARTESIAN_POINT ( 'NONE',  ( 12.00000000000000000, -1.278221433540507768, -26.51162292216071492 ) ) ;
#32685=EDGE_LOOP ( 'NONE', ( #6772, #40413, #31395, #26948 ) ) ;
#32686=ORIENTED_EDGE ( 'NONE', *, *, #4429, .F. ) ;
#32687=ADVANCED_FACE ( 'NONE', ( #20621 ), #28704, .T. ) ;
#32692=AXIS2_PLACEMENT_3D ( 'NONE', #27552, #1369, #45667 ) ;
#32694=CARTESIAN_POINT ( 'NONE',  ( 15.00000000000000000, -4.261787119644963262, 26.19803753235780164 ) ) ;
#32695=EDGE_CURVE ( 'NONE', #39278, #34677, #25010, .T. ) ;
#32701=EDGE_CURVE ( 'NONE', #25362, #45891, #443, .T. ) ;
#32706=CARTESIAN_POINT ( 'NONE',  ( 0.000000000000000000, 0.000000000000000000, 0.000000000000000000 ) ) ;
#32707=ORIENTED_EDGE ( 'NONE', *, *, #17886, .F. ) ;
#32712=CARTESIAN_POINT ( 'NONE',  ( 0.000000000000000000, 76.69515212746016175, 29.01471420065590578 ) ) ;
#32713=VECTOR ( 'NONE', #24696, 1000.000000000000000 ) ;
#32714=CARTESIAN_POINT ( 'NONE',  ( 11.99999999999999822, 20.41045688087824317, 72.35160999960824313 ) ) ;
#32719=DIRECTION ( 'NONE',  ( 0.000000000000000000, 0.9969173337331276308, 0.07845909572784874608 ) ) ;
#32725=VERTEX_POINT ( 'NONE', #1787 ) ;
#32726=CARTESIAN_POINT ( 'NONE',  ( 11.99999999999999822, 73.72996012237440766, 14.67089635893739619 ) ) ;
#32729=FACE_OUTER_BOUND ( 'NONE', #37813, .T. ) ;
#32731=AXIS2_PLACEMENT_3D ( 'NONE', #28169, #24748, #6386 ) ;
#32735=DIRECTION ( 'NONE',  ( -1.000000000000000000, -0.000000000000000000, 0.000000000000000000 ) ) ;
#32736=DIRECTION ( 'NONE',  ( 1.000000000000000000, -0.000000000000000000, -0.000000000000000000 ) ) ;
#32740=AXIS2_PLACEMENT_3D ( 'NONE', #3123, #10485, #36434 ) ;
#32743=CIRCLE ( 'NONE', #11658, 31.99999999999999645 ) ;
#32746=AXIS2_PLACEMENT_3D ( 'NONE', #11365, #795, #29467 ) ;
#32748=CYLINDRICAL_SURFACE ( 'NONE', #6215, 77.49899999999999523 ) ;
#32751=EDGE_CURVE ( 'NONE', #40605, #43691, #30971, .T. ) ;
#32752=EDGE_CURVE ( 'NONE', #28743, #38129, #41131, .T. ) ;
#32753=EDGE_CURVE ( 'NONE', #23167, #19565, #9851, .T. ) ;
#32758=EDGE_CURVE ( 'NONE', #22722, #4498, #26240, .T. ) ;
#32760=EDGE_CURVE ( 'NONE', #44059, #29462, #9594, .T. ) ;
#32761=LINE ( 'NONE', #36675, #417 ) ;
#32765=CARTESIAN_POINT ( 'NONE',  ( 11.99999999999999822, -75.11725578898466438, -2.956366410621452001 ) ) ;
#32766=CIRCLE ( 'NONE', #29630, 82.00000000000000000 ) ;
#32772=CARTESIAN_POINT ( 'NONE',  ( 0.000000000000000000, 74.18225833017937987, -34.94270380257559339 ) ) ;
#32773=VERTEX_POINT ( 'NONE', #6186 ) ;
#32774=ORIENTED_EDGE ( 'NONE', *, *, #25734, .F. ) ;
#32778=FACE_OUTER_BOUND ( 'NONE', #16639, .T. ) ;
#32781=CARTESIAN_POINT ( 'NONE',  ( 11.99999999999999822, -67.80270845531921964, 46.11716303203162681 ) ) ;
#32783=DIRECTION ( 'NONE',  ( -1.000000000000000000, -0.000000000000000000, -0.000000000000000000 ) ) ;
#32784=AXIS2_PLACEMENT_3D ( 'NONE', #18681, #36800, #37530 ) ;
#32790=ORIENTED_EDGE ( 'NONE', *, *, #44960, .F. ) ;
#32793=EDGE_CURVE ( 'NONE', #30536, #24231, #47529, .T. ) ;
#32796=DIRECTION ( 'NONE',  ( -1.000000000000000000, 0.000000000000000000, -0.000000000000000000 ) ) ;
#32801=CARTESIAN_POINT ( 'NONE',  ( 0.000000000000000000, 0.000000000000000000, 0.000000000000000000 ) ) ;
#32802=ORIENTED_EDGE ( 'NONE', *, *, #4762, .F. ) ;
#32804=AXIS2_PLACEMENT_3D ( 'NONE', #26936, #38185, #19798 ) ;
#32806=AXIS2_PLACEMENT_3D ( 'NONE', #47174, #47885, #40558 ) ;
#32809=DIRECTION ( 'NONE',  ( -1.000000000000000000, -0.000000000000000000, 0.000000000000000000 ) ) ;
#32817=ORIENTED_EDGE ( 'NONE', *, *, #39654, .T. ) ;
#32822=EDGE_CURVE ( 'NONE', #34540, #32940, #36325, .T. ) ;
#32825=DIRECTION ( 'NONE',  ( 0.000000000000000000, 0.000000000000000000, 1.000000000000000000 ) ) ;
#32827=CYLINDRICAL_SURFACE ( 'NONE', #47494, 31.99999999999998579 ) ;
#32831=DIRECTION ( 'NONE',  ( -1.000000000000000000, 0.000000000000000000, -0.000000000000000000 ) ) ;
#32834=CARTESIAN_POINT ( 'NONE',  ( 6.000000000000000000, -34.94270380257692921, 74.18225833017875459 ) ) ;
#32838=CARTESIAN_POINT ( 'NONE',  ( 12.00000000000000000, -3.948201729842032215, 23.21447184625297666 ) ) ;
#32839=DIRECTION ( 'NONE',  ( 0.000000000000000000, 0.000000000000000000, 1.000000000000000000 ) ) ;
#32841=VECTOR ( 'NONE', #46804, 1000.000000000000000 ) ;
#32842=LINE ( 'NONE', #28933, #19947 ) ;
#32845=CYLINDRICAL_SURFACE ( 'NONE', #15360, 77.49899999999999523 ) ;
#32850=CARTESIAN_POINT ( 'NONE',  ( 11.99999999999999822, 68.26794271651262136, 31.47745569255165066 ) ) ;
#32851=CARTESIAN_POINT ( 'NONE',  ( 5.999999999999999112, -50.23322058963393744, 64.81221759200325039 ) ) ;
#32855=ORIENTED_EDGE ( 'NONE', *, *, #3967, .F. ) ;
#32856=ADVANCED_FACE ( 'NONE', ( #44827 ), #44103, .T. ) ;
#32859=ORIENTED_EDGE ( 'NONE', *, *, #44100, .F. ) ;
#32863=EDGE_CURVE ( 'NONE', #4472, #45870, #2978, .T. ) ;
#32865=CARTESIAN_POINT ( 'NONE',  ( 11.99999999999999822, 72.35160999960817207, 20.41045688087850607 ) ) ;
#32870=AXIS2_PLACEMENT_3D ( 'NONE', #22616, #18210, #92 ) ;
#32872=ORIENTED_EDGE ( 'NONE', *, *, #44203, .F. ) ;
#32874=EDGE_CURVE ( 'NONE', #46628, #40605, #29312, .T. ) ;
#32884=DIRECTION ( 'NONE',  ( 0.000000000000000000, -0.8090169943749503378, -0.5877852522924690293 ) ) ;
#32897=ORIENTED_EDGE ( 'NONE', *, *, #15003, .F. ) ;
#32898=FACE_OUTER_BOUND ( 'NONE', #46064, .T. ) ;
#32902=LINE ( 'NONE', #31974, #14532 ) ;
#32904=ORIENTED_EDGE ( 'NONE', *, *, #16601, .T. ) ;
#32909=AXIS2_PLACEMENT_3D ( 'NONE', #26722, #23045, #26971 ) ;
#32911=CARTESIAN_POINT ( 'NONE',  ( 11.99999999999999822, 0.000000000000000000, 0.000000000000000000 ) ) ;
#32912=CARTESIAN_POINT ( 'NONE',  ( 11.99999999999999822, 14.66109333815564852, -73.73191006444555740 ) ) ;
#32914=ORIENTED_EDGE ( 'NONE', *, *, #4585, .F. ) ;
#32916=AXIS2_PLACEMENT_3D ( 'NONE', #15093, #19700, #19241 ) ;
#32919=CARTESIAN_POINT ( 'NONE',  ( 11.99999999999999822, 20.40083707022987625, -72.35432306680462489 ) ) ;
#32920=EDGE_CURVE ( 'NONE', #46892, #12455, #40204, .T. ) ;
#32921=AXIS2_PLACEMENT_3D ( 'NONE', #6364, #28860, #44036 ) ;
#32928=AXIS2_PLACEMENT_3D ( 'NONE', #46265, #19814, #24224 ) ;
#32931=ORIENTED_EDGE ( 'NONE', *, *, #10395, .T. ) ;
#32936=ORIENTED_EDGE ( 'NONE', *, *, #25086, .T. ) ;
#32937=DIRECTION ( 'NONE',  ( -1.000000000000000000, 0.000000000000000000, -0.000000000000000000 ) ) ;
#32938=ORIENTED_EDGE ( 'NONE', *, *, #11337, .T. ) ;
#32940=VERTEX_POINT ( 'NONE', #5174 ) ;
#32951=VECTOR ( 'NONE', #10309, 999.9999999999998863 ) ;
#32956=DIRECTION ( 'NONE',  ( 1.000000000000000000, 0.000000000000000000, 0.000000000000000000 ) ) ;
#32959=AXIS2_PLACEMENT_3D ( 'NONE', #31799, #9484, #46942 ) ;
#32969=ORIENTED_EDGE ( 'NONE', *, *, #9286, .T. ) ;
#32974=ADVANCED_FACE ( 'NONE', ( #30624 ), #4677, .T. ) ;
#32985=AXIS2_PLACEMENT_3D ( 'NONE', #29970, #348, #7464 ) ;
#32988=CIRCLE ( 'NONE', #26779, 31.99999999999998579 ) ;
#32994=CIRCLE ( 'NONE', #11914, 31.99999999999999289 ) ;
#32996=ORIENTED_EDGE ( 'NONE', *, *, #3986, .F. ) ;
#32999=CARTESIAN_POINT ( 'NONE',  ( 11.99999999999999822, 75.54627589209944460, 17.28742895386110945 ) ) ;
#33000=ORIENTED_EDGE ( 'NONE', *, *, #37682, .F. ) ;
#33006=VERTEX_POINT ( 'NONE', #4452 ) ;
#33010=AXIS2_PLACEMENT_3D ( 'NONE', #7383, #48004, #10818 ) ;
#33017=ORIENTED_EDGE ( 'NONE', *, *, #6802, .F. ) ;
#33020=DIRECTION ( 'NONE',  ( -1.000000000000000000, 0.000000000000000000, -0.000000000000000000 ) ) ;
#33025=EDGE_CURVE ( 'NONE', #10422, #40361, #30193, .T. ) ;
#33027=CYLINDRICAL_SURFACE ( 'NONE', #20796, 31.99999999999998579 ) ;
#33028=DIRECTION ( 'NONE',  ( -1.000000000000000000, -0.000000000000000000, -0.000000000000000000 ) ) ;
#33029=EDGE_CURVE ( 'NONE', #7137, #33736, #16418, .T. ) ;
#33031=DIRECTION ( 'NONE',  ( 0.000000000000000000, 0.7604059656000322631, -0.6494480483301821039 ) ) ;
#33036=ORIENTED_EDGE ( 'NONE', *, *, #39300, .F. ) ;
#33038=ORIENTED_EDGE ( 'NONE', *, *, #10061, .F. ) ;
#33039=EDGE_CURVE ( 'NONE', #1298, #22174, #21582, .T. ) ;
#33044=EDGE_CURVE ( 'NONE', #23927, #8722, #41895, .T. ) ;
#33047=VERTEX_POINT ( 'NONE', #6129 ) ;
#33050=CARTESIAN_POINT ( 'NONE',  ( 11.99999999999999822, -49.70050353004846500, -59.46389618802017907 ) ) ;
#33051=CIRCLE ( 'NONE', #26806, 77.49900000000002365 ) ;
#33058=EDGE_CURVE ( 'NONE', #3151, #46329, #34083, .T. ) ;
#33060=CIRCLE ( 'NONE', #1813, 82.00000000000000000 ) ;
#33063=AXIS2_PLACEMENT_3D ( 'NONE', #28728, #43174, #9388 ) ;
#33066=DIRECTION ( 'NONE',  ( -1.000000000000000000, 0.000000000000000000, 0.000000000000000000 ) ) ;
#33069=FACE_OUTER_BOUND ( 'NONE', #2246, .T. ) ;
#33076=ORIENTED_EDGE ( 'NONE', *, *, #9448, .T. ) ;
#33077=FACE_OUTER_BOUND ( 'NONE', #10585, .T. ) ;
#33079=EDGE_CURVE ( 'NONE', #43138, #9412, #10030, .T. ) ;
#33080=DIRECTION ( 'NONE',  ( 0.000000000000000000, 0.000000000000000000, 1.000000000000000000 ) ) ;
#33086=CARTESIAN_POINT ( 'NONE',  ( 5.999999999999999112, -27.74655509720726698, 77.16300072079651784 ) ) ;
#33092=DIRECTION ( 'NONE',  ( -1.000000000000000000, 0.000000000000000000, 0.000000000000000000 ) ) ;
#33096=AXIS2_PLACEMENT_3D ( 'NONE', #1516, #28415, #43360 ) ;
#33101=CARTESIAN_POINT ( 'NONE',  ( 0.000000000000000000, -20.40083707022829174, -72.35432306680507963 ) ) ;
#33104=AXIS2_PLACEMENT_3D ( 'NONE', #15362, #30036, #18282 ) ;
#33106=ADVANCED_FACE ( 'NONE', ( #24482 ), #36214, .T. ) ;
#33109=CARTESIAN_POINT ( 'NONE',  ( 6.000000000000000000, -3.894527615418457600, 81.90746397400387480 ) ) ;
#33110=AXIS2_PLACEMENT_3D ( 'NONE', #27516, #42440, #26781 ) ;
#33112=DIRECTION ( 'NONE',  ( -1.000000000000000000, -0.000000000000000000, 0.000000000000000000 ) ) ;
#33115=CARTESIAN_POINT ( 'NONE',  ( 15.00000000000000000, 0.000000000000000000, 0.000000000000000000 ) ) ;
#33119=CARTESIAN_POINT ( 'NONE',  ( 11.99999999999999822, 34.44570377933598593, 69.42325613327452061 ) ) ;
#33122=CIRCLE ( 'NONE', #4244, 31.99999999999998224 ) ;
#33123=DIRECTION ( 'NONE',  ( 0.000000000000000000, -0.1045284632676449221, 0.9945218953682741780 ) ) ;
#33132=ORIENTED_EDGE ( 'NONE', *, *, #24768, .F. ) ;
#33142=EDGE_LOOP ( 'NONE', ( #4214, #41816, #10537, #18274 ) ) ;
#33150=CARTESIAN_POINT ( 'NONE',  ( 11.99999999999999822, -65.59268652807183742, -36.72794159290312166 ) ) ;
#33151=DIRECTION ( 'NONE',  ( -1.000000000000000000, 0.000000000000000000, -0.000000000000000000 ) ) ;
#33152=ORIENTED_EDGE ( 'NONE', *, *, #37382, .F. ) ;
#33153=CARTESIAN_POINT ( 'NONE',  ( 11.99999999999999822, -59.03342792756297541, 46.54456581323783126 ) ) ;
#33158=DIRECTION ( 'NONE',  ( -1.000000000000000000, -0.000000000000000000, -0.000000000000000000 ) ) ;
#33160=ORIENTED_EDGE ( 'NONE', *, *, #7285, .F. ) ;
#33162=CYLINDRICAL_SURFACE ( 'NONE', #43504, 31.99999999999998579 ) ;
#33166=EDGE_CURVE ( 'NONE', #41935, #17996, #47000, .T. ) ;
#33170=ORIENTED_EDGE ( 'NONE', *, *, #3300, .F. ) ;
#33172=DIRECTION ( 'NONE',  ( -1.000000000000000000, 0.000000000000000000, -0.000000000000000000 ) ) ;
#33175=CARTESIAN_POINT ( 'NONE',  ( 0.000000000000000000, 21.60688246758697062, -79.10210256391344785 ) ) ;
#33177=EDGE_CURVE ( 'NONE', #37777, #36444, #5402, .T. ) ;
#33178=VECTOR ( 'NONE', #43724, 1000.000000000000000 ) ;
#33181=AXIS2_PLACEMENT_3D ( 'NONE', #43542, #32282, #32523 ) ;
#33192=ORIENTED_EDGE ( 'NONE', *, *, #8657, .F. ) ;
#33194=ORIENTED_EDGE ( 'NONE', *, *, #29966, .T. ) ;
#33199=VERTEX_POINT ( 'NONE', #13233 ) ;
#33203=CARTESIAN_POINT ( 'NONE',  ( 0.000000000000000000, 55.20638768913831029, -51.02545421589267960 ) ) ;
#33206=CARTESIAN_POINT ( 'NONE',  ( 11.99999999999999822, 78.73519480814985627, -22.90783923731548199 ) ) ;
#33211=DIRECTION ( 'NONE',  ( -1.000000000000000000, 0.000000000000000000, 0.000000000000000000 ) ) ;
#33213=DIRECTION ( 'NONE',  ( -1.000000000000000000, 0.000000000000000000, 0.000000000000000000 ) ) ;
#33217=EDGE_LOOP ( 'NONE', ( #4228, #42275, #37213, #24572 ) ) ;
#33218=EDGE_CURVE ( 'NONE', #30063, #6579, #10998, .T. ) ;
#33222=CARTESIAN_POINT ( 'NONE',  ( 0.000000000000000000, 73.95703589264006439, -23.16143007188350822 ) ) ;
#33230=EDGE_CURVE ( 'NONE', #46424, #37720, #6670, .T. ) ;
#33232=AXIS2_PLACEMENT_3D ( 'NONE', #45030, #44777, #26668 ) ;
#33237=EDGE_CURVE ( 'NONE', #37785, #44445, #10587, .T. ) ;
#33238=VECTOR ( 'NONE', #1564, 1000.000000000000000 ) ;
#33239=EDGE_LOOP ( 'NONE', ( #46693, #10961, #38284, #45001 ) ) ;
#33240=CARTESIAN_POINT ( 'NONE',  ( 11.99999999999999822, 73.72996012237460661, -14.67089635893632504 ) ) ;
#33244=AXIS2_PLACEMENT_3D ( 'NONE', #39469, #46081, #46320 ) ;
#33249=VECTOR ( 'NONE', #32657, 1000.000000000000000 ) ;
#33250=CIRCLE ( 'NONE', #7476, 82.00000000000000000 ) ;
#33251=CARTESIAN_POINT ( 'NONE',  ( 0.000000000000000000, 0.000000000000000000, 0.000000000000000000 ) ) ;
#33253=CARTESIAN_POINT ( 'NONE',  ( -10.00000000000000000, 0.000000000000000000, 0.000000000000000000 ) ) ;
#33257=EDGE_CURVE ( 'NONE', #8722, #33303, #30117, .T. ) ;
#33263=EDGE_LOOP ( 'NONE', ( #9755, #9814, #27519, #29640 ) ) ;
#33264=CARTESIAN_POINT ( 'NONE',  ( 11.99999999999999822, 76.66974797899837313, 11.30684508768366747 ) ) ;
#33268=ORIENTED_EDGE ( 'NONE', *, *, #1830, .T. ) ;
#33272=VERTEX_POINT ( 'NONE', #21534 ) ;
#33273=FACE_OUTER_BOUND ( 'NONE', #13654, .T. ) ;
#33274=FACE_OUTER_BOUND ( 'NONE', #3395, .T. ) ;
#33275=CARTESIAN_POINT ( 'NONE',  ( 0.000000000000000000, -26.01480285779785362, -70.53064760720343429 ) ) ;
#33282=AXIS2_PLACEMENT_3D ( 'NONE', #47826, #39295, #35860 ) ;
#33283=FACE_OUTER_BOUND ( 'NONE', #14904, .T. ) ;
#33286=CARTESIAN_POINT ( 'NONE',  ( 15.00000000000000000, 24.81905959214260804, -9.408202855044828894 ) ) ;
#33287=EDGE_LOOP ( 'NONE', ( #12609, #31207, #22513, #2258 ) ) ;
#33288=VERTEX_POINT ( 'NONE', #37183 ) ;
#33290=CIRCLE ( 'NONE', #21591, 77.49899999999999523 ) ;
#33291=CYLINDRICAL_SURFACE ( 'NONE', #13558, 77.49899999999999523 ) ;
#33292=CIRCLE ( 'NONE', #12211, 77.49899999999999523 ) ;
#33294=CARTESIAN_POINT ( 'NONE',  ( 11.99999999999999822, 76.66974797899852945, -11.30684508768257679 ) ) ;
#33297=ORIENTED_EDGE ( 'NONE', *, *, #1238, .T. ) ;
#33299=CYLINDRICAL_SURFACE ( 'NONE', #6169, 31.99999999999998579 ) ;
#33300=EDGE_LOOP ( 'NONE', ( #8666, #8865, #27313, #33731 ) ) ;
#33301=CARTESIAN_POINT ( 'NONE',  ( 11.99999999999999822, -76.41127070299262414, -12.93880638057396304 ) ) ;
#33303=VERTEX_POINT ( 'NONE', #21762 ) ;
#33304=ORIENTED_EDGE ( 'NONE', *, *, #5255, .T. ) ;
#33314=EDGE_LOOP ( 'NONE', ( #14059, #25363, #41602, #25619 ) ) ;
#33316=DIRECTION ( 'NONE',  ( 0.000000000000000000, 0.000000000000000000, 1.000000000000000000 ) ) ;
#33318=CARTESIAN_POINT ( 'NONE',  ( 11.99999999999999822, -14.67089635893764665, 73.72996012237435082 ) ) ;
#33320=DIRECTION ( 'NONE',  ( 0.000000000000000000, 0.7071067811865486830, -0.7071067811865463515 ) ) ;
#33321=DIRECTION ( 'NONE',  ( 0.000000000000000000, 0.000000000000000000, 1.000000000000000000 ) ) ;
#33324=ORIENTED_EDGE ( 'NONE', *, *, #28242, .T. ) ;
#33329=EDGE_CURVE ( 'NONE', #9618, #11259, #3153, .T. ) ;
#33330=CARTESIAN_POINT ( 'NONE',  ( 0.000000000000000000, 81.96053171279902472, 2.543863470248677316 ) ) ;
#33331=CARTESIAN_POINT ( 'NONE',  ( 6.000000000000000000, -80.55351364060599906, 15.33399622253457295 ) ) ;
#33338=ORIENTED_EDGE ( 'NONE', *, *, #32285, .F. ) ;
#33341=CYLINDRICAL_SURFACE ( 'NONE', #47745, 77.49899999999999523 ) ;
#33345=DIRECTION ( 'NONE',  ( -1.000000000000000000, 0.000000000000000000, 0.000000000000000000 ) ) ;
#33347=CARTESIAN_POINT ( 'NONE',  ( 11.99999999999999822, -51.29473840253177741, -63.97538442413483750 ) ) ;
#33348=CYLINDRICAL_SURFACE ( 'NONE', #42516, 82.00000000000000000 ) ;
#33351=ORIENTED_EDGE ( 'NONE', *, *, #4825, .T. ) ;
#33354=CARTESIAN_POINT ( 'NONE',  ( 12.00000000000000000, -13.04903810567675393, -19.60159698893424718 ) ) ;
#33355=VERTEX_POINT ( 'NONE', #32772 ) ;
#33365=CYLINDRICAL_SURFACE ( 'NONE', #22249, 77.49899999999999523 ) ;
#33367=VECTOR ( 'NONE', #47651, 1000.000000000000000 ) ;
#33368=EDGE_CURVE ( 'NONE', #11531, #48354, #872, .T. ) ;
#33371=VERTEX_POINT ( 'NONE', #35132 ) ;
#33373=CARTESIAN_POINT ( 'NONE',  ( 5.999999999999999112, 81.96053171279902472, 2.543863470248677316 ) ) ;
#33376=EDGE_CURVE ( 'NONE', #7935, #5492, #45930, .T. ) ;
#33382=DIRECTION ( 'NONE',  ( 1.000000000000000000, 0.000000000000000000, 0.000000000000000000 ) ) ;
#33385=DIRECTION ( 'NONE',  ( 0.000000000000000000, 0.000000000000000000, 1.000000000000000000 ) ) ;
#33388=VERTEX_POINT ( 'NONE', #12397 ) ;
#33392=ADVANCED_FACE ( 'NONE', ( #45677 ), #16543, .T. ) ;
#33400=DIRECTION ( 'NONE',  ( 0.000000000000000000, -0.6494480483301904306, 0.7604059656000252687 ) ) ;
#33406=DIRECTION ( 'NONE',  ( 0.000000000000000000, 0.000000000000000000, 1.000000000000000000 ) ) ;
#33408=CARTESIAN_POINT ( 'NONE',  ( 0.000000000000000000, 0.000000000000000000, 0.000000000000000000 ) ) ;
#33416=ORIENTED_EDGE ( 'NONE', *, *, #43215, .T. ) ;
#33425=ADVANCED_FACE ( 'NONE', ( #20442 ), #23635, .T. ) ;
#33432=ORIENTED_EDGE ( 'NONE', *, *, #47922, .F. ) ;
#33433=ORIENTED_EDGE ( 'NONE', *, *, #3912, .T. ) ;
#33434=ORIENTED_EDGE ( 'NONE', *, *, #38478, .T. ) ;
#33438=DIRECTION ( 'NONE',  ( -1.000000000000000000, 0.000000000000000000, 0.000000000000000000 ) ) ;
#33442=DIRECTION ( 'NONE',  ( -1.000000000000000000, -0.000000000000000000, -0.000000000000000000 ) ) ;
#33448=CARTESIAN_POINT ( 'NONE',  ( 12.00000000000000000, -11.95096189432345746, -23.69967320028757030 ) ) ;
#33449=DIRECTION ( 'NONE',  ( 0.000000000000000000, 0.000000000000000000, 1.000000000000000000 ) ) ;
#33463=DIRECTION ( 'NONE',  ( -1.000000000000000000, 0.000000000000000000, -0.000000000000000000 ) ) ;
#33466=DIRECTION ( 'NONE',  ( 0.000000000000000000, 0.000000000000000000, 1.000000000000000000 ) ) ;
#33469=ORIENTED_EDGE ( 'NONE', *, *, #1799, .T. ) ;
#33474=CARTESIAN_POINT ( 'NONE',  ( 0.000000000000000000, -72.35432306680469594, -20.40083707022958848 ) ) ;
#33475=DIRECTION ( 'NONE',  ( -1.000000000000000000, 0.000000000000000000, 0.000000000000000000 ) ) ;
#33477=EDGE_CURVE ( 'NONE', #20327, #23602, #13121, .T. ) ;
#33480=ORIENTED_EDGE ( 'NONE', *, *, #32822, .F. ) ;
#33482=AXIS2_PLACEMENT_3D ( 'NONE', #27305, #5753, #5027 ) ;
#33484=ADVANCED_FACE ( 'NONE', ( #9426 ), #24360, .F. ) ;
#33485=ORIENTED_EDGE ( 'NONE', *, *, #4958, .F. ) ;
#33488=CARTESIAN_POINT ( 'NONE',  ( 0.000000000000000000, 0.000000000000000000, 0.000000000000000000 ) ) ;
#33489=EDGE_CURVE ( 'NONE', #6565, #21764, #29374, .T. ) ;
#33490=ORIENTED_EDGE ( 'NONE', *, *, #26072, .F. ) ;
#33497=CARTESIAN_POINT ( 'NONE',  ( 11.99999999999999822, 0.000000000000000000, 0.000000000000000000 ) ) ;
#33500=EDGE_LOOP ( 'NONE', ( #26609, #24576, #24785, #28088 ) ) ;
#33501=ORIENTED_EDGE ( 'NONE', *, *, #16521, .F. ) ;
#33502=CYLINDRICAL_SURFACE ( 'NONE', #18952, 82.00000000000000000 ) ;
#33516=CARTESIAN_POINT ( 'NONE',  ( 5.999999999999999112, 40.65526001592713357, -71.21200624218752750 ) ) ;
#33521=ORIENTED_EDGE ( 'NONE', *, *, #8913, .T. ) ;
#33522=VERTEX_POINT ( 'NONE', #43929 ) ;
#33525=CARTESIAN_POINT ( 'NONE',  ( 11.99999999999999822, 0.000000000000000000, 0.000000000000000000 ) ) ;
#33531=EDGE_CURVE ( 'NONE', #25033, #7137, #24848, .T. ) ;
#33540=ORIENTED_EDGE ( 'NONE', *, *, #11724, .T. ) ;
#33541=CYLINDRICAL_SURFACE ( 'NONE', #23008, 82.00000000000000000 ) ;
#33545=ORIENTED_EDGE ( 'NONE', *, *, #24819, .F. ) ;
#33548=CARTESIAN_POINT ( 'NONE',  ( 11.99999999999999822, 14.67089635893819377, -73.72996012237423713 ) ) ;
#33550=AXIS2_PLACEMENT_3D ( 'NONE', #47913, #44259, #25640 ) ;
#33553=ORIENTED_EDGE ( 'NONE', *, *, #43894, .T. ) ;
#33557=DIRECTION ( 'NONE',  ( 0.000000000000000000, -0.8526401643540860720, -0.5224985647159590130 ) ) ;
#33560=PLANE ( 'NONE',  #30555 ) ;
#33564=CIRCLE ( 'NONE', #1532, 31.99999999999998224 ) ;
#33565=ORIENTED_EDGE ( 'NONE', *, *, #20177, .T. ) ;
#33571=EDGE_CURVE ( 'NONE', #20008, #28171, #32902, .T. ) ;
#33573=DIRECTION ( 'NONE',  ( 0.000000000000000000, -0.7431448254773954654, -0.6691306063588569053 ) ) ;
#33574=DIRECTION ( 'NONE',  ( 0.000000000000000000, 0.000000000000000000, 1.000000000000000000 ) ) ;
#33575=EDGE_CURVE ( 'NONE', #17439, #14824, #5945, .T. ) ;
#33579=DIRECTION ( 'NONE',  ( -1.000000000000000000, -0.000000000000000000, -0.000000000000000000 ) ) ;
#33583=LINE ( 'NONE', #6689, #24115 ) ;
#33585=EDGE_CURVE ( 'NONE', #6004, #1147, #17247, .T. ) ;
#33586=VECTOR ( 'NONE', #43343, 1000.000000000000000 ) ;
#33596=VERTEX_POINT ( 'NONE', #28530 ) ;
#33599=CARTESIAN_POINT ( 'NONE',  ( 11.99999999999999822, -79.10210256391381733, 21.60688246758557796 ) ) ;
#33603=DIRECTION ( 'NONE',  ( 1.000000000000000000, -0.000000000000000000, -0.000000000000000000 ) ) ;
#33604=ORIENTED_EDGE ( 'NONE', *, *, #5996, .F. ) ;
#33609=CARTESIAN_POINT ( 'NONE',  ( 0.000000000000000000, 0.000000000000000000, 0.000000000000000000 ) ) ;
#33612=ORIENTED_EDGE ( 'NONE', *, *, #12044, .T. ) ;
#33628=CARTESIAN_POINT ( 'NONE',  ( 11.99999999999999822, 0.000000000000000000, 0.000000000000000000 ) ) ;
#33629=CIRCLE ( 'NONE', #29720, 77.49899999999999523 ) ;
#33633=DIRECTION ( 'NONE',  ( 0.000000000000000000, 0.000000000000000000, 1.000000000000000000 ) ) ;
#33639=CARTESIAN_POINT ( 'NONE',  ( 11.99999999999999822, 51.29473840253317007, -63.97538442413369353 ) ) ;
#33641=ADVANCED_FACE ( 'NONE', ( #18929 ), #343, .T. ) ;
#33642=LINE ( 'NONE', #44669, #18946 ) ;
#33646=VECTOR ( 'NONE', #12317, 1000.000000000000000 ) ;
#33647=EDGE_CURVE ( 'NONE', #40057, #9769, #1216, .T. ) ;
#33657=LINE ( 'NONE', #123, #41384 ) ;
#33666=LINE ( 'NONE', #3575, #1660 ) ;
#33667=VERTEX_POINT ( 'NONE', #30452 ) ;
#33670=CARTESIAN_POINT ( 'NONE',  ( -10.00000000000000000, 0.000000000000000000, 0.000000000000000000 ) ) ;
#33674=DIRECTION ( 'NONE',  ( 0.000000000000000000, -0.9510565162951566398, 0.3090169943749381809 ) ) ;
#33677=DIRECTION ( 'NONE',  ( -1.000000000000000000, -0.000000000000000000, 0.000000000000000000 ) ) ;
#33678=DIRECTION ( 'NONE',  ( 0.000000000000000000, -0.8660254037844374864, 0.5000000000000019984 ) ) ;
#33681=CARTESIAN_POINT ( 'NONE',  ( 6.000000000000000000, 80.55351364060589958, 15.33399622253512540 ) ) ;
#33684=CIRCLE ( 'NONE', #31374, 31.99999999999998934 ) ;
#33685=CARTESIAN_POINT ( 'NONE',  ( 11.99999999999999822, 0.000000000000000000, 0.000000000000000000 ) ) ;
#33692=EDGE_CURVE ( 'NONE', #12857, #30611, #46574, .T. ) ;
#33695=DIRECTION ( 'NONE',  ( -1.000000000000000000, -0.000000000000000000, -0.000000000000000000 ) ) ;
#33696=EDGE_CURVE ( 'NONE', #33667, #14588, #38752, .T. ) ;
#33697=CIRCLE ( 'NONE', #21956, 31.99999999999999289 ) ;
#33698=DIRECTION ( 'NONE',  ( 1.000000000000000000, 0.000000000000000000, 0.000000000000000000 ) ) ;
#33700=AXIS2_PLACEMENT_3D ( 'NONE', #21711, #44234, #43985 ) ;
#33701=CARTESIAN_POINT ( 'NONE',  ( 12.00000000000000000, -1.278221433540507546, -26.51162292216071492 ) ) ;
#33709=EDGE_LOOP ( 'NONE', ( #15404, #4903, #25292, #46380 ) ) ;
#33711=CARTESIAN_POINT ( 'NONE',  ( 11.99999999999999822, 70.53064760720316428, -26.01480285779861035 ) ) ;
#33712=ORIENTED_EDGE ( 'NONE', *, *, #17692, .F. ) ;
#33720=ORIENTED_EDGE ( 'NONE', *, *, #39138, .F. ) ;
#33728=DIRECTION ( 'NONE',  ( 0.000000000000000000, -0.9945218953682740670, -0.1045284632676459352 ) ) ;
#33729=CARTESIAN_POINT ( 'NONE',  ( 6.000000000000000000, -39.47590169984898267, 71.87247863392400404 ) ) ;
#33730=ORIENTED_EDGE ( 'NONE', *, *, #23760, .T. ) ;
#33731=ORIENTED_EDGE ( 'NONE', *, *, #13808, .T. ) ;
#33736=VERTEX_POINT ( 'NONE', #11384 ) ;
#33737=DIRECTION ( 'NONE',  ( 0.000000000000000000, -0.9781476007338041345, 0.2079116908177663092 ) ) ;
#33740=ADVANCED_FACE ( 'NONE', ( #22618 ), #22857, .T. ) ;
#33741=DIRECTION ( 'NONE',  ( 1.000000000000000000, 0.000000000000000000, 0.000000000000000000 ) ) ;
#33743=DIRECTION ( 'NONE',  ( -1.000000000000000000, -0.000000000000000000, 0.000000000000000000 ) ) ;
#33750=DIRECTION ( 'NONE',  ( 0.000000000000000000, 0.000000000000000000, 1.000000000000000000 ) ) ;
#33753=CARTESIAN_POINT ( 'NONE',  ( 11.99999999999999822, 0.000000000000000000, 0.000000000000000000 ) ) ;
#33754=DIRECTION ( 'NONE',  ( 0.000000000000000000, 0.000000000000000000, 1.000000000000000000 ) ) ;
#33758=ADVANCED_FACE ( 'NONE', ( #48086 ), #22389, .T. ) ;
#33762=CARTESIAN_POINT ( 'NONE',  ( 0.000000000000000000, -41.19522573413689059, -65.64334221924951862 ) ) ;
#33766=VERTEX_POINT ( 'NONE', #46108 ) ;
#33771=EDGE_LOOP ( 'NONE', ( #676, #33268, #46676, #40971 ) ) ;
#33773=DIRECTION ( 'NONE',  ( 0.000000000000000000, -0.9723699203976741146, -0.2334453638559160493 ) ) ;
#33776=ORIENTED_EDGE ( 'NONE', *, *, #35541, .F. ) ;
#33780=PLANE ( 'NONE',  #44998 ) ;
#33785=CARTESIAN_POINT ( 'NONE',  ( 0.000000000000000000, -74.18225833017913828, 34.94270380257611208 ) ) ;
#33791=DIRECTION ( 'NONE',  ( 0.000000000000000000, 0.000000000000000000, 1.000000000000000000 ) ) ;
#33793=CARTESIAN_POINT ( 'NONE',  ( 11.99999999999999822, 8.966570791700714693, 81.50828551894230145 ) ) ;
#33795=VERTEX_POINT ( 'NONE', #45613 ) ;
#33799=CARTESIAN_POINT ( 'NONE',  ( 11.99999999999999822, 71.27951684758026829, 30.41916302227139113 ) ) ;
#33804=DIRECTION ( 'NONE',  ( 0.000000000000000000, 0.000000000000000000, 1.000000000000000000 ) ) ;
#33807=VERTEX_POINT ( 'NONE', #1800 ) ;
#33809=DIRECTION ( 'NONE',  ( 0.000000000000000000, 0.8090169943749445647, 0.5877852522924770229 ) ) ;
#33811=DIRECTION ( 'NONE',  ( -1.000000000000000000, 0.000000000000000000, 0.000000000000000000 ) ) ;
#33815=DIRECTION ( 'NONE',  ( 1.000000000000000000, -0.000000000000000000, -0.000000000000000000 ) ) ;
#33816=DIRECTION ( 'NONE',  ( -1.000000000000000000, 0.000000000000000000, -0.000000000000000000 ) ) ;
#33818=DIRECTION ( 'NONE',  ( -1.000000000000000000, 0.000000000000000000, 0.000000000000000000 ) ) ;
#33822=VECTOR ( 'NONE', #42733, 1000.000000000000000 ) ;
#33824=ORIENTED_EDGE ( 'NONE', *, *, #10774, .T. ) ;
#33825=EDGE_CURVE ( 'NONE', #45805, #6579, #24734, .T. ) ;
#33827=AXIS2_PLACEMENT_3D ( 'NONE', #35962, #10255, #6119 ) ;
#33829=AXIS2_PLACEMENT_3D ( 'NONE', #28324, #38882, #39611 ) ;
#33836=CARTESIAN_POINT ( 'NONE',  ( 11.99999999999999822, -34.44570377933647620, 69.42325613327427902 ) ) ;
#33847=PLANE ( 'NONE',  #133 ) ;
#33848=AXIS2_PLACEMENT_3D ( 'NONE', #24966, #46785, #17860 ) ;
#33849=DIRECTION ( 'NONE',  ( 0.000000000000000000, 0.9876883405951371042, 0.1564344650402346715 ) ) ;
#33856=CARTESIAN_POINT ( 'NONE',  ( 11.99999999999999822, -68.67312586194971402, -35.91791733033549860 ) ) ;
#33858=ADVANCED_FACE ( 'NONE', ( #15763 ), #20154, .T. ) ;
#33860=CARTESIAN_POINT ( 'NONE',  ( 11.99999999999999822, -51.02545421589285723, -55.20638768913812555 ) ) ;
#33866=EDGE_CURVE ( 'NONE', #17937, #22938, #13762, .T. ) ;
#33868=CARTESIAN_POINT ( 'NONE',  ( 0.000000000000000000, 0.000000000000000000, 0.000000000000000000 ) ) ;
#33874=DIRECTION ( 'NONE',  ( -1.000000000000000000, -0.000000000000000000, 0.000000000000000000 ) ) ;
#33878=AXIS2_PLACEMENT_3D ( 'NONE', #3506, #14537, #32418 ) ;
#33881=CARTESIAN_POINT ( 'NONE',  ( 11.99999999999999822, 0.000000000000000000, 0.000000000000000000 ) ) ;
#33882=DIRECTION ( 'NONE',  ( -1.000000000000000000, 0.000000000000000000, 0.000000000000000000 ) ) ;
#33883=DIRECTION ( 'NONE',  ( 0.000000000000000000, 0.8526401643540935105, -0.5224985647159466895 ) ) ;
#33886=EDGE_LOOP ( 'NONE', ( #2983, #33433, #44980, #4950 ) ) ;
#33889=VECTOR ( 'NONE', #3530, 1000.000000000000000 ) ;
#33898=FACE_OUTER_BOUND ( 'NONE', #13802, .T. ) ;
#33901=ORIENTED_EDGE ( 'NONE', *, *, #1025, .F. ) ;
#33903=VERTEX_POINT ( 'NONE', #42687 ) ;
#33913=CYLINDRICAL_SURFACE ( 'NONE', #11335, 31.99999999999998579 ) ;
#33914=CARTESIAN_POINT ( 'NONE',  ( 11.99999999999999822, 62.50329211542494789, -41.76937507738723099 ) ) ;
#33918=EDGE_CURVE ( 'NONE', #20499, #24200, #18473, .T. ) ;
#33922=DIRECTION ( 'NONE',  ( -1.000000000000000000, 0.000000000000000000, -0.000000000000000000 ) ) ;
#33923=ORIENTED_EDGE ( 'NONE', *, *, #10526, .F. ) ;
#33925=AXIS2_PLACEMENT_3D ( 'NONE', #20878, #31913, #16478 ) ;
#33926=ORIENTED_EDGE ( 'NONE', *, *, #31512, .F. ) ;
#33927=ORIENTED_EDGE ( 'NONE', *, *, #40181, .F. ) ;
#33930=VECTOR ( 'NONE', #26174, 1000.000000000000000 ) ;
#33933=ADVANCED_FACE ( 'NONE', ( #35810, #35575 ), #27999, .F. ) ;
#33935=CARTESIAN_POINT ( 'NONE',  ( 15.00000000000000000, -19.89357724624986545, 12.59942793731086219 ) ) ;
#33939=AXIS2_PLACEMENT_3D ( 'NONE', #2003, #12763, #27700 ) ;
#33942=AXIS2_PLACEMENT_3D ( 'NONE', #30056, #22229, #37154 ) ;
#33945=CARTESIAN_POINT ( 'NONE',  ( -10.00000000000000000, 0.000000000000000000, 0.000000000000000000 ) ) ;
#33946=AXIS2_PLACEMENT_3D ( 'NONE', #5368, #37937, #719 ) ;
#33953=VECTOR ( 'NONE', #44048, 1000.000000000000114 ) ;
#33954=ADVANCED_FACE ( 'NONE', ( #24797 ), #10333, .F. ) ;
#33960=ORIENTED_EDGE ( 'NONE', *, *, #25291, .T. ) ;
#33966=CARTESIAN_POINT ( 'NONE',  ( 11.99999999999999822, 0.8261519478431255115, 77.49459641780886443 ) ) ;
#33967=AXIS2_PLACEMENT_3D ( 'NONE', #48115, #14601, #18961 ) ;
#33970=EDGE_LOOP ( 'NONE', ( #47131, #20603, #25929, #18564 ) ) ;
#33975=AXIS2_PLACEMENT_3D ( 'NONE', #25495, #22058, #3211 ) ;
#33979=VECTOR ( 'NONE', #18740, 1000.000000000000000 ) ;
#33990=CARTESIAN_POINT ( 'NONE',  ( 11.99999999999999822, 66.50666863322055633, -39.78640506895536078 ) ) ;
#33992=DIRECTION ( 'NONE',  ( 0.000000000000000000, 0.000000000000000000, 1.000000000000000000 ) ) ;
#33993=DIRECTION ( 'NONE',  ( 1.000000000000000000, 0.000000000000000000, 0.000000000000000000 ) ) ;
#33997=AXIS2_PLACEMENT_3D ( 'NONE', #22980, #33741, #19059 ) ;
#34001=DIRECTION ( 'NONE',  ( -1.000000000000000000, 0.000000000000000000, -0.000000000000000000 ) ) ;
#34005=CIRCLE ( 'NONE', #2734, 77.49900000000000944 ) ;
#34008=CARTESIAN_POINT ( 'NONE',  ( -10.00000000000000000, 0.000000000000000000, 0.000000000000000000 ) ) ;
#34010=CARTESIAN_POINT ( 'NONE',  ( 0.000000000000000000, -34.44570377933647620, 69.42325613327427902 ) ) ;
#34012=CIRCLE ( 'NONE', #12937, 31.99999999999998224 ) ;
#34015=ORIENTED_EDGE ( 'NONE', *, *, #39897, .T. ) ;
#34017=DIRECTION ( 'NONE',  ( 0.000000000000000000, -0.9969173337331287410, 0.07845909572783495156 ) ) ;
#34026=DIRECTION ( 'NONE',  ( -1.000000000000000000, 0.000000000000000000, 0.000000000000000000 ) ) ;
#34031=DIRECTION ( 'NONE',  ( 0.000000000000000000, 0.3826834323650841752, 0.9238795325112891810 ) ) ;
#34032=FACE_OUTER_BOUND ( 'NONE', #31062, .T. ) ;
#34034=EDGE_CURVE ( 'NONE', #2290, #20052, #9835, .T. ) ;
#34035=CARTESIAN_POINT ( 'NONE',  ( 15.00000000000000000, -19.89357724624986545, 12.59942793731086219 ) ) ;
#34037=ORIENTED_EDGE ( 'NONE', *, *, #44437, .T. ) ;
#34048=ORIENTED_EDGE ( 'NONE', *, *, #31312, .F. ) ;
#34052=DIRECTION ( 'NONE',  ( 0.000000000000000000, -0.6494480483301739993, -0.7604059656000391465 ) ) ;
#34055=CARTESIAN_POINT ( 'NONE',  ( 11.99999999999999822, -35.91791733033525702, 68.67312586194982771 ) ) ;
#34057=DIRECTION ( 'NONE',  ( -1.000000000000000000, 0.000000000000000000, 0.000000000000000000 ) ) ;
#34065=VECTOR ( 'NONE', #15740, 1000.000000000000000 ) ;
#34067=ORIENTED_EDGE ( 'NONE', *, *, #30109, .T. ) ;
#34069=CIRCLE ( 'NONE', #17643, 31.99999999999998934 ) ;
#34071=ORIENTED_EDGE ( 'NONE', *, *, #45829, .F. ) ;
#34076=ORIENTED_EDGE ( 'NONE', *, *, #25636, .T. ) ;
#34083=CIRCLE ( 'NONE', #13660, 77.49899999999998101 ) ;
#34084=EDGE_CURVE ( 'NONE', #3949, #33371, #28612, .T. ) ;
#34085=DIRECTION ( 'NONE',  ( 0.000000000000000000, 0.000000000000000000, 1.000000000000000000 ) ) ;
#34092=AXIS2_PLACEMENT_3D ( 'NONE', #23522, #24249, #1745 ) ;
#34096=ADVANCED_FACE ( 'NONE', ( #36998 ), #44835, .T. ) ;
#34097=CARTESIAN_POINT ( 'NONE',  ( 15.00000000000000000, 0.000000000000000000, 0.000000000000000000 ) ) ;
#34099=CARTESIAN_POINT ( 'NONE',  ( 15.00000000000000000, 16.83928648764945635, 16.46020748918027010 ) ) ;
#34101=DIRECTION ( 'NONE',  ( -1.000000000000000000, -0.000000000000000000, 0.000000000000000000 ) ) ;
#34104=EDGE_CURVE ( 'NONE', #47105, #24099, #37731, .T. ) ;
#34105=CARTESIAN_POINT ( 'NONE',  ( 0.000000000000000000, 14.67089635893713684, 73.72996012237443608 ) ) ;
#34108=LINE ( 'NONE', #30683, #18794 ) ;
#34110=DIRECTION ( 'NONE',  ( 0.000000000000000000, 0.000000000000000000, 1.000000000000000000 ) ) ;
#34111=DIRECTION ( 'NONE',  ( 0.000000000000000000, 0.000000000000000000, 1.000000000000000000 ) ) ;
#34112=DIRECTION ( 'NONE',  ( -1.000000000000000000, 0.000000000000000000, 0.000000000000000000 ) ) ;
#34113=CYLINDRICAL_SURFACE ( 'NONE', #8006, 31.99999999999998579 ) ;
#34115=DIRECTION ( 'NONE',  ( -1.000000000000000000, -0.000000000000000000, 0.000000000000000000 ) ) ;
#34125=ORIENTED_EDGE ( 'NONE', *, *, #48451, .F. ) ;
#34130=CIRCLE ( 'NONE', #2110, 31.99999999999998224 ) ;
#34135=ORIENTED_EDGE ( 'NONE', *, *, #20530, .T. ) ;
#34140=ORIENTED_EDGE ( 'NONE', *, *, #39876, .F. ) ;
#34141=ORIENTED_EDGE ( 'NONE', *, *, #15315, .F. ) ;
#34145=EDGE_CURVE ( 'NONE', #30146, #28808, #11322, .T. ) ;
#34148=DIRECTION ( 'NONE',  ( -1.000000000000000000, -0.000000000000000000, 0.000000000000000000 ) ) ;
#34149=DIRECTION ( 'NONE',  ( -1.000000000000000000, 0.000000000000000000, 0.000000000000000000 ) ) ;
#34150=EDGE_LOOP ( 'NONE', ( #2674, #185, #14772, #24006 ) ) ;
#34154=CARTESIAN_POINT ( 'NONE',  ( -10.00000000000000000, 0.000000000000000000, 0.000000000000000000 ) ) ;
#34161=ORIENTED_EDGE ( 'NONE', *, *, #11341, .T. ) ;
#34163=DIRECTION ( 'NONE',  ( -1.000000000000000000, -0.000000000000000000, 0.000000000000000000 ) ) ;
#34165=CARTESIAN_POINT ( 'NONE',  ( 0.000000000000000000, -81.50828551894220197, -8.966570791701586884 ) ) ;
#34170=DIRECTION ( 'NONE',  ( 0.000000000000000000, 0.000000000000000000, -1.000000000000000000 ) ) ;
#34183=DIRECTION ( 'NONE',  ( -1.000000000000000000, -0.000000000000000000, -0.000000000000000000 ) ) ;
#34185=AXIS2_PLACEMENT_3D ( 'NONE', #19174, #38030, #30673 ) ;
#34194=ORIENTED_EDGE ( 'NONE', *, *, #5950, .T. ) ;
#34204=EDGE_CURVE ( 'NONE', #23962, #39152, #30402, .T. ) ;
#34209=DIRECTION ( 'NONE',  ( -1.000000000000000000, 0.000000000000000000, -0.000000000000000000 ) ) ;
#34216=DIRECTION ( 'NONE',  ( 0.000000000000000000, 0.7604059656000276002, 0.6494480483301876550 ) ) ;
#34221=( NAMED_UNIT ( * ) PLANE_ANGLE_UNIT ( ) SI_UNIT ( $, .RADIAN. ) );
#34225=ORIENTED_EDGE ( 'NONE', *, *, #35238, .F. ) ;
#34231=DIRECTION ( 'NONE',  ( -1.000000000000000000, -0.000000000000000000, 0.000000000000000000 ) ) ;
#34244=ORIENTED_EDGE ( 'NONE', *, *, #22036, .T. ) ;
#34246=ADVANCED_FACE ( 'NONE', ( #1001 ), #45313, .T. ) ;
#34250=ADVANCED_FACE ( 'NONE', ( #19363 ), #30634, .T. ) ;
#34257=VERTEX_POINT ( 'NONE', #27691 ) ;
#34259=AXIS2_PLACEMENT_3D ( 'NONE', #15478, #19601, #45828 ) ;
#34266=CARTESIAN_POINT ( 'NONE',  ( -10.00000000000000000, 0.000000000000000000, 0.000000000000000000 ) ) ;
#34269=CARTESIAN_POINT ( 'NONE',  ( 11.99999999999999822, 0.000000000000000000, 0.000000000000000000 ) ) ;
#34276=FACE_OUTER_BOUND ( 'NONE', #4948, .T. ) ;
#34277=ORIENTED_EDGE ( 'NONE', *, *, #6367, .F. ) ;
#34281=AXIS2_PLACEMENT_3D ( 'NONE', #16384, #46246, #46967 ) ;
#34284=CYLINDRICAL_SURFACE ( 'NONE', #11244, 82.00000000000000000 ) ;
#34298=EDGE_LOOP ( 'NONE', ( #37568, #39601, #41805, #43012 ) ) ;
#34303=DIRECTION ( 'NONE',  ( -0.000000000000000000, 0.000000000000000000, 1.000000000000000000 ) ) ;
#34310=EDGE_CURVE ( 'NONE', #44612, #47223, #27116, .T. ) ;
#34315=EDGE_CURVE ( 'NONE', #44874, #46424, #41158, .T. ) ;
#34319=ORIENTED_EDGE ( 'NONE', *, *, #46084, .T. ) ;
#34321=DIRECTION ( 'NONE',  ( -1.000000000000000000, 0.000000000000000000, 0.000000000000000000 ) ) ;
#34322=CYLINDRICAL_SURFACE ( 'NONE', #44464, 31.99999999999998579 ) ;
#34326=CARTESIAN_POINT ( 'NONE',  ( 6.000000000000000000, -76.69515212745996280, -29.01471420065643869 ) ) ;
#34329=CYLINDRICAL_SURFACE ( 'NONE', #32494, 77.49899999999999523 ) ;
#34330=ORIENTED_EDGE ( 'NONE', *, *, #30472, .F. ) ;
#34332=DIRECTION ( 'NONE',  ( 0.000000000000000000, -0.9510565162951566398, 0.3090169943749381809 ) ) ;
#34337=CARTESIAN_POINT ( 'NONE',  ( 0.000000000000000000, 73.44644590900092851, -24.73286445877629092 ) ) ;
#34344=CARTESIAN_POINT ( 'NONE',  ( 0.000000000000000000, 2.571758278209441661E-15, -21.00000000000000000 ) ) ;
#34345=CARTESIAN_POINT ( 'NONE',  ( 15.00000000000000000, -20.55727247249748402, -16.78983467731284307 ) ) ;
#34348=EDGE_CURVE ( 'NONE', #36067, #39062, #13473, .T. ) ;
#34349=CARTESIAN_POINT ( 'NONE',  ( 11.99999999999999822, -65.58780272294048075, -36.73666225445966660 ) ) ;
#34351=ADVANCED_FACE ( 'NONE', ( #17369 ), #5904, .T. ) ;
#34352=DIRECTION ( 'NONE',  ( 0.000000000000000000, 0.3090169943749410675, 0.9510565162951556406 ) ) ;
#34356=DIRECTION ( 'NONE',  ( -1.000000000000000000, 0.000000000000000000, 0.000000000000000000 ) ) ;
#34359=VERTEX_POINT ( 'NONE', #9799 ) ;
#34364=ORIENTED_EDGE ( 'NONE', *, *, #10342, .T. ) ;
#34366=ORIENTED_EDGE ( 'NONE', *, *, #39351, .F. ) ;
#34367=EDGE_CURVE ( 'NONE', #35720, #11988, #46644, .T. ) ;
#34368=CIRCLE ( 'NONE', #24218, 31.99999999999999289 ) ;
#34370=AXIS2_PLACEMENT_3D ( 'NONE', #20182, #12852, #9168 ) ;
#34374=ORIENTED_EDGE ( 'NONE', *, *, #20264, .T. ) ;
#34375=LINE ( 'NONE', #34616, #18759 ) ;
#34376=ORIENTED_EDGE ( 'NONE', *, *, #16904, .T. ) ;
#34377=ORIENTED_EDGE ( 'NONE', *, *, #34412, .F. ) ;
#34380=DIRECTION ( 'NONE',  ( 0.000000000000000000, -0.9510565162951510887, 0.3090169943749551673 ) ) ;
#34382=EDGE_LOOP ( 'NONE', ( #4859, #27293, #46776, #29290 ) ) ;
#34383=AXIS2_PLACEMENT_3D ( 'NONE', #13996, #40661, #18129 ) ;
#34384=CARTESIAN_POINT ( 'NONE',  ( 0.000000000000000000, -3.894527615418457600, 81.90746397400387480 ) ) ;
#34394=DIRECTION ( 'NONE',  ( 0.000000000000000000, 0.000000000000000000, -1.000000000000000000 ) ) ;
#34396=ORIENTED_EDGE ( 'NONE', *, *, #42563, .F. ) ;
#34397=ORIENTED_EDGE ( 'NONE', *, *, #32067, .F. ) ;
#34398=DIRECTION ( 'NONE',  ( 0.000000000000000000, 0.3090169943749461745, -0.9510565162951539753 ) ) ;
#34399=EDGE_CURVE ( 'NONE', #37878, #6565, #23186, .T. ) ;
#34411=AXIS2_PLACEMENT_3D ( 'NONE', #42051, #22954, #15857 ) ;
#34412=EDGE_CURVE ( 'NONE', #19565, #32725, #28647, .T. ) ;
#34416=FACE_OUTER_BOUND ( 'NONE', #14397, .T. ) ;
#34423=ADVANCED_FACE ( 'NONE', ( #10037 ), #13240, .T. ) ;
#34428=ORIENTED_EDGE ( 'NONE', *, *, #2118, .F. ) ;
#34433=CARTESIAN_POINT ( 'NONE',  ( 15.00000000000000000, 16.83928648764922542, -16.46020748918050458 ) ) ;
#34436=ADVANCED_FACE ( 'NONE', ( #43095 ), #9548, .T. ) ;
#34438=CIRCLE ( 'NONE', #11793, 31.99999999999998579 ) ;
#34439=ORIENTED_EDGE ( 'NONE', *, *, #21868, .T. ) ;
#34444=VECTOR ( 'NONE', #18690, 1000.000000000000000 ) ;
#34446=DIRECTION ( 'NONE',  ( -1.000000000000000000, 0.000000000000000000, -0.000000000000000000 ) ) ;
#34450=VERTEX_POINT ( 'NONE', #3161 ) ;
#34468=CARTESIAN_POINT ( 'NONE',  ( 11.99999999999999822, -77.19088730480528682, 6.903761155837505825 ) ) ;
#34471=EDGE_CURVE ( 'NONE', #41935, #19037, #32556, .T. ) ;
#34474=CARTESIAN_POINT ( 'NONE',  ( 11.99999999999999822, -62.50329211542465657, 41.76937507738766442 ) ) ;
#34475=ORIENTED_EDGE ( 'NONE', *, *, #2306, .T. ) ;
#34478=AXIS2_PLACEMENT_3D ( 'NONE', #43451, #17475, #36087 ) ;
#34488=ORIENTED_EDGE ( 'NONE', *, *, #32448, .F. ) ;
#34494=ORIENTED_EDGE ( 'NONE', *, *, #31031, .F. ) ;
#34497=ORIENTED_EDGE ( 'NONE', *, *, #39018, .T. ) ;
#34498=CARTESIAN_POINT ( 'NONE',  ( 11.99999999999999822, 44.99326035066149387, -68.55367621811095091 ) ) ;
#34503=CARTESIAN_POINT ( 'NONE',  ( 11.99999999999999822, 76.41127070299273782, 12.93880638057342836 ) ) ;
#34504=ORIENTED_EDGE ( 'NONE', *, *, #9891, .T. ) ;
#34512=DIRECTION ( 'NONE',  ( 0.000000000000000000, 0.07845909572784530439, -0.9969173337331279638 ) ) ;
#34513=ORIENTED_EDGE ( 'NONE', *, *, #40249, .F. ) ;
#34515=EDGE_CURVE ( 'NONE', #31321, #27284, #22510, .T. ) ;
#34519=LINE ( 'NONE', #38216, #23765 ) ;
#34527=DIRECTION ( 'NONE',  ( -1.000000000000000000, -0.000000000000000000, 0.000000000000000000 ) ) ;
#34528=ORIENTED_EDGE ( 'NONE', *, *, #38177, .F. ) ;
#34529=DIRECTION ( 'NONE',  ( 0.000000000000000000, -0.8526401643540970632, 0.5224985647159409163 ) ) ;
#34538=DIRECTION ( 'NONE',  ( -1.000000000000000000, 0.000000000000000000, 0.000000000000000000 ) ) ;
#34540=VERTEX_POINT ( 'NONE', #32781 ) ;
#34543=LINE ( 'NONE', #5430, #32291 ) ;
#34554=CARTESIAN_POINT ( 'NONE',  ( 11.99999999999999822, -62.50329211542407393, -41.76937507738853839 ) ) ;
#34559=ADVANCED_FACE ( 'NONE', ( #11256 ), #3403, .T. ) ;
#34561=CARTESIAN_POINT ( 'NONE',  ( 11.99999999999999822, 0.000000000000000000, 0.000000000000000000 ) ) ;
#34562=PLANE ( 'NONE',  #34837 ) ;
#34563=PLANE ( 'NONE',  #8731 ) ;
#34571=LINE ( 'NONE', #27260, #16025 ) ;
#34572=DIRECTION ( 'NONE',  ( -1.000000000000000000, 0.000000000000000000, 0.000000000000000000 ) ) ;
#34573=CARTESIAN_POINT ( 'NONE',  ( 15.00000000000000000, 6.762365576493310826, -25.66652317338401090 ) ) ;
#34575=CARTESIAN_POINT ( 'NONE',  ( 0.000000000000000000, 0.000000000000000000, 0.000000000000000000 ) ) ;
#34577=DIRECTION ( 'NONE',  ( -1.000000000000000000, 0.000000000000000000, -0.000000000000000000 ) ) ;
#34579=EDGE_CURVE ( 'NONE', #36859, #40057, #9149, .T. ) ;
#34582=DIRECTION ( 'NONE',  ( 0.000000000000000000, 0.000000000000000000, 1.000000000000000000 ) ) ;
#34584=CIRCLE ( 'NONE', #47855, 82.00000000000000000 ) ;
#34585=DIRECTION ( 'NONE',  ( -1.000000000000000000, -0.000000000000000000, 0.000000000000000000 ) ) ;
#34588=VECTOR ( 'NONE', #16129, 1000.000000000000000 ) ;
#34589=CIRCLE ( 'NONE', #18203, 82.00000000000000000 ) ;
#34593=ORIENTED_EDGE ( 'NONE', *, *, #9331, .T. ) ;
#34596=DIRECTION ( 'NONE',  ( 0.000000000000000000, -1.000000000000000000, -1.047444401652940007E-14 ) ) ;
#34597=ORIENTED_EDGE ( 'NONE', *, *, #31300, .T. ) ;
#34601=ORIENTED_EDGE ( 'NONE', *, *, #42098, .T. ) ;
#34609=DIRECTION ( 'NONE',  ( 0.000000000000000000, -0.9781476007338065770, -0.2079116908177544853 ) ) ;
#34613=DIRECTION ( 'NONE',  ( -1.000000000000000000, -0.000000000000000000, 0.000000000000000000 ) ) ;
#34615=ORIENTED_EDGE ( 'NONE', *, *, #4049, .F. ) ;
#34616=CARTESIAN_POINT ( 'NONE',  ( 11.99999999999999822, -44.88180994100419952, 63.18004540533013369 ) ) ;
#34617=CIRCLE ( 'NONE', #40892, 82.00000000000000000 ) ;
#34619=EDGE_CURVE ( 'NONE', #15250, #43433, #31073, .T. ) ;
#34623=DIRECTION ( 'NONE',  ( -1.000000000000000000, 0.000000000000000000, -0.000000000000000000 ) ) ;
#34626=ORIENTED_EDGE ( 'NONE', *, *, #16531, .F. ) ;
#34631=AXIS2_PLACEMENT_3D ( 'NONE', #32106, #47026, #24039 ) ;
#34635=DIRECTION ( 'NONE',  ( -1.000000000000000000, 0.000000000000000000, 0.000000000000000000 ) ) ;
#34648=CARTESIAN_POINT ( 'NONE',  ( 12.00000000000000000, 14.60985201121703980, -18.46759930825707841 ) ) ;
#34649=CARTESIAN_POINT ( 'NONE',  ( 15.00000000000000000, 5.835314593368470248, -22.81335362449854642 ) ) ;
#34650=AXIS2_PLACEMENT_3D ( 'NONE', #41603, #3913, #22282 ) ;
#34654=VECTOR ( 'NONE', #40101, 999.9999999999998863 ) ;
#34658=CARTESIAN_POINT ( 'NONE',  ( 11.99999999999999822, 35.91791733033476675, 68.67312586195008350 ) ) ;
#34668=ORIENTED_EDGE ( 'NONE', *, *, #10738, .T. ) ;
#34669=AXIS2_PLACEMENT_3D ( 'NONE', #26198, #37451, #45045 ) ;
#34670=PLANE ( 'NONE',  #5404 ) ;
#34675=CARTESIAN_POINT ( 'NONE',  ( 11.99999999999999822, 0.000000000000000000, 0.000000000000000000 ) ) ;
#34677=VERTEX_POINT ( 'NONE', #42315 ) ;
#34678=VERTEX_POINT ( 'NONE', #37924 ) ;
#34679=ADVANCED_FACE ( 'NONE', ( #31079 ), #4405, .F. ) ;
#34681=DIRECTION ( 'NONE',  ( 0.000000000000000000, -0.9945218953682730678, 0.1045284632676570929 ) ) ;
#34683=ORIENTED_EDGE ( 'NONE', *, *, #6367, .T. ) ;
#34685=CYLINDRICAL_SURFACE ( 'NONE', #32166, 31.99999999999998579 ) ;
#34687=DIRECTION ( 'NONE',  ( 0.000000000000000000, -0.4067366430758009299, -0.9135454576426005335 ) ) ;
#34689=EDGE_LOOP ( 'NONE', ( #27022, #43382, #18578, #9592 ) ) ;
#34691=DIRECTION ( 'NONE',  ( -1.000000000000000000, 0.000000000000000000, 0.000000000000000000 ) ) ;
#34693=CIRCLE ( 'NONE', #32341, 31.99999999999999289 ) ;
#34700=VERTEX_POINT ( 'NONE', #34468 ) ;
#34715=CARTESIAN_POINT ( 'NONE',  ( 11.99999999999999822, 46.53671651293948486, 59.03961581697416250 ) ) ;
#34716=VECTOR ( 'NONE', #26596, 1000.000000000000000 ) ;
#34717=DIRECTION ( 'NONE',  ( 0.000000000000000000, -0.5877852522924625900, -0.8090169943749551118 ) ) ;
#34727=CYLINDRICAL_SURFACE ( 'NONE', #5849, 31.99999999999998579 ) ;
#34731=CIRCLE ( 'NONE', #39321, 82.00000000000000000 ) ;
#34736=VECTOR ( 'NONE', #6522, 1000.000000000000114 ) ;
#34738=AXIS2_PLACEMENT_3D ( 'NONE', #40562, #44714, #11189 ) ;
#34739=EDGE_CURVE ( 'NONE', #39062, #25700, #9946, .T. ) ;
#34743=ORIENTED_EDGE ( 'NONE', *, *, #21551, .T. ) ;
#34747=VECTOR ( 'NONE', #11432, 1000.000000000000000 ) ;
#34755=DIRECTION ( 'NONE',  ( 0.000000000000000000, 0.9876883405951371042, 0.1564344650402347547 ) ) ;
#34756=DIRECTION ( 'NONE',  ( 0.000000000000000000, 0.000000000000000000, 1.000000000000000000 ) ) ;
#34758=ORIENTED_EDGE ( 'NONE', *, *, #16807, .T. ) ;
#34765=DIRECTION ( 'NONE',  ( -1.000000000000000000, -0.000000000000000000, -0.000000000000000000 ) ) ;
#34767=VERTEX_POINT ( 'NONE', #23965 ) ;
#34773=DIRECTION ( 'NONE',  ( -1.000000000000000000, -0.000000000000000000, -0.000000000000000000 ) ) ;
#34774=CYLINDRICAL_SURFACE ( 'NONE', #40948, 31.99999999999998579 ) ;
#34777=DIRECTION ( 'NONE',  ( -1.000000000000000000, 0.000000000000000000, 0.000000000000000000 ) ) ;
#34779=VECTOR ( 'NONE', #39268, 1000.000000000000000 ) ;
#34780=VECTOR ( 'NONE', #42991, 1000.000000000000000 ) ;
#34790=ORIENTED_EDGE ( 'NONE', *, *, #22714, .F. ) ;
#34804=FACE_OUTER_BOUND ( 'NONE', #47473, .T. ) ;
#34815=ORIENTED_EDGE ( 'NONE', *, *, #47765, .T. ) ;
#34817=EDGE_CURVE ( 'NONE', #40828, #29191, #30254, .T. ) ;
#34819=CIRCLE ( 'NONE', #9809, 31.99999999999998579 ) ;
#34822=CARTESIAN_POINT ( 'NONE',  ( 11.99999999999999822, 74.65491531819118620, -8.830959090342659579 ) ) ;
#34823=CARTESIAN_POINT ( 'NONE',  ( 11.99999999999999822, 66.50666863322000211, 39.78640506895628448 ) ) ;
#34827=ORIENTED_EDGE ( 'NONE', *, *, #37424, .F. ) ;
#34836=CARTESIAN_POINT ( 'NONE',  ( 0.000000000000000000, 0.000000000000000000, 0.000000000000000000 ) ) ;
#34837=AXIS2_PLACEMENT_3D ( 'NONE', #38990, #39224, #5692 ) ;
#34838=DIRECTION ( 'NONE',  ( -1.000000000000000000, 0.000000000000000000, 0.000000000000000000 ) ) ;
#34840=FACE_OUTER_BOUND ( 'NONE', #3016, .T. ) ;
#34845=CARTESIAN_POINT ( 'NONE',  ( 11.99999999999999822, 0.000000000000000000, 0.000000000000000000 ) ) ;
#34864=EDGE_CURVE ( 'NONE', #35557, #9076, #42767, .T. ) ;
#34867=EDGE_CURVE ( 'NONE', #33766, #1684, #32580, .T. ) ;
#34879=DIRECTION ( 'NONE',  ( -1.000000000000000000, 0.000000000000000000, 0.000000000000000000 ) ) ;
#34885=EDGE_LOOP ( 'NONE', ( #34513, #48211, #42198, #12272 ) ) ;
#34888=FACE_OUTER_BOUND ( 'NONE', #6895, .T. ) ;
#34889=DIRECTION ( 'NONE',  ( -1.000000000000000000, 0.000000000000000000, 0.000000000000000000 ) ) ;
#34898=DIRECTION ( 'NONE',  ( 0.000000000000000000, 0.000000000000000000, 1.000000000000000000 ) ) ;
#34901=AXIS2_PLACEMENT_3D ( 'NONE', #7208, #1934, #3283 ) ;
#34903=CARTESIAN_POINT ( 'NONE',  ( 11.99999999999999822, -55.20638768913797634, 51.02545421589302777 ) ) ;
#34905=CARTESIAN_POINT ( 'NONE',  ( 11.99999999999999822, 0.000000000000000000, 0.000000000000000000 ) ) ;
#34907=EDGE_CURVE ( 'NONE', #34932, #14857, #17731, .T. ) ;
#34909=DIRECTION ( 'NONE',  ( -1.000000000000000000, -0.000000000000000000, -0.000000000000000000 ) ) ;
#34911=EDGE_CURVE ( 'NONE', #32361, #14333, #13670, .T. ) ;
#34915=ADVANCED_FACE ( 'NONE', ( #46955 ), #12701, .T. ) ;
#34916=ORIENTED_EDGE ( 'NONE', *, *, #9850, .T. ) ;
#34924=CARTESIAN_POINT ( 'NONE',  ( 11.99999999999999822, 54.21277698773752007, -55.38113227695726692 ) ) ;
#34929=CIRCLE ( 'NONE', #2134, 82.00000000000000000 ) ;
#34932=VERTEX_POINT ( 'NONE', #44481 ) ;
#34937=ORIENTED_EDGE ( 'NONE', *, *, #34619, .F. ) ;
#34942=ORIENTED_EDGE ( 'NONE', *, *, #7150, .F. ) ;
#34943=VERTEX_POINT ( 'NONE', #21957 ) ;
#34944=CARTESIAN_POINT ( 'NONE',  ( 12.00000000000000000, -26.23277895567251861, -4.042438405569750870 ) ) ;
#34955=ORIENTED_EDGE ( 'NONE', *, *, #44470, .F. ) ;
#34962=ORIENTED_EDGE ( 'NONE', *, *, #20944, .T. ) ;
#34963=CARTESIAN_POINT ( 'NONE',  ( 0.000000000000000000, 46.11716303203283474, -67.80270845531839541 ) ) ;
#34971=EDGE_CURVE ( 'NONE', #48222, #31890, #40461, .T. ) ;
#34974=ORIENTED_EDGE ( 'NONE', *, *, #22080, .F. ) ;
#34975=CIRCLE ( 'NONE', #12353, 31.99999999999998579 ) ;
#34978=VERTEX_POINT ( 'NONE', #3105 ) ;
#34983=ADVANCED_FACE ( 'NONE', ( #11194 ), #18038, .F. ) ;
#34985=CIRCLE ( 'NONE', #13894, 31.99999999999998224 ) ;
#34990=EDGE_LOOP ( 'NONE', ( #46956, #5558, #1969, #22278 ) ) ;
#34994=EDGE_CURVE ( 'NONE', #13012, #38297, #29065, .T. ) ;
#34997=VERTEX_POINT ( 'NONE', #22461 ) ;
#34999=ORIENTED_EDGE ( 'NONE', *, *, #25136, .T. ) ;
#35004=LINE ( 'NONE', #27672, #27097 ) ;
#35010=CYLINDRICAL_SURFACE ( 'NONE', #647, 82.00000000000000000 ) ;
#35011=ORIENTED_EDGE ( 'NONE', *, *, #16521, .T. ) ;
#35016=CARTESIAN_POINT ( 'NONE',  ( 12.00000000000000000, -22.67460108101782978, -6.353146135317906840 ) ) ;
#35017=DIRECTION ( 'NONE',  ( -1.000000000000000000, 0.000000000000000000, 0.000000000000000000 ) ) ;
#35023=LINE ( 'NONE', #16200, #36541 ) ;
#35026=AXIS2_PLACEMENT_3D ( 'NONE', #4607, #19508, #917 ) ;
#35034=EDGE_CURVE ( 'NONE', #33355, #28298, #25145, .T. ) ;
#35041=CARTESIAN_POINT ( 'NONE',  ( 11.99999999999999822, -59.46389618801999433, 49.70050353004867816 ) ) ;
#35043=ORIENTED_EDGE ( 'NONE', *, *, #26627, .T. ) ;
#35044=EDGE_CURVE ( 'NONE', #24044, #5585, #13094, .T. ) ;
#35048=DIRECTION ( 'NONE',  ( 0.000000000000000000, 0.000000000000000000, 1.000000000000000000 ) ) ;
#35050=CARTESIAN_POINT ( 'NONE',  ( 11.99999999999999822, 0.000000000000000000, 0.000000000000000000 ) ) ;
#35054=ORIENTED_EDGE ( 'NONE', *, *, #38478, .F. ) ;
#35056=CIRCLE ( 'NONE', #35026, 82.00000000000000000 ) ;
#35058=VERTEX_POINT ( 'NONE', #45940 ) ;
#35067=DIRECTION ( 'NONE',  ( -1.000000000000000000, -0.000000000000000000, -0.000000000000000000 ) ) ;
#35068=VERTEX_POINT ( 'NONE', #4812 ) ;
#35070=DIRECTION ( 'NONE',  ( 0.000000000000000000, 0.000000000000000000, 1.000000000000000000 ) ) ;
#35071=ORIENTED_EDGE ( 'NONE', *, *, #2297, .T. ) ;
#35074=CYLINDRICAL_SURFACE ( 'NONE', #39, 77.49899999999999523 ) ;
#35076=DIRECTION ( 'NONE',  ( -1.000000000000000000, -0.000000000000000000, -0.000000000000000000 ) ) ;
#35080=DIRECTION ( 'NONE',  ( -1.000000000000000000, 0.000000000000000000, -0.000000000000000000 ) ) ;
#35081=EDGE_CURVE ( 'NONE', #44069, #7113, #6834, .T. ) ;
#35083=CARTESIAN_POINT ( 'NONE',  ( 11.99999999999999822, 6.903761155837791819, 77.19088730480525840 ) ) ;
#35085=DIRECTION ( 'NONE',  ( -1.000000000000000000, -0.000000000000000000, -0.000000000000000000 ) ) ;
#35091=CARTESIAN_POINT ( 'NONE',  ( 15.00000000000000000, 0.000000000000000000, 0.000000000000000000 ) ) ;
#35095=DIRECTION ( 'NONE',  ( 0.000000000000000000, -0.9723699203976789995, 0.2334453638558956767 ) ) ;
#35101=EDGE_LOOP ( 'NONE', ( #25940, #25482, #15675, #46014 ) ) ;
#35105=DIRECTION ( 'NONE',  ( -1.000000000000000000, -0.000000000000000000, 0.000000000000000000 ) ) ;
#35114=ADVANCED_FACE ( 'NONE', ( #5060 ), #4575, .T. ) ;
#35115=ORIENTED_EDGE ( 'NONE', *, *, #18436, .T. ) ;
#35116=ORIENTED_EDGE ( 'NONE', *, *, #3062, .F. ) ;
#35120=FACE_OUTER_BOUND ( 'NONE', #955, .T. ) ;
#35122=DIRECTION ( 'NONE',  ( -1.000000000000000000, 0.000000000000000000, 0.000000000000000000 ) ) ;
#35124=DIRECTION ( 'NONE',  ( -1.000000000000000000, 0.000000000000000000, 0.000000000000000000 ) ) ;
#35127=DIRECTION ( 'NONE',  ( 0.000000000000000000, 0.000000000000000000, 1.000000000000000000 ) ) ;
#35129=CARTESIAN_POINT ( 'NONE',  ( 11.99999999999999822, -75.16055320797016748, -18.89407956138335365 ) ) ;
#35132=CARTESIAN_POINT ( 'NONE',  ( 12.00000000000000355, 0.000000000000000000, 21.00000000000000000 ) ) ;
#35133=ORIENTED_EDGE ( 'NONE', *, *, #25216, .F. ) ;
#35136=EDGE_CURVE ( 'NONE', #18133, #2410, #13868, .T. ) ;
#35137=DIRECTION ( 'NONE',  ( 0.000000000000000000, 0.9510565162951523099, 0.3090169943749514481 ) ) ;
#35140=DIRECTION ( 'NONE',  ( 0.000000000000000000, 0.000000000000000000, 1.000000000000000000 ) ) ;
#35141=DIRECTION ( 'NONE',  ( -1.000000000000000000, 0.000000000000000000, 0.000000000000000000 ) ) ;
#35144=CARTESIAN_POINT ( 'NONE',  ( 5.999999999999999112, -46.11716303203233736, 67.80270845531873647 ) ) ;
#35152=ORIENTED_EDGE ( 'NONE', *, *, #47854, .T. ) ;
#35156=ORIENTED_EDGE ( 'NONE', *, *, #14984, .F. ) ;
#35160=AXIS2_PLACEMENT_3D ( 'NONE', #44338, #18628, #17 ) ;
#35161=CARTESIAN_POINT ( 'NONE',  ( 11.99999999999999822, 26.01480285779837232, 70.53064760720326376 ) ) ;
#35163=EDGE_LOOP ( 'NONE', ( #22412, #44110, #11113, #45361 ) ) ;
#35165=ORIENTED_EDGE ( 'NONE', *, *, #17681, .T. ) ;
#35169=DIRECTION ( 'NONE',  ( -1.000000000000000000, 0.000000000000000000, -0.000000000000000000 ) ) ;
#35171=DIRECTION ( 'NONE',  ( -1.000000000000000000, 0.000000000000000000, 0.000000000000000000 ) ) ;
#35173=ORIENTED_EDGE ( 'NONE', *, *, #46704, .T. ) ;
#35187=VERTEX_POINT ( 'NONE', #31984 ) ;
#35203=AXIS2_PLACEMENT_3D ( 'NONE', #3189, #47280, #36964 ) ;
#35211=LINE ( 'NONE', #42082, #29350 ) ;
#35221=VECTOR ( 'NONE', #14113, 1000.000000000000000 ) ;
#35227=ORIENTED_EDGE ( 'NONE', *, *, #30844, .T. ) ;
#35230=DIRECTION ( 'NONE',  ( 1.000000000000000000, -0.000000000000000000, -0.000000000000000000 ) ) ;
#35231=EDGE_CURVE ( 'NONE', #21898, #36090, #42061, .T. ) ;
#35237=CARTESIAN_POINT ( 'NONE',  ( 11.99999999999999822, 0.000000000000000000, 0.000000000000000000 ) ) ;
#35238=EDGE_CURVE ( 'NONE', #22545, #46408, #41260, .T. ) ;
#35245=PLANE ( 'NONE',  #23493 ) ;
#35253=VERTEX_POINT ( 'NONE', #12646 ) ;
#35261=EDGE_CURVE ( 'NONE', #975, #43484, #35639, .T. ) ;
#35264=VECTOR ( 'NONE', #26815, 1000.000000000000000 ) ;
#35270=PLANE ( 'NONE',  #4935 ) ;
#35271=CARTESIAN_POINT ( 'NONE',  ( 15.00000000000000000, 16.61724383029361718, -20.69703378468926402 ) ) ;
#35273=FACE_OUTER_BOUND ( 'NONE', #40331, .T. ) ;
#35279=CARTESIAN_POINT ( 'NONE',  ( 5.999999999999999112, 60.67117009219215618, -55.16347631942977614 ) ) ;
#35280=EDGE_LOOP ( 'NONE', ( #11874, #10028, #28751, #42492 ) ) ;
#35285=CARTESIAN_POINT ( 'NONE',  ( 0.000000000000000000, 31.46837873494978055, 68.27212725128286763 ) ) ;
#35287=DIRECTION ( 'NONE',  ( 0.000000000000000000, 0.000000000000000000, 1.000000000000000000 ) ) ;
#35288=AXIS2_PLACEMENT_3D ( 'NONE', #26522, #4256, #11833 ) ;
#35293=ORIENTED_EDGE ( 'NONE', *, *, #37559, .T. ) ;
#35294=EDGE_CURVE ( 'NONE', #26344, #36873, #12364, .T. ) ;
#35297=VECTOR ( 'NONE', #35325, 1000.000000000000000 ) ;
#35300=ORIENTED_EDGE ( 'NONE', *, *, #318, .F. ) ;
#35310=ADVANCED_FACE ( 'NONE', ( #12891 ), #31752, .T. ) ;
#35311=DIRECTION ( 'NONE',  ( -1.000000000000000000, -0.000000000000000000, 0.000000000000000000 ) ) ;
#35314=CARTESIAN_POINT ( 'NONE',  ( 6.000000000000000000, -44.99326035066007279, -68.55367621811190304 ) ) ;
#35316=ORIENTED_EDGE ( 'NONE', *, *, #37682, .T. ) ;
#35319=CARTESIAN_POINT ( 'NONE',  ( 11.99999999999999822, 0.000000000000000000, 0.000000000000000000 ) ) ;
#35325=DIRECTION ( 'NONE',  ( -1.000000000000000000, -0.000000000000000000, -0.000000000000000000 ) ) ;
#35326=CYLINDRICAL_SURFACE ( 'NONE', #18511, 77.49899999999999523 ) ;
#35329=ORIENTED_EDGE ( 'NONE', *, *, #7013, .F. ) ;
#35331=EDGE_CURVE ( 'NONE', #40544, #41750, #14998, .T. ) ;
#35337=LINE ( 'NONE', #43654, #21324 ) ;
#35340=ADVANCED_FACE ( 'NONE', ( #22342 ), #26493, .T. ) ;
#35345=CARTESIAN_POINT ( 'NONE',  ( 15.00000000000000000, 8.688484142253932063, -21.88630264137371029 ) ) ;
#35347=CARTESIAN_POINT ( 'NONE',  ( 6.000000000000000000, -10.30890764327323161, -81.34940948281348483 ) ) ;
#35349=ORIENTED_EDGE ( 'NONE', *, *, #30978, .T. ) ;
#35350=EDGE_CURVE ( 'NONE', #34700, #29866, #37501, .T. ) ;
#35353=EDGE_CURVE ( 'NONE', #37286, #46628, #40690, .T. ) ;
#35354=CARTESIAN_POINT ( 'NONE',  ( 6.000000000000000000, 80.28980883073781172, -16.65972982744850128 ) ) ;
#35359=AXIS2_PLACEMENT_3D ( 'NONE', #43858, #22556, #17905 ) ;
#35367=CARTESIAN_POINT ( 'NONE',  ( 0.000000000000000000, 0.000000000000000000, 0.000000000000000000 ) ) ;
#35372=CARTESIAN_POINT ( 'NONE',  ( 11.99999999999999822, -24.73286445877757345, 73.44644590900053061 ) ) ;
#35374=CARTESIAN_POINT ( 'NONE',  ( 11.99999999999999822, -76.69515212745996280, -29.01471420065643869 ) ) ;
#35375=CARTESIAN_POINT ( 'NONE',  ( 0.000000000000000000, -70.52718814184240159, -26.02418014898383802 ) ) ;
#35376=DIRECTION ( 'NONE',  ( -1.000000000000000000, -0.000000000000000000, 0.000000000000000000 ) ) ;
#35377=DIRECTION ( 'NONE',  ( 1.000000000000000000, -0.000000000000000000, -0.000000000000000000 ) ) ;
#35385=FACE_OUTER_BOUND ( 'NONE', #46571, .T. ) ;
#35386=CARTESIAN_POINT ( 'NONE',  ( 0.000000000000000000, 0.000000000000000000, 0.000000000000000000 ) ) ;
#35390=VERTEX_POINT ( 'NONE', #11333 ) ;
#35391=AXIS2_PLACEMENT_3D ( 'NONE', #21625, #33112, #21365 ) ;
#35393=DIRECTION ( 'NONE',  ( -1.000000000000000000, -0.000000000000000000, 0.000000000000000000 ) ) ;
#35394=EDGE_LOOP ( 'NONE', ( #14414, #25537, #26901, #11698 ) ) ;
#35396=AXIS2_PLACEMENT_3D ( 'NONE', #47256, #13478, #21549 ) ;
#35398=ORIENTED_EDGE ( 'NONE', *, *, #3435, .F. ) ;
#35402=CIRCLE ( 'NONE', #43281, 82.00000000000000000 ) ;
#35403=ORIENTED_EDGE ( 'NONE', *, *, #40362, .T. ) ;
#35406=CARTESIAN_POINT ( 'NONE',  ( 11.99999999999999822, -69.42325613327415113, -34.44570377933671779 ) ) ;
#35412=VERTEX_POINT ( 'NONE', #44 ) ;
#35416=DIRECTION ( 'NONE',  ( -0.000000000000000000, 0.9945218953682744001, 0.1045284632676437842 ) ) ;
#35419=CARTESIAN_POINT ( 'NONE',  ( 12.00000000000000000, 5.835314593368777558, 22.81335362449846471 ) ) ;
#35426=CARTESIAN_POINT ( 'NONE',  ( 11.99999999999999822, 0.000000000000000000, 0.000000000000000000 ) ) ;
#35429=CARTESIAN_POINT ( 'NONE',  ( 11.99999999999999822, 79.10210256391367523, 21.60688246758614284 ) ) ;
#35432=CIRCLE ( 'NONE', #44833, 31.99999999999998579 ) ;
#35433=LINE ( 'NONE', #1924, #31348 ) ;
#35434=FACE_OUTER_BOUND ( 'NONE', #20487, .T. ) ;
#35442=AXIS2_PLACEMENT_3D ( 'NONE', #41050, #45668, #33674 ) ;
#35444=CARTESIAN_POINT ( 'NONE',  ( 11.99999999999999822, -74.18225833017913828, 34.94270380257611208 ) ) ;
#35448=DIRECTION ( 'NONE',  ( -1.000000000000000000, -0.000000000000000000, -0.000000000000000000 ) ) ;
#35455=VECTOR ( 'NONE', #3961, 1000.000000000000000 ) ;
#35458=VECTOR ( 'NONE', #11992, 1000.000000000000000 ) ;
#35459=ORIENTED_EDGE ( 'NONE', *, *, #33230, .T. ) ;
#35462=CARTESIAN_POINT ( 'NONE',  ( 0.000000000000000000, 0.000000000000000000, 0.000000000000000000 ) ) ;
#35464=EDGE_CURVE ( 'NONE', #40215, #11148, #14754, .T. ) ;
#35466=CYLINDRICAL_SURFACE ( 'NONE', #38210, 82.00000000000000000 ) ;
#35467=VECTOR ( 'NONE', #46885, 1000.000000000000000 ) ;
#35475=EDGE_CURVE ( 'NONE', #41750, #2177, #24860, .T. ) ;
#35477=ADVANCED_FACE ( 'NONE', ( #38728 ), #37992, .T. ) ;
#35478=LINE ( 'NONE', #31100, #25096 ) ;
#35480=CIRCLE ( 'NONE', #26125, 82.00000000000000000 ) ;
#35482=ORIENTED_EDGE ( 'NONE', *, *, #30195, .F. ) ;
#35484=EDGE_LOOP ( 'NONE', ( #13696, #9938, #45993, #12441 ) ) ;
#35485=CIRCLE ( 'NONE', #4233, 77.49900000000000944 ) ;
#35487=AXIS2_PLACEMENT_3D ( 'NONE', #29860, #26681, #4642 ) ;
#35488=VECTOR ( 'NONE', #35856, 1000.000000000000000 ) ;
#35489=CYLINDRICAL_SURFACE ( 'NONE', #41866, 77.49899999999999523 ) ;
#35490=DIRECTION ( 'NONE',  ( 0.000000000000000000, -0.8910065241883722287, 0.4539904997395383113 ) ) ;
#35491=AXIS2_PLACEMENT_3D ( 'NONE', #38488, #4954, #35287 ) ;
#35492=ORIENTED_EDGE ( 'NONE', *, *, #39582, .T. ) ;
#35497=CARTESIAN_POINT ( 'NONE',  ( 11.99999999999999822, -77.49459641780886443, -0.8261519478439277586 ) ) ;
#35506=DIRECTION ( 'NONE',  ( -1.000000000000000000, 0.000000000000000000, -0.000000000000000000 ) ) ;
#35507=DIRECTION ( 'NONE',  ( 0.000000000000000000, 0.6494480483301793283, 0.7604059656000345946 ) ) ;
#35511=DIRECTION ( 'NONE',  ( -1.000000000000000000, 0.000000000000000000, 0.000000000000000000 ) ) ;
#35519=CARTESIAN_POINT ( 'NONE',  ( 11.99999999999999822, -30.41916302227164337, 71.27951684758015460 ) ) ;
#35523=EDGE_CURVE ( 'NONE', #41773, #25899, #41917, .T. ) ;
#35531=DIRECTION ( 'NONE',  ( 0.000000000000000000, 0.6494480483301849905, -0.7604059656000298206 ) ) ;
#35534=EDGE_LOOP ( 'NONE', ( #16476, #9832, #21623, #1358 ) ) ;
#35536=ORIENTED_EDGE ( 'NONE', *, *, #7361, .T. ) ;
#35541=EDGE_CURVE ( 'NONE', #19547, #22184, #31627, .T. ) ;
#35542=ADVANCED_FACE ( 'NONE', ( #31385 ), #38963, .T. ) ;
#35543=CIRCLE ( 'NONE', #14443, 77.49900000000000944 ) ;
#35548=LINE ( 'NONE', #12550, #19966 ) ;
#35549=AXIS2_PLACEMENT_3D ( 'NONE', #44850, #15716, #38000 ) ;
#35555=EDGE_CURVE ( 'NONE', #2082, #42556, #15474, .T. ) ;
#35556=DIRECTION ( 'NONE',  ( 0.000000000000000000, 0.000000000000000000, 1.000000000000000000 ) ) ;
#35557=VERTEX_POINT ( 'NONE', #38467 ) ;
#35559=ORIENTED_EDGE ( 'NONE', *, *, #47722, .T. ) ;
#35563=DIRECTION ( 'NONE',  ( -1.000000000000000000, 0.000000000000000000, 0.000000000000000000 ) ) ;
#35566=LINE ( 'NONE', #35314, #41496 ) ;
#35570=AXIS2_PLACEMENT_3D ( 'NONE', #35375, #8695, #12164 ) ;
#35572=AXIS2_PLACEMENT_3D ( 'NONE', #4898, #1241, #34031 ) ;
#35575=FACE_OUTER_BOUND ( 'NONE', #37609, .T. ) ;
#35578=DIRECTION ( 'NONE',  ( -1.000000000000000000, -0.000000000000000000, 0.000000000000000000 ) ) ;
#35580=CARTESIAN_POINT ( 'NONE',  ( 15.00000000000000000, 0.000000000000000000, 0.000000000000000000 ) ) ;
#35584=FACE_OUTER_BOUND ( 'NONE', #44099, .T. ) ;
#35586=DIRECTION ( 'NONE',  ( 0.000000000000000000, 0.9510565162951523099, 0.3090169943749516146 ) ) ;
#35588=EDGE_CURVE ( 'NONE', #39158, #2161, #8122, .T. ) ;
#35589=CYLINDRICAL_SURFACE ( 'NONE', #3331, 82.00000000000000000 ) ;
#35591=ORIENTED_EDGE ( 'NONE', *, *, #26269, .F. ) ;
#35592=CIRCLE ( 'NONE', #36355, 31.99999999999998934 ) ;
#35593=VECTOR ( 'NONE', #14048, 1000.000000000000000 ) ;
#35594=EDGE_CURVE ( 'NONE', #19983, #42640, #4568, .T. ) ;
#35597=ORIENTED_EDGE ( 'NONE', *, *, #3557, .T. ) ;
#35599=AXIS2_PLACEMENT_3D ( 'NONE', #42730, #38090, #12386 ) ;
#35600=AXIS2_PLACEMENT_3D ( 'NONE', #34266, #23023, #26700 ) ;
#35605=CARTESIAN_POINT ( 'NONE',  ( 11.99999999999999822, 29.01471420065563933, 76.69515212746024702 ) ) ;
#35610=ORIENTED_EDGE ( 'NONE', *, *, #45996, .F. ) ;
#35623=CARTESIAN_POINT ( 'NONE',  ( 0.000000000000000000, 2.956366410620650420, 75.11725578898469280 ) ) ;
#35625=CARTESIAN_POINT ( 'NONE',  ( 11.99999999999999822, 58.39081064771822582, -50.95692526931267707 ) ) ;
#35632=ORIENTED_EDGE ( 'NONE', *, *, #4706, .F. ) ;
#35636=DIRECTION ( 'NONE',  ( -1.000000000000000000, -0.000000000000000000, 0.000000000000000000 ) ) ;
#35639=LINE ( 'NONE', #17027, #38920 ) ;
#35645=DIRECTION ( 'NONE',  ( -1.000000000000000000, -0.000000000000000000, -0.000000000000000000 ) ) ;
#35653=ORIENTED_EDGE ( 'NONE', *, *, #10550, .F. ) ;
#35660=VERTEX_POINT ( 'NONE', #28659 ) ;
#35661=AXIS2_PLACEMENT_3D ( 'NONE', #25416, #10747, #10979 ) ;
#35662=DIRECTION ( 'NONE',  ( -1.000000000000000000, -0.000000000000000000, -0.000000000000000000 ) ) ;
#35663=DIRECTION ( 'NONE',  ( 0.000000000000000000, -0.4067366430757899942, 0.9135454576426055295 ) ) ;
#35669=CYLINDRICAL_SURFACE ( 'NONE', #46201, 82.00000000000000000 ) ;
#35673=VERTEX_POINT ( 'NONE', #39193 ) ;
#35675=CARTESIAN_POINT ( 'NONE',  ( 11.99999999999999822, 59.03961581697399907, 46.53671651293969802 ) ) ;
#35679=AXIS2_PLACEMENT_3D ( 'NONE', #27093, #8706, #5055 ) ;
#35683=EDGE_CURVE ( 'NONE', #4413, #913, #20575, .T. ) ;
#35685=ORIENTED_EDGE ( 'NONE', *, *, #16813, .F. ) ;
#35691=DIRECTION ( 'NONE',  ( -1.000000000000000000, 0.000000000000000000, 0.000000000000000000 ) ) ;
#35696=EDGE_LOOP ( 'NONE', ( #25283, #31286, #7049, #26866 ) ) ;
#35699=CARTESIAN_POINT ( 'NONE',  ( 15.00000000000000000, 26.49999999999999645, 1.499999999999995781 ) ) ;
#35701=DIRECTION ( 'NONE',  ( -1.000000000000000000, 0.000000000000000000, -0.000000000000000000 ) ) ;
#35704=EDGE_CURVE ( 'NONE', #30959, #22184, #28168, .T. ) ;
#35708=ORIENTED_EDGE ( 'NONE', *, *, #38177, .T. ) ;
#35715=VERTEX_POINT ( 'NONE', #46456 ) ;
#35719=ORIENTED_EDGE ( 'NONE', *, *, #48028, .F. ) ;
#35720=VERTEX_POINT ( 'NONE', #16124 ) ;
#35722=CARTESIAN_POINT ( 'NONE',  ( 11.99999999999999822, 0.000000000000000000, 0.000000000000000000 ) ) ;
#35729=DIRECTION ( 'NONE',  ( -1.000000000000000000, -0.000000000000000000, -0.000000000000000000 ) ) ;
#35735=CYLINDRICAL_SURFACE ( 'NONE', #5584, 31.99999999999998579 ) ;
#35740=DIRECTION ( 'NONE',  ( 0.000000000000000000, -0.8090169943749504489, -0.5877852522924689183 ) ) ;
#35741=DIRECTION ( 'NONE',  ( -1.000000000000000000, 0.000000000000000000, -0.000000000000000000 ) ) ;
#35745=DIRECTION ( 'NONE',  ( 0.000000000000000000, 0.000000000000000000, 1.000000000000000000 ) ) ;
#35748=DIRECTION ( 'NONE',  ( 0.000000000000000000, 0.9510565162951521989, 0.3090169943749515591 ) ) ;
#35750=CARTESIAN_POINT ( 'NONE',  ( 11.99999999999999822, 74.65374052328660071, -8.840884882374309583 ) ) ;
#35751=ORIENTED_EDGE ( 'NONE', *, *, #1830, .F. ) ;
#35756=EDGE_CURVE ( 'NONE', #47844, #34450, #15501, .T. ) ;
#35759=EDGE_CURVE ( 'NONE', #33903, #21863, #2979, .T. ) ;
#35765=DIRECTION ( 'NONE',  ( 0.000000000000000000, -0.9876883405951394357, 0.1564344650402205716 ) ) ;
#35766=ADVANCED_FACE ( 'NONE', ( #27607 ), #38142, .T. ) ;
#35768=EDGE_CURVE ( 'NONE', #33272, #28804, #22559, .T. ) ;
#35774=ORIENTED_EDGE ( 'NONE', *, *, #39302, .F. ) ;
#35775=DIRECTION ( 'NONE',  ( 0.000000000000000000, -0.5000000000000028866, -0.8660254037844369313 ) ) ;
#35777=DIRECTION ( 'NONE',  ( -1.000000000000000000, 0.000000000000000000, 0.000000000000000000 ) ) ;
#35780=CARTESIAN_POINT ( 'NONE',  ( 11.99999999999999822, 11.30684508768450769, -76.66974797899825944 ) ) ;
#35782=VERTEX_POINT ( 'NONE', #31056 ) ;
#35785=ORIENTED_EDGE ( 'NONE', *, *, #10893, .T. ) ;
#35786=DIRECTION ( 'NONE',  ( -1.000000000000000000, 0.000000000000000000, 0.000000000000000000 ) ) ;
#35789=AXIS2_PLACEMENT_3D ( 'NONE', #26354, #29538, #18266 ) ;
#35790=CARTESIAN_POINT ( 'NONE',  ( 11.99999999999999822, 59.03961581697465277, -46.53671651293886669 ) ) ;
#35808=CARTESIAN_POINT ( 'NONE',  ( 11.99999999999999822, -58.39081064771786345, 50.95692526931308919 ) ) ;
#35809=CYLINDRICAL_SURFACE ( 'NONE', #26005, 31.99999999999998579 ) ;
#35810=FACE_BOUND ( 'NONE', #41083, .T. ) ;
#35815=DIRECTION ( 'NONE',  ( -1.000000000000000000, 0.000000000000000000, 0.000000000000000000 ) ) ;
#35819=EDGE_CURVE ( 'NONE', #22174, #35557, #7703, .T. ) ;
#35828=EDGE_CURVE ( 'NONE', #2924, #39337, #35056, .T. ) ;
#35834=DIRECTION ( 'NONE',  ( -1.000000000000000000, -0.000000000000000000, -0.000000000000000000 ) ) ;
#35840=ORIENTED_EDGE ( 'NONE', *, *, #22524, .F. ) ;
#35843=DIRECTION ( 'NONE',  ( -1.000000000000000000, -0.000000000000000000, -0.000000000000000000 ) ) ;
#35853=CARTESIAN_POINT ( 'NONE',  ( 0.000000000000000000, 0.000000000000000000, 0.000000000000000000 ) ) ;
#35855=EDGE_CURVE ( 'NONE', #41683, #352, #13162, .T. ) ;
#35856=DIRECTION ( 'NONE',  ( -1.000000000000000000, 0.000000000000000000, -0.000000000000000000 ) ) ;
#35860=DIRECTION ( 'NONE',  ( 0.000000000000000000, 0.8090169943749445647, 0.5877852522924770229 ) ) ;
#35863=CYLINDRICAL_SURFACE ( 'NONE', #30186, 31.99999999999998579 ) ;
#35864=CIRCLE ( 'NONE', #24134, 31.99999999999998579 ) ;
#35865=VECTOR ( 'NONE', #34398, 1000.000000000000114 ) ;
#35871=VERTEX_POINT ( 'NONE', #32712 ) ;
#35873=LINE ( 'NONE', #43222, #38637 ) ;
#35884=ORIENTED_EDGE ( 'NONE', *, *, #19347, .F. ) ;
#35888=CARTESIAN_POINT ( 'NONE',  ( 0.000000000000000000, 46.21855187248719687, -62.20884554313968806 ) ) ;
#35889=LINE ( 'NONE', #24877, #33178 ) ;
#35891=CIRCLE ( 'NONE', #3860, 31.99999999999998934 ) ;
#35892=VERTEX_POINT ( 'NONE', #28809 ) ;
#35894=ORIENTED_EDGE ( 'NONE', *, *, #40944, .F. ) ;
#35895=DIRECTION ( 'NONE',  ( -1.000000000000000000, -0.000000000000000000, -0.000000000000000000 ) ) ;
#35896=CARTESIAN_POINT ( 'NONE',  ( 11.99999999999999822, 75.11764819372142199, 2.946379043147685728 ) ) ;
#35899=ORIENTED_EDGE ( 'NONE', *, *, #18890, .T. ) ;
#35900=CIRCLE ( 'NONE', #21851, 31.99999999999998934 ) ;
#35912=EDGE_CURVE ( 'NONE', #43484, #25704, #2368, .T. ) ;
#35917=EDGE_LOOP ( 'NONE', ( #26673, #2836, #16023, #7844 ) ) ;
#35920=CARTESIAN_POINT ( 'NONE',  ( 11.99999999999999822, 26.02418014898310261, 70.52718814184268581 ) ) ;
#35922=EDGE_CURVE ( 'NONE', #26066, #48059, #10853, .T. ) ;
#35927=DIRECTION ( 'NONE',  ( -1.000000000000000000, 0.000000000000000000, 0.000000000000000000 ) ) ;
#35932=VERTEX_POINT ( 'NONE', #24407 ) ;
#35934=CARTESIAN_POINT ( 'NONE',  ( 0.000000000000000000, 60.67117009219215618, -55.16347631942977614 ) ) ;
#35935=VERTEX_POINT ( 'NONE', #47413 ) ;
#35938=EDGE_CURVE ( 'NONE', #43255, #6361, #37439, .T. ) ;
#35940=ORIENTED_EDGE ( 'NONE', *, *, #11997, .F. ) ;
#35941=VERTEX_POINT ( 'NONE', #17784 ) ;
#35943=CARTESIAN_POINT ( 'NONE',  ( 15.00000000000000000, -3.948201729842032215, 23.21447184625297666 ) ) ;
#35949=ORIENTED_EDGE ( 'NONE', *, *, #10622, .F. ) ;
#35951=ORIENTED_EDGE ( 'NONE', *, *, #43551, .F. ) ;
#35962=CARTESIAN_POINT ( 'NONE',  ( 0.000000000000000000, 75.11725578898472122, -2.956366410619845730 ) ) ;
#35968=AXIS2_PLACEMENT_3D ( 'NONE', #18689, #7450, #11843 ) ;
#35972=VECTOR ( 'NONE', #18075, 1000.000000000000000 ) ;
#35973=VERTEX_POINT ( 'NONE', #43301 ) ;
#35981=CARTESIAN_POINT ( 'NONE',  ( 12.00000000000000000, -0.9646360437372099028, 23.52805723605590771 ) ) ;
#35986=CARTESIAN_POINT ( 'NONE',  ( 15.00000000000000000, -10.45096189432344502, -21.10159698893425784 ) ) ;
#35992=CIRCLE ( 'NONE', #18788, 82.00000000000000000 ) ;
#35995=AXIS2_PLACEMENT_3D ( 'NONE', #36726, #6167, #36253 ) ;
#36001=CIRCLE ( 'NONE', #17269, 82.00000000000000000 ) ;
#36006=EDGE_CURVE ( 'NONE', #10618, #5001, #16335, .T. ) ;
#36007=ORIENTED_EDGE ( 'NONE', *, *, #7021, .T. ) ;
#36010=EDGE_LOOP ( 'NONE', ( #8516, #16618, #4649, #5761 ) ) ;
#36011=ADVANCED_FACE ( 'NONE', ( #31327 ), #38912, .T. ) ;
#36018=DIRECTION ( 'NONE',  ( -1.000000000000000000, -0.000000000000000000, -0.000000000000000000 ) ) ;
#36019=AXIS2_PLACEMENT_3D ( 'NONE', #4508, #16729, #46105 ) ;
#36027=VERTEX_POINT ( 'NONE', #9274 ) ;
#36028=EDGE_CURVE ( 'NONE', #12206, #59, #35864, .T. ) ;
#36029=DIRECTION ( 'NONE',  ( 0.000000000000000000, 0.7431448254773954654, 0.6691306063588569053 ) ) ;
#36038=LINE ( 'NONE', #33990, #33930 ) ;
#36042=DIRECTION ( 'NONE',  ( -0.000000000000000000, 0.8660254037844432595, 0.4999999999999921729 ) ) ;
#36045=DIRECTION ( 'NONE',  ( 0.000000000000000000, -0.5224985647159380298, -0.8526401643540988395 ) ) ;
#36050=ORIENTED_EDGE ( 'NONE', *, *, #13808, .F. ) ;
#36058=CARTESIAN_POINT ( 'NONE',  ( 0.000000000000000000, 76.66974797899835892, 11.30684508768366570 ) ) ;
#36062=CIRCLE ( 'NONE', #12637, 31.99999999999998579 ) ;
#36067=VERTEX_POINT ( 'NONE', #5372 ) ;
#36069=ORIENTED_EDGE ( 'NONE', *, *, #32268, .T. ) ;
#36071=CIRCLE ( 'NONE', #1702, 77.49900000000000944 ) ;
#36072=CARTESIAN_POINT ( 'NONE',  ( 0.000000000000000000, 74.65491531819118620, -8.830959090342659579 ) ) ;
#36082=ORIENTED_EDGE ( 'NONE', *, *, #42954, .T. ) ;
#36083=EDGE_CURVE ( 'NONE', #35253, #7167, #28835, .T. ) ;
#36087=DIRECTION ( 'NONE',  ( 0.000000000000000000, 0.000000000000000000, 1.000000000000000000 ) ) ;
#36090=VERTEX_POINT ( 'NONE', #2180 ) ;
#36091=ORIENTED_EDGE ( 'NONE', *, *, #4763, .T. ) ;
#36093=CARTESIAN_POINT ( 'NONE',  ( 0.000000000000000000, 0.000000000000000000, 0.000000000000000000 ) ) ;
#36094=CARTESIAN_POINT ( 'NONE',  ( 11.99999999999999822, 41.76106447765489094, 62.50884508063442269 ) ) ;
#36096=FACE_OUTER_BOUND ( 'NONE', #5727, .T. ) ;
#36106=VECTOR ( 'NONE', #21929, 1000.000000000000000 ) ;
#36109=CIRCLE ( 'NONE', #12671, 31.99999999999998934 ) ;
#36113=LINE ( 'NONE', #35144, #15186 ) ;
#36115=CARTESIAN_POINT ( 'NONE',  ( 0.000000000000000000, 0.000000000000000000, 0.000000000000000000 ) ) ;
#36116=AXIS2_PLACEMENT_3D ( 'NONE', #43785, #3137, #44275 ) ;
#36121=VERTEX_POINT ( 'NONE', #21502 ) ;
#36125=EDGE_CURVE ( 'NONE', #43252, #5777, #28613, .T. ) ;
#36131=ORIENTED_EDGE ( 'NONE', *, *, #43649, .F. ) ;
#36132=VERTEX_POINT ( 'NONE', #17579 ) ;
#36134=AXIS2_PLACEMENT_3D ( 'NONE', #8175, #23107, #38274 ) ;
#36136=ADVANCED_FACE ( 'NONE', ( #47667 ), #6569, .F. ) ;
#36137=DIRECTION ( 'NONE',  ( 0.000000000000000000, 0.9723699203976773342, -0.2334453638559024213 ) ) ;
#36146=AXIS2_PLACEMENT_3D ( 'NONE', #46181, #27580, #45701 ) ;
#36149=CARTESIAN_POINT ( 'NONE',  ( 15.00000000000000000, -19.89357724625003598, -12.59942793731059041 ) ) ;
#36151=EDGE_CURVE ( 'NONE', #45717, #30959, #7041, .T. ) ;
#36157=FACE_OUTER_BOUND ( 'NONE', #45594, .T. ) ;
#36165=ORIENTED_EDGE ( 'NONE', *, *, #2758, .F. ) ;
#36168=DIRECTION ( 'NONE',  ( -1.000000000000000000, -0.000000000000000000, -0.000000000000000000 ) ) ;
#36172=CIRCLE ( 'NONE', #27590, 82.00000000000000000 ) ;
#36174=ORIENTED_EDGE ( 'NONE', *, *, #23662, .T. ) ;
#36179=CARTESIAN_POINT ( 'NONE',  ( 15.00000000000000000, 20.85821328998741109, -10.92862929874522671 ) ) ;
#36181=ORIENTED_EDGE ( 'NONE', *, *, #6957, .T. ) ;
#36182=EDGE_CURVE ( 'NONE', #25081, #20359, #26474, .T. ) ;
#36183=ORIENTED_EDGE ( 'NONE', *, *, #42497, .T. ) ;
#36189=VECTOR ( 'NONE', #29384, 1000.000000000000000 ) ;
#36190=EDGE_CURVE ( 'NONE', #35058, #36090, #44495, .T. ) ;
#36194=DIRECTION ( 'NONE',  ( 0.000000000000000000, -0.3826834323650772363, -0.9238795325112919565 ) ) ;
#36195=EDGE_CURVE ( 'NONE', #24721, #13159, #18049, .T. ) ;
#36207=DIRECTION ( 'NONE',  ( 0.000000000000000000, 0.000000000000000000, -1.000000000000000000 ) ) ;
#36209=CARTESIAN_POINT ( 'NONE',  ( 15.00000000000000000, -13.04903810567646971, 19.60159698893442481 ) ) ;
#36214=CYLINDRICAL_SURFACE ( 'NONE', #44189, 31.99999999999998579 ) ;
#36215=ORIENTED_EDGE ( 'NONE', *, *, #46664, .T. ) ;
#36233=ORIENTED_EDGE ( 'NONE', *, *, #8697, .T. ) ;
#36234=EDGE_CURVE ( 'NONE', #24923, #25899, #36625, .T. ) ;
#36241=ORIENTED_EDGE ( 'NONE', *, *, #19751, .F. ) ;
#36243=VERTEX_POINT ( 'NONE', #21243 ) ;
#36246=EDGE_CURVE ( 'NONE', #23602, #32725, #30422, .T. ) ;
#36250=VERTEX_POINT ( 'NONE', #22943 ) ;
#36253=DIRECTION ( 'NONE',  ( 0.000000000000000000, 0.000000000000000000, -1.000000000000000000 ) ) ;
#36254=DIRECTION ( 'NONE',  ( -1.000000000000000000, -0.000000000000000000, 0.000000000000000000 ) ) ;
#36255=ORIENTED_EDGE ( 'NONE', *, *, #520, .T. ) ;
#36256=FACE_OUTER_BOUND ( 'NONE', #1347, .T. ) ;
#36257=VERTEX_POINT ( 'NONE', #30532 ) ;
#36261=LINE ( 'NONE', #28912, #8150 ) ;
#36262=DIRECTION ( 'NONE',  ( 0.000000000000000000, 0.000000000000000000, 1.000000000000000000 ) ) ;
#36264=CARTESIAN_POINT ( 'NONE',  ( 11.99999999999999822, -65.64334221924882229, -41.19522573413803457 ) ) ;
#36274=AXIS2_PLACEMENT_3D ( 'NONE', #34575, #1058, #30947 ) ;
#36275=CARTESIAN_POINT ( 'NONE',  ( 11.99999999999999822, 75.54627589209970040, -17.28742895386005785 ) ) ;
#36278=CARTESIAN_POINT ( 'NONE',  ( 11.99999999999999822, 0.000000000000000000, 0.000000000000000000 ) ) ;
#36279=CARTESIAN_POINT ( 'NONE',  ( 11.99999999999999822, -71.87247863392441616, 39.47590169984818687 ) ) ;
#36291=CIRCLE ( 'NONE', #15965, 82.00000000000000000 ) ;
#36292=CARTESIAN_POINT ( 'NONE',  ( 12.00000000000000000, -4.261787119644964150, 26.19803753235780164 ) ) ;
#36293=FACE_OUTER_BOUND ( 'NONE', #21277, .T. ) ;
#36300=ORIENTED_EDGE ( 'NONE', *, *, #1397, .T. ) ;
#36301=CARTESIAN_POINT ( 'NONE',  ( 11.99999999999999822, -74.65374052328654386, 8.840884882374837161 ) ) ;
#36304=CARTESIAN_POINT ( 'NONE',  ( 11.99999999999999822, -22.90783923731575200, -78.73519480814978522 ) ) ;
#36307=PLANE ( 'NONE',  #19738 ) ;
#36308=ORIENTED_EDGE ( 'NONE', *, *, #40951, .F. ) ;
#36309=VECTOR ( 'NONE', #45079, 1000.000000000000000 ) ;
#36311=VECTOR ( 'NONE', #38073, 1000.000000000000000 ) ;
#36316=EDGE_LOOP ( 'NONE', ( #33565, #26999, #24786, #42929 ) ) ;
#36317=VECTOR ( 'NONE', #25592, 1000.000000000000000 ) ;
#36320=CYLINDRICAL_SURFACE ( 'NONE', #17193, 31.99999999999998579 ) ;
#36325=CIRCLE ( 'NONE', #14460, 31.99999999999998579 ) ;
#36327=CIRCLE ( 'NONE', #46509, 77.49899999999999523 ) ;
#36335=CARTESIAN_POINT ( 'NONE',  ( 0.000000000000000000, -23.16143007188376757, -73.95703589263997912 ) ) ;
#36336=DIRECTION ( 'NONE',  ( -1.000000000000000000, 0.000000000000000000, 0.000000000000000000 ) ) ;
#36337=DIRECTION ( 'NONE',  ( -1.000000000000000000, -0.000000000000000000, 0.000000000000000000 ) ) ;
#36339=LINE ( 'NONE', #47371, #12003 ) ;
#36341=DIRECTION ( 'NONE',  ( 0.000000000000000000, 0.000000000000000000, 1.000000000000000000 ) ) ;
#36349=CIRCLE ( 'NONE', #42617, 31.99999999999999645 ) ;
#36353=EDGE_CURVE ( 'NONE', #46432, #22825, #15129, .T. ) ;
#36355=AXIS2_PLACEMENT_3D ( 'NONE', #41992, #34613, #1097 ) ;
#36359=VERTEX_POINT ( 'NONE', #25880 ) ;
#36362=EDGE_CURVE ( 'NONE', #20992, #39592, #10119, .T. ) ;
#36363=CARTESIAN_POINT ( 'NONE',  ( 0.000000000000000000, 31.47745569255140552, 68.26794271651274926 ) ) ;
#36367=EDGE_CURVE ( 'NONE', #925, #5623, #4362, .T. ) ;
#36373=EDGE_CURVE ( 'NONE', #15803, #9234, #46847, .T. ) ;
#36377=AXIS2_PLACEMENT_3D ( 'NONE', #24080, #10104, #39244 ) ;
#36378=CARTESIAN_POINT ( 'NONE',  ( 0.000000000000000000, 79.10210256391368944, 21.60688246758614994 ) ) ;
#36379=DIRECTION ( 'NONE',  ( -1.000000000000000000, 0.000000000000000000, 0.000000000000000000 ) ) ;
#36380=DIRECTION ( 'NONE',  ( 0.000000000000000000, 0.000000000000000000, 1.000000000000000000 ) ) ;
#36385=VERTEX_POINT ( 'NONE', #1895 ) ;
#36387=DIRECTION ( 'NONE',  ( -1.000000000000000000, -0.000000000000000000, 0.000000000000000000 ) ) ;
#36388=ORIENTED_EDGE ( 'NONE', *, *, #27757, .F. ) ;
#36403=ADVANCED_FACE ( 'NONE', ( #8728 ), #34670, .F. ) ;
#36405=CARTESIAN_POINT ( 'NONE',  ( 6.000000000000000000, 81.90746397400393164, -3.894527615416979671 ) ) ;
#36411=CARTESIAN_POINT ( 'NONE',  ( 11.99999999999999822, 54.21277698773752007, -55.38113227695726692 ) ) ;
#36412=CIRCLE ( 'NONE', #1274, 77.49900000000000944 ) ;
#36417=DIRECTION ( 'NONE',  ( 0.000000000000000000, 0.000000000000000000, 1.000000000000000000 ) ) ;
#36422=VERTEX_POINT ( 'NONE', #27848 ) ;
#36429=DIRECTION ( 'NONE',  ( -0.000000000000000000, 0.5000000000000038858, 0.8660254037844363761 ) ) ;
#36432=VERTEX_POINT ( 'NONE', #34924 ) ;
#36434=DIRECTION ( 'NONE',  ( 0.000000000000000000, 0.000000000000000000, 1.000000000000000000 ) ) ;
#36435=ORIENTED_EDGE ( 'NONE', *, *, #37189, .T. ) ;
#36442=EDGE_LOOP ( 'NONE', ( #11336, #12687, #7629, #43730 ) ) ;
#36443=CARTESIAN_POINT ( 'NONE',  ( 11.99999999999999822, -35.91791733033525702, 68.67312586194982771 ) ) ;
#36444=VERTEX_POINT ( 'NONE', #24384 ) ;
#36449=DIRECTION ( 'NONE',  ( -1.000000000000000000, 0.000000000000000000, -0.000000000000000000 ) ) ;
#36455=VERTEX_POINT ( 'NONE', #12659 ) ;
#36457=DIRECTION ( 'NONE',  ( 0.000000000000000000, 0.000000000000000000, 1.000000000000000000 ) ) ;
#36462=CARTESIAN_POINT ( 'NONE',  ( 11.99999999999999822, -63.18004540533059554, 44.88180994100355292 ) ) ;
#36469=DIRECTION ( 'NONE',  ( 0.000000000000000000, 0.000000000000000000, -1.000000000000000000 ) ) ;
#36475=ORIENTED_EDGE ( 'NONE', *, *, #16813, .T. ) ;
#36476=EDGE_CURVE ( 'NONE', #23651, #25704, #12190, .T. ) ;
#36480=EDGE_CURVE ( 'NONE', #13485, #18192, #46434, .T. ) ;
#36481=LINE ( 'NONE', #43591, #46364 ) ;
#36482=CARTESIAN_POINT ( 'NONE',  ( 11.99999999999999822, 0.000000000000000000, 0.000000000000000000 ) ) ;
#36489=AXIS2_PLACEMENT_3D ( 'NONE', #5601, #35448, #21231 ) ;
#36490=ORIENTED_EDGE ( 'NONE', *, *, #507, .F. ) ;
#36492=PLANE ( 'NONE',  #46180 ) ;
#36493=AXIS2_PLACEMENT_3D ( 'NONE', #5974, #27274, #42189 ) ;
#36495=ORIENTED_EDGE ( 'NONE', *, *, #45697, .F. ) ;
#36497=ORIENTED_EDGE ( 'NONE', *, *, #32760, .T. ) ;
#36509=CARTESIAN_POINT ( 'NONE',  ( 6.000000000000000000, -78.73519480814971416, 22.90783923731599359 ) ) ;
#36510=ORIENTED_EDGE ( 'NONE', *, *, #31936, .T. ) ;
#36511=EDGE_LOOP ( 'NONE', ( #26884, #23182, #8372, #16582 ) ) ;
#36518=VERTEX_POINT ( 'NONE', #6280 ) ;
#36520=CARTESIAN_POINT ( 'NONE',  ( 0.000000000000000000, 0.000000000000000000, 0.000000000000000000 ) ) ;
#36521=ADVANCED_FACE ( 'NONE', ( #10181 ), #14339, .T. ) ;
#36522=DIRECTION ( 'NONE',  ( -1.000000000000000000, 0.000000000000000000, -0.000000000000000000 ) ) ;
#36525=CIRCLE ( 'NONE', #574, 31.99999999999998579 ) ;
#36528=DIRECTION ( 'NONE',  ( -1.000000000000000000, -0.000000000000000000, -0.000000000000000000 ) ) ;
#36529=CARTESIAN_POINT ( 'NONE',  ( 12.00000000000000000, -22.32062822937469093, 14.36278369418830181 ) ) ;
#36530=EDGE_CURVE ( 'NONE', #45738, #461, #35891, .T. ) ;
#36534=CARTESIAN_POINT ( 'NONE',  ( 11.99999999999999822, -68.55367621811110723, -44.99326035066126650 ) ) ;
#36535=CARTESIAN_POINT ( 'NONE',  ( 15.00000000000000000, -25.60904388321916159, 6.976881207771517879 ) ) ;
#36540=CARTESIAN_POINT ( 'NONE',  ( -10.00000000000000000, 0.000000000000000000, 0.000000000000000000 ) ) ;
#36541=VECTOR ( 'NONE', #8587, 999.9999999999998863 ) ;
#36550=FACE_OUTER_BOUND ( 'NONE', #38310, .T. ) ;
#36551=ORIENTED_EDGE ( 'NONE', *, *, #22343, .T. ) ;
#36552=ORIENTED_EDGE ( 'NONE', *, *, #32056, .T. ) ;
#36554=VERTEX_POINT ( 'NONE', #17763 ) ;
#36564=EDGE_CURVE ( 'NONE', #39485, #33288, #6512, .T. ) ;
#36567=ORIENTED_EDGE ( 'NONE', *, *, #38632, .F. ) ;
#36568=ORIENTED_EDGE ( 'NONE', *, *, #20944, .F. ) ;
#36575=EDGE_CURVE ( 'NONE', #37777, #18965, #30458, .T. ) ;
#36581=AXIS2_PLACEMENT_3D ( 'NONE', #5037, #862, #15809 ) ;
#36587=CARTESIAN_POINT ( 'NONE',  ( 0.000000000000000000, 71.27951684758068041, -30.41916302227036439 ) ) ;
#36588=CARTESIAN_POINT ( 'NONE',  ( 11.99999999999999822, 50.95692526931329525, 58.39081064771768581 ) ) ;
#36590=AXIS2_PLACEMENT_3D ( 'NONE', #42360, #5894, #46039 ) ;
#36592=DIRECTION ( 'NONE',  ( -1.000000000000000000, 0.000000000000000000, -0.000000000000000000 ) ) ;
#36597=CYLINDRICAL_SURFACE ( 'NONE', #38493, 77.49899999999999523 ) ;
#36598=ORIENTED_EDGE ( 'NONE', *, *, #46431, .F. ) ;
#36600=DIRECTION ( 'NONE',  ( -1.000000000000000000, -0.000000000000000000, -0.000000000000000000 ) ) ;
#36603=CIRCLE ( 'NONE', #46798, 82.00000000000000000 ) ;
#36607=FACE_OUTER_BOUND ( 'NONE', #6400, .T. ) ;
#36609=ORIENTED_EDGE ( 'NONE', *, *, #27886, .T. ) ;
#36610=CARTESIAN_POINT ( 'NONE',  ( 11.99999999999999822, -29.01471420065616513, 76.69515212746006227 ) ) ;
#36611=ORIENTED_EDGE ( 'NONE', *, *, #1548, .T. ) ;
#36613=ORIENTED_EDGE ( 'NONE', *, *, #17949, .F. ) ;
#36614=CARTESIAN_POINT ( 'NONE',  ( 11.99999999999999822, 8.840884882375075193, 74.65374052328651544 ) ) ;
#36617=CARTESIAN_POINT ( 'NONE',  ( 12.00000000000000000, -14.54903810567676636, -22.19967320028756674 ) ) ;
#36618=ORIENTED_EDGE ( 'NONE', *, *, #13912, .T. ) ;
#36624=DIRECTION ( 'NONE',  ( 0.000000000000000000, -0.7604059656000369261, 0.6494480483301766638 ) ) ;
#36625=CIRCLE ( 'NONE', #33550, 31.99999999999998579 ) ;
#36630=EDGE_CURVE ( 'NONE', #16364, #25709, #1568, .T. ) ;
#36636=DIRECTION ( 'NONE',  ( -1.000000000000000000, -0.000000000000000000, -0.000000000000000000 ) ) ;
#36641=CARTESIAN_POINT ( 'NONE',  ( 0.000000000000000000, 0.000000000000000000, 0.000000000000000000 ) ) ;
#36644=DIRECTION ( 'NONE',  ( -1.000000000000000000, 0.000000000000000000, -0.000000000000000000 ) ) ;
#36646=CARTESIAN_POINT ( 'NONE',  ( 0.000000000000000000, 0.000000000000000000, 0.000000000000000000 ) ) ;
#36662=ADVANCED_FACE ( 'NONE', ( #37091 ), #15318, .F. ) ;
#36663=CARTESIAN_POINT ( 'NONE',  ( 0.000000000000000000, 20.41045688087930898, -72.35160999960793049 ) ) ;
#36666=ORIENTED_EDGE ( 'NONE', *, *, #28074, .F. ) ;
#36670=ORIENTED_EDGE ( 'NONE', *, *, #32508, .T. ) ;
#36673=ORIENTED_EDGE ( 'NONE', *, *, #26139, .F. ) ;
#36675=CARTESIAN_POINT ( 'NONE',  ( 11.99999999999999822, 39.78640506895698792, -66.50666863321958999 ) ) ;
#36688=CARTESIAN_POINT ( 'NONE',  ( 11.99999999999999822, 68.67312586195046720, -35.91791733033404199 ) ) ;
#36690=ORIENTED_EDGE ( 'NONE', *, *, #20213, .F. ) ;
#36695=DIRECTION ( 'NONE',  ( 0.000000000000000000, 0.000000000000000000, 1.000000000000000000 ) ) ;
#36696=DIRECTION ( 'NONE',  ( 0.000000000000000000, 0.000000000000000000, -1.000000000000000000 ) ) ;
#36698=CARTESIAN_POINT ( 'NONE',  ( 11.99999999999999822, 0.000000000000000000, 0.000000000000000000 ) ) ;
#36707=ORIENTED_EDGE ( 'NONE', *, *, #47304, .F. ) ;
#36708=EDGE_LOOP ( 'NONE', ( #20855, #23005, #34428, #42220 ) ) ;
#36711=CYLINDRICAL_SURFACE ( 'NONE', #14393, 82.00000000000000000 ) ;
#36715=AXIS2_PLACEMENT_3D ( 'NONE', #18903, #45117, #23078 ) ;
#36719=CIRCLE ( 'NONE', #43000, 31.99999999999999645 ) ;
#36722=ORIENTED_EDGE ( 'NONE', *, *, #35555, .F. ) ;
#36726=CARTESIAN_POINT ( 'NONE',  ( 0.000000000000000000, 72.35432306680455383, 20.40083707023012494 ) ) ;
#36738=CARTESIAN_POINT ( 'NONE',  ( 11.99999999999999822, 0.000000000000000000, 0.000000000000000000 ) ) ;
#36739=CARTESIAN_POINT ( 'NONE',  ( 11.99999999999999822, 0.000000000000000000, 0.000000000000000000 ) ) ;
#36740=VERTEX_POINT ( 'NONE', #26073 ) ;
#36742=ORIENTED_EDGE ( 'NONE', *, *, #38291, .T. ) ;
#36747=CARTESIAN_POINT ( 'NONE',  ( 0.000000000000000000, 41.76106447765580043, -62.50884508063379741 ) ) ;
#36769=CIRCLE ( 'NONE', #25822, 77.49900000000000944 ) ;
#36773=ORIENTED_EDGE ( 'NONE', *, *, #42534, .T. ) ;
#36778=DIRECTION ( 'NONE',  ( 0.000000000000000000, 0.07845909572783793529, 0.9969173337331285190 ) ) ;
#36780=ORIENTED_EDGE ( 'NONE', *, *, #36195, .T. ) ;
#36781=ORIENTED_EDGE ( 'NONE', *, *, #2930, .F. ) ;
#36786=EDGE_CURVE ( 'NONE', #15331, #22290, #47277, .T. ) ;
#36788=CARTESIAN_POINT ( 'NONE',  ( 15.00000000000000000, -0.9646360437372099028, 23.52805723605590771 ) ) ;
#36790=CIRCLE ( 'NONE', #15707, 77.49900000000002365 ) ;
#36791=ORIENTED_EDGE ( 'NONE', *, *, #19661, .F. ) ;
#36792=DIRECTION ( 'NONE',  ( 0.000000000000000000, 0.000000000000000000, 1.000000000000000000 ) ) ;
#36800=DIRECTION ( 'NONE',  ( -1.000000000000000000, 0.000000000000000000, 0.000000000000000000 ) ) ;
#36803=DIRECTION ( 'NONE',  ( -1.000000000000000000, 0.000000000000000000, 0.000000000000000000 ) ) ;
#36808=LINE ( 'NONE', #21401, #19920 ) ;
#36810=CARTESIAN_POINT ( 'NONE',  ( 11.99999999999999822, 36.73666225445988687, -65.58780272294035285 ) ) ;
#36819=CARTESIAN_POINT ( 'NONE',  ( 12.00000000000000000, 14.60985201121703980, -18.46759930825707841 ) ) ;
#36825=LINE ( 'NONE', #44185, #32595 ) ;
#36827=AXIS2_PLACEMENT_3D ( 'NONE', #9411, #1107, #2087 ) ;
#36830=CIRCLE ( 'NONE', #4002, 82.00000000000000000 ) ;
#36832=DIRECTION ( 'NONE',  ( 0.000000000000000000, 0.000000000000000000, 1.000000000000000000 ) ) ;
#36841=ADVANCED_FACE ( 'NONE', ( #9106 ), #39457, .T. ) ;
#36843=CARTESIAN_POINT ( 'NONE',  ( 11.99999999999999822, -72.35160999960831418, 20.41045688087797672 ) ) ;
#36845=DIRECTION ( 'NONE',  ( 0.000000000000000000, 0.000000000000000000, 1.000000000000000000 ) ) ;
#36847=ORIENTED_EDGE ( 'NONE', *, *, #44378, .T. ) ;
#36849=EDGE_LOOP ( 'NONE', ( #6330, #30471, #44163, #11492 ) ) ;
#36852=CARTESIAN_POINT ( 'NONE',  ( 11.99999999999999822, 0.000000000000000000, 0.000000000000000000 ) ) ;
#36853=CARTESIAN_POINT ( 'NONE',  ( 11.99999999999999822, 17.28742895386084655, 75.54627589209950145 ) ) ;
#36857=AXIS2_PLACEMENT_3D ( 'NONE', #45124, #30205, #40976 ) ;
#36859=VERTEX_POINT ( 'NONE', #24761 ) ;
#36860=DIRECTION ( 'NONE',  ( 0.000000000000000000, 0.5877852522924708056, -0.8090169943749491166 ) ) ;
#36865=CARTESIAN_POINT ( 'NONE',  ( 11.99999999999999822, -35.91791733033428358, -68.67312586195033930 ) ) ;
#36866=CARTESIAN_POINT ( 'NONE',  ( 11.99999999999999822, 74.74816331893428867, 33.71516098798767302 ) ) ;
#36869=AXIS2_PLACEMENT_3D ( 'NONE', #32497, #17303, #13408 ) ;
#36873=VERTEX_POINT ( 'NONE', #12137 ) ;
#36874=CARTESIAN_POINT ( 'NONE',  ( 11.99999999999999822, 64.81221759200343513, 50.23322058963371006 ) ) ;
#36876=ORIENTED_EDGE ( 'NONE', *, *, #9783, .F. ) ;
#36877=DIRECTION ( 'NONE',  ( -1.000000000000000000, 0.000000000000000000, -0.000000000000000000 ) ) ;
#36879=CARTESIAN_POINT ( 'NONE',  ( 11.99999999999999822, 62.20884554314085335, -46.21855187248562657 ) ) ;
#36886=ORIENTED_EDGE ( 'NONE', *, *, #18885, .T. ) ;
#36893=EDGE_CURVE ( 'NONE', #25146, #4907, #39706, .T. ) ;
#36895=ORIENTED_EDGE ( 'NONE', *, *, #38639, .T. ) ;
#36909=DIRECTION ( 'NONE',  ( -1.000000000000000000, -0.000000000000000000, -0.000000000000000000 ) ) ;
#36912=VERTEX_POINT ( 'NONE', #16934 ) ;
#36919=ORIENTED_EDGE ( 'NONE', *, *, #28149, .F. ) ;
#36921=DIRECTION ( 'NONE',  ( -1.000000000000000000, 0.000000000000000000, -0.000000000000000000 ) ) ;
#36925=AXIS2_PLACEMENT_3D ( 'NONE', #22491, #38384, #34216 ) ;
#36926=DIRECTION ( 'NONE',  ( 0.000000000000000000, -0.9969173337331287410, 0.07845909572783489605 ) ) ;
#36927=CARTESIAN_POINT ( 'NONE',  ( 0.000000000000000000, 8.840884882375075193, 74.65374052328651544 ) ) ;
#36939=DIRECTION ( 'NONE',  ( 0.000000000000000000, 0.9510565162951503115, -0.3090169943749573878 ) ) ;
#36941=ADVANCED_FACE ( 'NONE', ( #29863 ), #33299, .T. ) ;
#36945=CARTESIAN_POINT ( 'NONE',  ( 11.99999999999999822, -12.93880638057260946, -76.41127070299286572 ) ) ;
#36948=LINE ( 'NONE', #3425, #2627 ) ;
#36957=ORIENTED_EDGE ( 'NONE', *, *, #10498, .F. ) ;
#36964=DIRECTION ( 'NONE',  ( 0.000000000000000000, -0.9510565162951502005, -0.3090169943749581094 ) ) ;
#36969=ORIENTED_EDGE ( 'NONE', *, *, #33866, .T. ) ;
#36972=AXIS2_PLACEMENT_3D ( 'NONE', #10613, #7419, #44616 ) ;
#36975=CYLINDRICAL_SURFACE ( 'NONE', #16038, 77.49899999999999523 ) ;
#36976=DIRECTION ( 'NONE',  ( 0.000000000000000000, 0.000000000000000000, 1.000000000000000000 ) ) ;
#36977=VERTEX_POINT ( 'NONE', #33050 ) ;
#36978=DIRECTION ( 'NONE',  ( -1.000000000000000000, 0.000000000000000000, 0.000000000000000000 ) ) ;
#36981=DIRECTION ( 'NONE',  ( -1.000000000000000000, -0.000000000000000000, -0.000000000000000000 ) ) ;
#36982=ORIENTED_EDGE ( 'NONE', *, *, #45996, .T. ) ;
#36983=DIRECTION ( 'NONE',  ( -1.000000000000000000, 0.000000000000000000, 0.000000000000000000 ) ) ;
#36986=ORIENTED_EDGE ( 'NONE', *, *, #17681, .F. ) ;
#36987=ORIENTED_EDGE ( 'NONE', *, *, #47138, .T. ) ;
#36990=CARTESIAN_POINT ( 'NONE',  ( 11.99999999999999822, -39.78640506895651896, 66.50666863321988842 ) ) ;
#36991=CARTESIAN_POINT ( 'NONE',  ( 0.000000000000000000, 12.93880638057426502, -76.41127070299258150 ) ) ;
#36998=FACE_OUTER_BOUND ( 'NONE', #17225, .T. ) ;
#37000=EDGE_CURVE ( 'NONE', #2082, #35557, #25942, .T. ) ;
#37002=DIRECTION ( 'NONE',  ( -0.000000000000000000, 0.8090169943749503378, 0.5877852522924690293 ) ) ;
#37004=DIRECTION ( 'NONE',  ( -1.000000000000000000, 0.000000000000000000, -0.000000000000000000 ) ) ;
#37008=DIRECTION ( 'NONE',  ( -1.000000000000000000, -0.000000000000000000, 0.000000000000000000 ) ) ;
#37016=FACE_OUTER_BOUND ( 'NONE', #24034, .T. ) ;
#37020=DIRECTION ( 'NONE',  ( 0.000000000000000000, 0.000000000000000000, 1.000000000000000000 ) ) ;
#37023=VERTEX_POINT ( 'NONE', #3184 ) ;
#37030=VERTEX_POINT ( 'NONE', #25466 ) ;
#37033=AXIS2_PLACEMENT_3D ( 'NONE', #18138, #22326, #33080 ) ;
#37034=LINE ( 'NONE', #14283, #37829 ) ;
#37043=ORIENTED_EDGE ( 'NONE', *, *, #47708, .F. ) ;
#37048=CIRCLE ( 'NONE', #24557, 82.00000000000000000 ) ;
#37049=AXIS2_PLACEMENT_3D ( 'NONE', #12297, #7876, #42381 ) ;
#37052=ORIENTED_EDGE ( 'NONE', *, *, #2306, .F. ) ;
#37053=ORIENTED_EDGE ( 'NONE', *, *, #41548, .F. ) ;
#37056=CARTESIAN_POINT ( 'NONE',  ( 0.000000000000000000, 50.23322058963442061, -64.81221759200289512 ) ) ;
#37059=ORIENTED_EDGE ( 'NONE', *, *, #5426, .T. ) ;
#37062=CARTESIAN_POINT ( 'NONE',  ( 11.99999999999999822, 0.000000000000000000, 0.000000000000000000 ) ) ;
#37067=CARTESIAN_POINT ( 'NONE',  ( 11.99999999999999822, 20.40083707022882820, 72.35432306680490910 ) ) ;
#37069=EDGE_CURVE ( 'NONE', #34359, #25700, #27282, .T. ) ;
#37079=VECTOR ( 'NONE', #14271, 1000.000000000000000 ) ;
#37080=VECTOR ( 'NONE', #30932, 1000.000000000000000 ) ;
#37081=DIRECTION ( 'NONE',  ( -1.000000000000000000, 0.000000000000000000, 0.000000000000000000 ) ) ;
#37083=ADVANCED_FACE ( 'NONE', ( #26205 ), #30594, .F. ) ;
#37084=ORIENTED_EDGE ( 'NONE', *, *, #47127, .T. ) ;
#37087=CIRCLE ( 'NONE', #325, 82.00000000000000000 ) ;
#37088=ADVANCED_FACE ( 'NONE', ( #501 ), #19550, .F. ) ;
#37090=CIRCLE ( 'NONE', #16000, 82.00000000000000000 ) ;
#37091=FACE_OUTER_BOUND ( 'NONE', #19248, .T. ) ;
#37092=VERTEX_POINT ( 'NONE', #8547 ) ;
#37094=EDGE_CURVE ( 'NONE', #44946, #19509, #15194, .T. ) ;
#37099=VERTEX_POINT ( 'NONE', #23253 ) ;
#37100=LINE ( 'NONE', #7494, #3921 ) ;
#37105=AXIS2_PLACEMENT_3D ( 'NONE', #9257, #9023, #42562 ) ;
#37108=ORIENTED_EDGE ( 'NONE', *, *, #35261, .T. ) ;
#37109=DIRECTION ( 'NONE',  ( 0.000000000000000000, -0.4999999999999930611, 0.8660254037844425934 ) ) ;
#37111=AXIS2_PLACEMENT_3D ( 'NONE', #37782, #23098, #583 ) ;
#37115=FACE_OUTER_BOUND ( 'NONE', #17884, .T. ) ;
#37117=CARTESIAN_POINT ( 'NONE',  ( 11.99999999999999822, 0.000000000000000000, 0.000000000000000000 ) ) ;
#37119=CYLINDRICAL_SURFACE ( 'NONE', #45702, 31.99999999999998579 ) ;
#37121=CARTESIAN_POINT ( 'NONE',  ( 5.999999999999999112, -51.29473840253177030, -63.97538442413482329 ) ) ;
#37125=EDGE_CURVE ( 'NONE', #31325, #23206, #45051, .T. ) ;
#37130=CARTESIAN_POINT ( 'NONE',  ( 0.000000000000000000, 70.53064760720316428, -26.01480285779861035 ) ) ;
#37134=EDGE_CURVE ( 'NONE', #5004, #20016, #17959, .T. ) ;
#37139=ORIENTED_EDGE ( 'NONE', *, *, #14130, .T. ) ;
#37140=DIRECTION ( 'NONE',  ( -1.000000000000000000, -0.000000000000000000, -0.000000000000000000 ) ) ;
#37148=ORIENTED_EDGE ( 'NONE', *, *, #39400, .T. ) ;
#37149=AXIS2_PLACEMENT_3D ( 'NONE', #13898, #29488, #25799 ) ;
#37152=ORIENTED_EDGE ( 'NONE', *, *, #21555, .F. ) ;
#37154=DIRECTION ( 'NONE',  ( 0.000000000000000000, -0.1564344650402170744, -0.9876883405951399908 ) ) ;
#37158=CIRCLE ( 'NONE', #22317, 31.99999999999998579 ) ;
#37165=DIRECTION ( 'NONE',  ( -1.000000000000000000, 0.000000000000000000, -0.000000000000000000 ) ) ;
#37168=ORIENTED_EDGE ( 'NONE', *, *, #7361, .F. ) ;
#37169=ORIENTED_EDGE ( 'NONE', *, *, #32268, .F. ) ;
#37175=DIRECTION ( 'NONE',  ( 0.000000000000000000, 0.000000000000000000, 1.000000000000000000 ) ) ;
#37178=PLANE ( 'NONE',  #3219 ) ;
#37182=DIRECTION ( 'NONE',  ( 0.000000000000000000, 0.000000000000000000, 1.000000000000000000 ) ) ;
#37183=CARTESIAN_POINT ( 'NONE',  ( 0.000000000000000000, -68.55367621811173251, 44.99326035066031437 ) ) ;
#37184=ORIENTED_EDGE ( 'NONE', *, *, #28463, .T. ) ;
#37188=DIRECTION ( 'NONE',  ( 0.000000000000000000, 0.000000000000000000, 1.000000000000000000 ) ) ;
#37189=EDGE_CURVE ( 'NONE', #19593, #45468, #36719, .T. ) ;
#37193=DIRECTION ( 'NONE',  ( 0.000000000000000000, 0.000000000000000000, 1.000000000000000000 ) ) ;
#37197=CARTESIAN_POINT ( 'NONE',  ( 15.00000000000000000, 5.835314593368777558, 22.81335362449846471 ) ) ;
#37199=AXIS2_PLACEMENT_3D ( 'NONE', #14790, #29952, #29707 ) ;
#37207=DIRECTION ( 'NONE',  ( 0.000000000000000000, 0.000000000000000000, 1.000000000000000000 ) ) ;
#37213=ORIENTED_EDGE ( 'NONE', *, *, #15431, .T. ) ;
#37216=ORIENTED_EDGE ( 'NONE', *, *, #13912, .F. ) ;
#37217=DIRECTION ( 'NONE',  ( 0.000000000000000000, 0.000000000000000000, -1.000000000000000000 ) ) ;
#37218=CIRCLE ( 'NONE', #27897, 31.99999999999998579 ) ;
#37220=EDGE_LOOP ( 'NONE', ( #36773, #1571, #22474, #5388 ) ) ;
#37221=CARTESIAN_POINT ( 'NONE',  ( 0.000000000000000000, -18.89407956138204980, -75.16055320797050854 ) ) ;
#37234=FACE_OUTER_BOUND ( 'NONE', #41075, .T. ) ;
#37236=CIRCLE ( 'NONE', #34901, 77.49899999999999523 ) ;
#37237=CIRCLE ( 'NONE', #35572, 77.49899999999998101 ) ;
#37238=LINE ( 'NONE', #36509, #20913 ) ;
#37240=ORIENTED_EDGE ( 'NONE', *, *, #12908, .F. ) ;
#37241=DIRECTION ( 'NONE',  ( -1.000000000000000000, -0.000000000000000000, -0.000000000000000000 ) ) ;
#37262=CARTESIAN_POINT ( 'NONE',  ( 11.99999999999999822, -81.90746397400391743, 3.894527615417590294 ) ) ;
#37266=VECTOR ( 'NONE', #26053, 1000.000000000000000 ) ;
#37267=ORIENTED_EDGE ( 'NONE', *, *, #45502, .T. ) ;
#37285=LINE ( 'NONE', #36788, #8996 ) ;
#37286=VERTEX_POINT ( 'NONE', #20790 ) ;
#37287=ADVANCED_FACE ( 'NONE', ( #38683 ), #35466, .T. ) ;
#37288=ORIENTED_EDGE ( 'NONE', *, *, #9177, .F. ) ;
#37292=CIRCLE ( 'NONE', #22458, 31.99999999999998934 ) ;
#37301=ORIENTED_EDGE ( 'NONE', *, *, #825, .T. ) ;
#37306=CARTESIAN_POINT ( 'NONE',  ( 5.999999999999999112, -68.55367621811110723, -44.99326035066126650 ) ) ;
#37307=ORIENTED_EDGE ( 'NONE', *, *, #22937, .T. ) ;
#37308=CARTESIAN_POINT ( 'NONE',  ( 11.99999999999999822, 55.38113227695858143, -54.21277698773617715 ) ) ;
#37314=DIRECTION ( 'NONE',  ( 0.000000000000000000, 0.000000000000000000, 1.000000000000000000 ) ) ;
#37317=DIRECTION ( 'NONE',  ( -1.000000000000000000, -0.000000000000000000, -0.000000000000000000 ) ) ;
#37321=DIRECTION ( 'NONE',  ( -1.000000000000000000, 0.000000000000000000, 0.000000000000000000 ) ) ;
#37336=ORIENTED_EDGE ( 'NONE', *, *, #18574, .T. ) ;
#37338=VECTOR ( 'NONE', #659, 1000.000000000000000 ) ;
#37340=FACE_OUTER_BOUND ( 'NONE', #44210, .T. ) ;
#37342=ADVANCED_FACE ( 'NONE', ( #12974 ), #42828, .T. ) ;
#37350=CIRCLE ( 'NONE', #41274, 31.99999999999999289 ) ;
#37355=CARTESIAN_POINT ( 'NONE',  ( 15.00000000000000000, 22.07842321921480888, -8.187992925817425771 ) ) ;
#37356=ORIENTED_EDGE ( 'NONE', *, *, #23542, .T. ) ;
#37362=FACE_OUTER_BOUND ( 'NONE', #439, .T. ) ;
#37363=CARTESIAN_POINT ( 'NONE',  ( 15.00000000000000000, -11.95096189432345746, -23.69967320028757030 ) ) ;
#37364=EDGE_CURVE ( 'NONE', #33288, #43680, #18664, .T. ) ;
#37372=LINE ( 'NONE', #8473, #35865 ) ;
#37374=VECTOR ( 'NONE', #10840, 1000.000000000000000 ) ;
#37375=DIRECTION ( 'NONE',  ( -1.000000000000000000, -0.000000000000000000, 0.000000000000000000 ) ) ;
#37380=LINE ( 'NONE', #36879, #17710 ) ;
#37382=EDGE_CURVE ( 'NONE', #22127, #19593, #39819, .T. ) ;
#37384=DIRECTION ( 'NONE',  ( -1.000000000000000000, -0.000000000000000000, -0.000000000000000000 ) ) ;
#37393=DIRECTION ( 'NONE',  ( 1.000000000000000000, -0.000000000000000000, 0.000000000000000000 ) ) ;
#37398=ORIENTED_EDGE ( 'NONE', *, *, #17835, .F. ) ;
#37404=DIRECTION ( 'NONE',  ( -1.000000000000000000, 0.000000000000000000, -0.000000000000000000 ) ) ;
#37407=ORIENTED_EDGE ( 'NONE', *, *, #36530, .F. ) ;
#37409=EDGE_CURVE ( 'NONE', #30376, #33522, #25706, .T. ) ;
#37423=VERTEX_POINT ( 'NONE', #3625 ) ;
#37424=EDGE_CURVE ( 'NONE', #21091, #37774, #45265, .T. ) ;
#37427=CARTESIAN_POINT ( 'NONE',  ( 11.99999999999999822, 65.58780272294076497, 36.73666225445916211 ) ) ;
#37437=LINE ( 'NONE', #48210, #1196 ) ;
#37439=CIRCLE ( 'NONE', #8496, 82.00000000000000000 ) ;
#37441=AXIS2_PLACEMENT_3D ( 'NONE', #44711, #38337, #155 ) ;
#37444=DIRECTION ( 'NONE',  ( 0.000000000000000000, -0.5877852522924779111, -0.8090169943749440096 ) ) ;
#37451=DIRECTION ( 'NONE',  ( 0.000000000000000000, 0.9510565162951504226, -0.3090169943749573322 ) ) ;
#37459=EDGE_CURVE ( 'NONE', #46408, #31210, #43546, .T. ) ;
#37466=VECTOR ( 'NONE', #41744, 1000.000000000000000 ) ;
#37467=ADVANCED_FACE ( 'NONE', ( #25162 ), #32748, .T. ) ;
#37474=EDGE_LOOP ( 'NONE', ( #14227, #5859, #16757, #19889 ) ) ;
#37475=ORIENTED_EDGE ( 'NONE', *, *, #8824, .F. ) ;
#37485=EDGE_LOOP ( 'NONE', ( #21521, #3862, #20195, #27680 ) ) ;
#37489=CARTESIAN_POINT ( 'NONE',  ( 11.99999999999999822, 0.000000000000000000, 0.000000000000000000 ) ) ;
#37492=CARTESIAN_POINT ( 'NONE',  ( 15.00000000000000000, 23.49999999999999645, -1.500000000000003997 ) ) ;
#37499=FACE_OUTER_BOUND ( 'NONE', #26467, .T. ) ;
#37501=LINE ( 'NONE', #44368, #37374 ) ;
#37502=CARTESIAN_POINT ( 'NONE',  ( 11.99999999999999822, -59.46389618801929089, -49.70050353004953081 ) ) ;
#37507=EDGE_LOOP ( 'NONE', ( #27238, #8002, #40049, #18514 ) ) ;
#37512=AXIS2_PLACEMENT_3D ( 'NONE', #32131, #9357, #35556 ) ;
#37513=ADVANCED_FACE ( 'NONE', ( #8266 ), #37642, .T. ) ;
#37514=DIRECTION ( 'NONE',  ( -1.000000000000000000, -0.000000000000000000, -0.000000000000000000 ) ) ;
#37517=DIRECTION ( 'NONE',  ( -1.000000000000000000, -0.000000000000000000, -0.000000000000000000 ) ) ;
#37519=CARTESIAN_POINT ( 'NONE',  ( 11.99999999999999822, 30.41916302227114599, 71.27951684758035356 ) ) ;
#37520=SHAPE_REPRESENTATION ( 'slow gear_ISO - Spur gear 2M 80T 20PA 12FW ---S80A75H50L38.0N', ( #11636 ), #21023 ) ;
#37521=CYLINDRICAL_SURFACE ( 'NONE', #15304, 77.49899999999999523 ) ;
#37522=EDGE_LOOP ( 'NONE', ( #23738, #3305, #34366, #5544 ) ) ;
#37530=DIRECTION ( 'NONE',  ( 0.000000000000000000, 0.000000000000000000, 1.000000000000000000 ) ) ;
#37532=VECTOR ( 'NONE', #8144, 1000.000000000000000 ) ;
#37550=DIRECTION ( 'NONE',  ( -1.000000000000000000, 0.000000000000000000, 0.000000000000000000 ) ) ;
#37553=PLANE ( 'NONE',  #9941 ) ;
#37555=CARTESIAN_POINT ( 'NONE',  ( 11.99999999999999822, 0.000000000000000000, 0.000000000000000000 ) ) ;
#37559=EDGE_CURVE ( 'NONE', #1488, #32651, #30535, .T. ) ;
#37563=CARTESIAN_POINT ( 'NONE',  ( 0.000000000000000000, 30.41916302227114599, 71.27951684758035356 ) ) ;
#37565=EDGE_CURVE ( 'NONE', #18579, #7117, #13982, .T. ) ;
#37566=CARTESIAN_POINT ( 'NONE',  ( 0.000000000000000000, -62.20884554313985149, -46.21855187248698371 ) ) ;
#37568=ORIENTED_EDGE ( 'NONE', *, *, #47183, .F. ) ;
#37573=DIRECTION ( 'NONE',  ( 0.000000000000000000, -0.2079116908177533474, 0.9781476007338069101 ) ) ;
#37576=AXIS2_PLACEMENT_3D ( 'NONE', #4197, #37965, #40916 ) ;
#37580=CARTESIAN_POINT ( 'NONE',  ( 11.99999999999999822, -73.73191006444561424, -14.66109333815538918 ) ) ;
#37583=DIRECTION ( 'NONE',  ( 0.000000000000000000, 0.000000000000000000, 1.000000000000000000 ) ) ;
#37584=ORIENTED_EDGE ( 'NONE', *, *, #17008, .T. ) ;
#37587=ORIENTED_EDGE ( 'NONE', *, *, #2535, .F. ) ;
#37593=ORIENTED_EDGE ( 'NONE', *, *, #16344, .F. ) ;
#37594=ORIENTED_EDGE ( 'NONE', *, *, #14608, .T. ) ;
#37597=CARTESIAN_POINT ( 'NONE',  ( 12.00000000000000000, -18.13022148937263012, -15.02647892043543898 ) ) ;
#37598=FACE_OUTER_BOUND ( 'NONE', #45580, .T. ) ;
#37599=CYLINDRICAL_SURFACE ( 'NONE', #43237, 82.00000000000000000 ) ;
#37600=DIRECTION ( 'NONE',  ( -1.000000000000000000, 0.000000000000000000, 0.000000000000000000 ) ) ;
#37601=CARTESIAN_POINT ( 'NONE',  ( 11.99999999999999822, 73.95703589263975175, 23.16143007188452785 ) ) ;
#37604=DIRECTION ( 'NONE',  ( 0.000000000000000000, -0.000000000000000000, 1.000000000000000000 ) ) ;
#37608=DIRECTION ( 'NONE',  ( 1.000000000000000000, -0.000000000000000000, 0.000000000000000000 ) ) ;
#37609=EDGE_LOOP ( 'NONE', ( #19543, #41988, #30835, #41044, #36091, #47915, #18611, #37059, #24672, #46277, #12000, #15078, #6052, #10807, #35884, #17331, #26456, #2032, #41978, #10565, #37709, #7882, #41997, #4231, #34319, #15446, #26222, #16295, #33730, #40313, #41920, #24382, #9360, #37148, #9138, #34067, #2544, #38247, #38744, #6621, #11216, #8844, #24616, #42047, #36435, #732, #19261, #2091, #11369, #41913, #8286, #6995, #37307, #23993, #30882, #8347, #11466, #10731, #6396, #23731, #39102, #21128, #42219, #1810, #36987, #25153, #38545, #10327, #31911, #39504, #17952, #28391, #28781, #10884, #38138, #31012, #9366, #22260, #34683, #42718, #23958, #9633, #32065, #12313, #26206, #41948, #35597, #26360, #21196, #40633, #46860, #27558, #34377, #30617, #22804, #9975, #2138, #32164, #8208, #5484, #3636, #1243, #621, #24601, #23484, #46375, #17944, #17901, #9284, #13866, #11411, #21396, #36919, #30370, #25857, #36510, #47511, #8162, #16982, #22632, #16346, #34161, #27482, #33324, #13737, #4332, #27342, #8549, #36690, #1490, #6295, #20962, #33720, #5873, #9521, #19852, #30706, #39106, #26374, #7655, #9942, #26853, #47287, #8809, #17396, #35227, #11294, #32027, #41580, #13234, #47681, #7962, #11264, #34668, #42759, #25727, #43767, #36181, #8152, #8202, #15002, #28018, #16892, #25642, #35894, #24214, #44006, #9479, #40560, #19293, #38786, #40113, #10135, #23102, #11764, #39694, #25238, #312, #17088, #9877, #6722, #19792, #38317, #5823, #1185, #37880, #32817, #19176, #40784, #31351, #31228, #9595, #39995, #11226, #8778, #38678, #22451, #24119, #9530, #17047, #41924, #1100, #27141, #26697, #4656, #20761, #27794, #39210, #46020, #29429, #25252, #10973, #14913, #33521, #19771, #36670, #16561, #46735, #19220, #32550, #35133, #14631, #4934, #9358, #12427, #34601, #25005, #16398, #43884, #44993, #46766, #10401, #31048, #27200, #44680, #13035, #22769, #6012, #31916, #6086, #12654, #28767, #36847, #22765, #16125, #44760, #10307, #438, #30143, #24947, #23660, #22160, #6409, #35899, #42108, #20133, #41621, #16407, #20844, #12551, #20427, #24403, #44284, #19404, #22903, #30122, #3884, #26142, #15182, #38985, #46130, #32563, #28258, #24974, #3086, #24448, #23717, #23503, #1515, #46218, #9973, #7043, #9041, #20647, #39033, #8682, #33926, #44374, #28556, #34015, #32402, #14721, #5840, #42585, #10864, #17322, #25656, #16846, #47852, #30084, #44819, #22576, #42943, #853, #22121, #503, #48399, #31103, #39826, #3124, #47139, #29363, #14297, #33540, #11378, #17648, #2399, #12413, #42418, #11650, #30530, #40270, #17211, #26524, #21028 ) ) ;
#37621=VERTEX_POINT ( 'NONE', #4592 ) ;
#37623=CARTESIAN_POINT ( 'NONE',  ( 12.00000000000000000, -19.89357724624986901, 12.59942793731086219 ) ) ;
#37636=CARTESIAN_POINT ( 'NONE',  ( 0.000000000000000000, -10.30890764327323161, -81.34940948281348483 ) ) ;
#37642=CYLINDRICAL_SURFACE ( 'NONE', #13230, 77.49899999999999523 ) ;
#37643=ORIENTED_EDGE ( 'NONE', *, *, #16917, .F. ) ;
#37644=CIRCLE ( 'NONE', #16551, 31.99999999999998934 ) ;
#37646=EDGE_CURVE ( 'NONE', #45561, #20366, #8531, .T. ) ;
#37647=DIRECTION ( 'NONE',  ( 0.000000000000000000, 0.2079116908177664758, 0.9781476007338042455 ) ) ;
#37652=VERTEX_POINT ( 'NONE', #38861 ) ;
#37653=CARTESIAN_POINT ( 'NONE',  ( 11.99999999999999822, -63.97538442413390669, -51.29473840253292138 ) ) ;
#37657=EDGE_LOOP ( 'NONE', ( #48054, #16271, #22297, #35591 ) ) ;
#37658=ORIENTED_EDGE ( 'NONE', *, *, #45786, .F. ) ;
#37663=CARTESIAN_POINT ( 'NONE',  ( 15.00000000000000000, 8.688484142253932063, -21.88630264137371029 ) ) ;
#37667=DIRECTION ( 'NONE',  ( 0.000000000000000000, 0.000000000000000000, 1.000000000000000000 ) ) ;
#37668=LINE ( 'NONE', #7324, #1890 ) ;
#37675=CARTESIAN_POINT ( 'NONE',  ( 11.99999999999999822, 0.000000000000000000, 0.000000000000000000 ) ) ;
#37676=AXIS2_PLACEMENT_3D ( 'NONE', #7614, #10, #41393 ) ;
#37679=CARTESIAN_POINT ( 'NONE',  ( 11.99999999999999822, -68.67312586195022561, 35.91791733033451806 ) ) ;
#37680=( NAMED_UNIT ( * ) SI_UNIT ( $, .STERADIAN. ) SOLID_ANGLE_UNIT ( ) );
#37682=EDGE_CURVE ( 'NONE', #33388, #15777, #3823, .T. ) ;
#37684=VERTEX_POINT ( 'NONE', #35406 ) ;
#37685=EDGE_CURVE ( 'NONE', #15671, #31890, #31041, .T. ) ;
#37687=VECTOR ( 'NONE', #38141, 1000.000000000000000 ) ;
#37689=CYLINDRICAL_SURFACE ( 'NONE', #15166, 82.00000000000000000 ) ;
#37691=ADVANCED_FACE ( 'NONE', ( #31523 ), #5325, .T. ) ;
#37695=ORIENTED_EDGE ( 'NONE', *, *, #41138, .T. ) ;
#37697=VERTEX_POINT ( 'NONE', #19996 ) ;
#37700=CIRCLE ( 'NONE', #46309, 82.00000000000000000 ) ;
#37701=FACE_OUTER_BOUND ( 'NONE', #30492, .T. ) ;
#37704=DIRECTION ( 'NONE',  ( -1.000000000000000000, -0.000000000000000000, 0.000000000000000000 ) ) ;
#37707=FACE_OUTER_BOUND ( 'NONE', #26736, .T. ) ;
#37709=ORIENTED_EDGE ( 'NONE', *, *, #19387, .T. ) ;
#37720=VERTEX_POINT ( 'NONE', #28075 ) ;
#37722=DIRECTION ( 'NONE',  ( 0.000000000000000000, 0.5877852522924708056, -0.8090169943749491166 ) ) ;
#37724=ORIENTED_EDGE ( 'NONE', *, *, #35828, .T. ) ;
#37726=CARTESIAN_POINT ( 'NONE',  ( 11.99999999999999822, 0.000000000000000000, 0.000000000000000000 ) ) ;
#37728=CARTESIAN_POINT ( 'NONE',  ( 11.99999999999999822, 31.47745569255237896, -68.26794271651228030 ) ) ;
#37731=LINE ( 'NONE', #3475, #11433 ) ;
#37736=ADVANCED_FACE ( 'NONE', ( #31276 ), #24159, .T. ) ;
#37737=CIRCLE ( 'NONE', #38508, 31.99999999999998579 ) ;
#37741=DIRECTION ( 'NONE',  ( -1.000000000000000000, 0.000000000000000000, 0.000000000000000000 ) ) ;
#37742=CIRCLE ( 'NONE', #21301, 77.49899999999999523 ) ;
#37745=AXIS2_PLACEMENT_3D ( 'NONE', #33753, #45033, #48212 ) ;
#37750=EDGE_CURVE ( 'NONE', #47807, #3020, #43243, .T. ) ;
#37757=AXIS2_PLACEMENT_3D ( 'NONE', #27029, #34838, #1059 ) ;
#37762=DIRECTION ( 'NONE',  ( -1.000000000000000000, 0.000000000000000000, 0.000000000000000000 ) ) ;
#37763=FACE_OUTER_BOUND ( 'NONE', #16320, .T. ) ;
#37773=LINE ( 'NONE', #15278, #13270 ) ;
#37774=VERTEX_POINT ( 'NONE', #18245 ) ;
#37777=VERTEX_POINT ( 'NONE', #10683 ) ;
#37782=CARTESIAN_POINT ( 'NONE',  ( 0.000000000000000000, -68.27212725128298132, 31.46837873494953541 ) ) ;
#37785=VERTEX_POINT ( 'NONE', #47857 ) ;
#37786=CYLINDRICAL_SURFACE ( 'NONE', #7302, 31.99999999999998579 ) ;
#37788=DIRECTION ( 'NONE',  ( 0.000000000000000000, 0.000000000000000000, 1.000000000000000000 ) ) ;
#37797=EDGE_CURVE ( 'NONE', #6843, #35390, #17767, .T. ) ;
#37799=DIRECTION ( 'NONE',  ( -0.000000000000000000, -0.9135454576426058626, -0.4067366430757889395 ) ) ;
#37801=ADVANCED_FACE ( 'NONE', ( #21687 ), #14346, .T. ) ;
#37802=CIRCLE ( 'NONE', #41718, 31.99999999999999645 ) ;
#37803=DIRECTION ( 'NONE',  ( 0.000000000000000000, 0.000000000000000000, 1.000000000000000000 ) ) ;
#37806=DIRECTION ( 'NONE',  ( 0.000000000000000000, 0.000000000000000000, 1.000000000000000000 ) ) ;
#37809=ADVANCED_FACE ( 'NONE', ( #2352 ), #47151, .T. ) ;
#37813=EDGE_LOOP ( 'NONE', ( #42697, #24001, #39930, #3794 ) ) ;
#37824=CARTESIAN_POINT ( 'NONE',  ( 11.99999999999999822, 0.000000000000000000, 0.000000000000000000 ) ) ;
#37825=ORIENTED_EDGE ( 'NONE', *, *, #25161, .F. ) ;
#37829=VECTOR ( 'NONE', #33123, 1000.000000000000227 ) ;
#37833=CARTESIAN_POINT ( 'NONE',  ( 11.99999999999999822, 77.16300072079698680, -27.74655509720590629 ) ) ;
#37839=CARTESIAN_POINT ( 'NONE',  ( 11.99999999999999822, -0.8261519478425843888, -77.49459641780887864 ) ) ;
#37841=DIRECTION ( 'NONE',  ( -1.000000000000000000, 0.000000000000000000, -0.000000000000000000 ) ) ;
#37843=DIRECTION ( 'NONE',  ( 0.000000000000000000, 0.07845909572784512398, -0.9969173337331279638 ) ) ;
#37844=DIRECTION ( 'NONE',  ( -1.000000000000000000, 0.000000000000000000, 0.000000000000000000 ) ) ;
#37846=CARTESIAN_POINT ( 'NONE',  ( 0.000000000000000000, 0.000000000000000000, 0.000000000000000000 ) ) ;
#37848=DIRECTION ( 'NONE',  ( 0.000000000000000000, -0.5224985647159561264, 0.8526401643540878483 ) ) ;
#37852=ORIENTED_EDGE ( 'NONE', *, *, #45687, .T. ) ;
#37863=DIRECTION ( 'NONE',  ( -1.000000000000000000, -0.000000000000000000, -0.000000000000000000 ) ) ;
#37866=CIRCLE ( 'NONE', #1091, 77.49900000000000944 ) ;
#37873=EDGE_CURVE ( 'NONE', #36027, #41278, #21191, .T. ) ;
#37874=LINE ( 'NONE', #1634, #18137 ) ;
#37878=VERTEX_POINT ( 'NONE', #35888 ) ;
#37879=ORIENTED_EDGE ( 'NONE', *, *, #15213, .F. ) ;
#37880=ORIENTED_EDGE ( 'NONE', *, *, #21006, .T. ) ;
#37884=VECTOR ( 'NONE', #41642, 1000.000000000000000 ) ;
#37886=AXIS2_PLACEMENT_3D ( 'NONE', #36843, #6992, #25824 ) ;
#37888=VERTEX_POINT ( 'NONE', #32233 ) ;
#37896=VECTOR ( 'NONE', #17509, 1000.000000000000000 ) ;
#37897=ORIENTED_EDGE ( 'NONE', *, *, #26072, .T. ) ;
#37906=DIRECTION ( 'NONE',  ( 0.000000000000000000, 0.000000000000000000, -1.000000000000000000 ) ) ;
#37907=EDGE_CURVE ( 'NONE', #30527, #42392, #42187, .T. ) ;
#37916=CARTESIAN_POINT ( 'NONE',  ( 0.000000000000000000, 0.000000000000000000, 0.000000000000000000 ) ) ;
#37919=CARTESIAN_POINT ( 'NONE',  ( 11.99999999999999822, 18.89407956138362010, -75.16055320797013906 ) ) ;
#37920=CARTESIAN_POINT ( 'NONE',  ( 6.000000000000000000, -3.894527615417333610, -81.90746397400393164 ) ) ;
#37924=CARTESIAN_POINT ( 'NONE',  ( 0.000000000000000000, -11.30684508768284680, -76.66974797899850103 ) ) ;
#37926=DIRECTION ( 'NONE',  ( 0.000000000000000000, 0.000000000000000000, 1.000000000000000000 ) ) ;
#37929=CARTESIAN_POINT ( 'NONE',  ( 5.999999999999999112, -79.10210256391353312, -21.60688246758669351 ) ) ;
#37930=FACE_OUTER_BOUND ( 'NONE', #15574, .T. ) ;
#37937=DIRECTION ( 'NONE',  ( 0.000000000000000000, 0.8660254037844370423, -0.5000000000000029976 ) ) ;
#37939=DIRECTION ( 'NONE',  ( -1.000000000000000000, 0.000000000000000000, 0.000000000000000000 ) ) ;
#37940=CYLINDRICAL_SURFACE ( 'NONE', #35487, 77.49899999999999523 ) ;
#37944=CIRCLE ( 'NONE', #44196, 31.99999999999998224 ) ;
#37950=CIRCLE ( 'NONE', #23108, 31.99999999999998579 ) ;
#37952=EDGE_CURVE ( 'NONE', #26872, #27749, #48351, .T. ) ;
#37953=VERTEX_POINT ( 'NONE', #26081 ) ;
#37958=DIRECTION ( 'NONE',  ( -1.000000000000000000, -0.000000000000000000, -0.000000000000000000 ) ) ;
#37962=DIRECTION ( 'NONE',  ( -1.000000000000000000, 0.000000000000000000, 0.000000000000000000 ) ) ;
#37965=DIRECTION ( 'NONE',  ( -1.000000000000000000, 0.000000000000000000, -0.000000000000000000 ) ) ;
#37966=VECTOR ( 'NONE', #25168, 1000.000000000000000 ) ;
#37970=ORIENTED_EDGE ( 'NONE', *, *, #30528, .T. ) ;
#37980=ADVANCED_FACE ( 'NONE', ( #37340 ), #22886, .T. ) ;
#37981=CARTESIAN_POINT ( 'NONE',  ( 0.000000000000000000, 81.90746397400393164, -3.894527615416979671 ) ) ;
#37982=EDGE_CURVE ( 'NONE', #5793, #29949, #15548, .T. ) ;
#37987=CARTESIAN_POINT ( 'NONE',  ( 0.000000000000000000, -74.65374052328654386, 8.840884882374837161 ) ) ;
#37988=CARTESIAN_POINT ( 'NONE',  ( 15.00000000000000000, 9.615535125379096826, 24.73947219025905042 ) ) ;
#37989=ORIENTED_EDGE ( 'NONE', *, *, #31764, .F. ) ;
#37992=CYLINDRICAL_SURFACE ( 'NONE', #7643, 77.49899999999999523 ) ;
#37995=ORIENTED_EDGE ( 'NONE', *, *, #1397, .F. ) ;
#37998=EDGE_LOOP ( 'NONE', ( #34597, #3615, #26955, #5171 ) ) ;
#38000=DIRECTION ( 'NONE',  ( 0.000000000000000000, 0.000000000000000000, 1.000000000000000000 ) ) ;
#38002=LINE ( 'NONE', #10848, #3345 ) ;
#38010=AXIS2_PLACEMENT_3D ( 'NONE', #41965, #8644, #1322 ) ;
#38011=ORIENTED_EDGE ( 'NONE', *, *, #46643, .F. ) ;
#38021=EDGE_CURVE ( 'NONE', #16137, #14267, #1524, .T. ) ;
#38023=DIRECTION ( 'NONE',  ( 0.000000000000000000, 0.000000000000000000, -1.000000000000000000 ) ) ;
#38024=FACE_OUTER_BOUND ( 'NONE', #13678, .T. ) ;
#38025=AXIS2_PLACEMENT_3D ( 'NONE', #29114, #18593, #47253 ) ;
#38026=EDGE_CURVE ( 'NONE', #46446, #5128, #33657, .T. ) ;
#38028=VERTEX_POINT ( 'NONE', #41265 ) ;
#38030=DIRECTION ( 'NONE',  ( 0.000000000000000000, -0.6691306063588654540, -0.7431448254773878048 ) ) ;
#38032=EDGE_LOOP ( 'NONE', ( #13085, #29573, #31145, #14597 ) ) ;
#38034=DIRECTION ( 'NONE',  ( 1.000000000000000000, 0.000000000000000000, 0.000000000000000000 ) ) ;
#38039=DIRECTION ( 'NONE',  ( -1.000000000000000000, -0.000000000000000000, -0.000000000000000000 ) ) ;
#38040=CARTESIAN_POINT ( 'NONE',  ( 11.99999999999999822, 71.27951684758026829, 30.41916302227139113 ) ) ;
#38042=CARTESIAN_POINT ( 'NONE',  ( 11.99999999999999822, 0.000000000000000000, 0.000000000000000000 ) ) ;
#38044=AXIS2_PLACEMENT_3D ( 'NONE', #26820, #23148, #38087 ) ;
#38047=DIRECTION ( 'NONE',  ( 0.000000000000000000, 0.000000000000000000, -1.000000000000000000 ) ) ;
#38050=DIRECTION ( 'NONE',  ( 0.000000000000000000, 0.000000000000000000, 1.000000000000000000 ) ) ;
#38061=ORIENTED_EDGE ( 'NONE', *, *, #9291, .F. ) ;
#38067=VERTEX_POINT ( 'NONE', #39267 ) ;
#38073=DIRECTION ( 'NONE',  ( -1.000000000000000000, -0.000000000000000000, 0.000000000000000000 ) ) ;
#38079=CARTESIAN_POINT ( 'NONE',  ( 15.00000000000000000, -25.60904388321925040, -6.976881207771165272 ) ) ;
#38081=EDGE_CURVE ( 'NONE', #12813, #1582, #27534, .T. ) ;
#38087=DIRECTION ( 'NONE',  ( 0.000000000000000000, 0.000000000000000000, -1.000000000000000000 ) ) ;
#38090=DIRECTION ( 'NONE',  ( -1.000000000000000000, 0.000000000000000000, 0.000000000000000000 ) ) ;
#38092=DIRECTION ( 'NONE',  ( 0.000000000000000000, 0.000000000000000000, 1.000000000000000000 ) ) ;
#38099=ORIENTED_EDGE ( 'NONE', *, *, #1873, .F. ) ;
#38101=DIRECTION ( 'NONE',  ( -1.000000000000000000, -0.000000000000000000, 0.000000000000000000 ) ) ;
#38114=DIRECTION ( 'NONE',  ( 0.000000000000000000, -6.938893903907231533E-15, 1.000000000000000000 ) ) ;
#38115=AXIS2_PLACEMENT_3D ( 'NONE', #25389, #40345, #26122 ) ;
#38118=ORIENTED_EDGE ( 'NONE', *, *, #27479, .T. ) ;
#38119=CIRCLE ( 'NONE', #28725, 31.99999999999998934 ) ;
#38124=ORIENTED_EDGE ( 'NONE', *, *, #35464, .T. ) ;
#38127=EDGE_CURVE ( 'NONE', #25362, #15864, #24220, .T. ) ;
#38128=DIRECTION ( 'NONE',  ( 0.000000000000000000, 0.000000000000000000, 1.000000000000000000 ) ) ;
#38129=VERTEX_POINT ( 'NONE', #20667 ) ;
#38138=ORIENTED_EDGE ( 'NONE', *, *, #41012, .T. ) ;
#38141=DIRECTION ( 'NONE',  ( -1.000000000000000000, 0.000000000000000000, 0.000000000000000000 ) ) ;
#38142=CYLINDRICAL_SURFACE ( 'NONE', #31164, 82.00000000000000000 ) ;
#38148=AXIS2_PLACEMENT_3D ( 'NONE', #28566, #29524, #36137 ) ;
#38153=EDGE_LOOP ( 'NONE', ( #47689, #20875, #48415, #11758 ) ) ;
#38159=LINE ( 'NONE', #42807, #17519 ) ;
#38162=LINE ( 'NONE', #8300, #14054 ) ;
#38168=CARTESIAN_POINT ( 'NONE',  ( 0.000000000000000000, -76.41127070299280888, 12.93880638057290788 ) ) ;
#38173=EDGE_LOOP ( 'NONE', ( #20877, #16574, #14931, #20754 ) ) ;
#38177=EDGE_CURVE ( 'NONE', #15200, #10250, #1831, .T. ) ;
#38185=DIRECTION ( 'NONE',  ( 0.000000000000000000, 0.9135454576426005335, -0.4067366430758010409 ) ) ;
#38189=EDGE_CURVE ( 'NONE', #16881, #21229, #32064, .T. ) ;
#38190=EDGE_CURVE ( 'NONE', #44007, #9506, #6277, .T. ) ;
#38191=ADVANCED_FACE ( 'NONE', ( #10131 ), #21635, .T. ) ;
#38196=EDGE_LOOP ( 'NONE', ( #11983, #20274, #7831, #23592 ) ) ;
#38199=LINE ( 'NONE', #12265, #22289 ) ;
#38202=DIRECTION ( 'NONE',  ( -1.000000000000000000, 0.000000000000000000, 0.000000000000000000 ) ) ;
#38204=ADVANCED_FACE ( 'NONE', ( #13563 ), #36320, .T. ) ;
#38210=AXIS2_PLACEMENT_3D ( 'NONE', #20531, #31334, #27651 ) ;
#38213=DIRECTION ( 'NONE',  ( 0.000000000000000000, -0.4539904997395542430, 0.8910065241883641241 ) ) ;
#38215=AXIS2_PLACEMENT_3D ( 'NONE', #46740, #20048, #8784 ) ;
#38216=CARTESIAN_POINT ( 'NONE',  ( 5.999999999999999112, 79.10210256391368944, 21.60688246758614994 ) ) ;
#38217=LINE ( 'NONE', #35016, #4008 ) ;
#38223=CARTESIAN_POINT ( 'NONE',  ( 11.99999999999999822, -36.72794159290197769, -65.59268652807249111 ) ) ;
#38225=DIRECTION ( 'NONE',  ( 0.000000000000000000, 0.000000000000000000, -1.000000000000000000 ) ) ;
#38226=CARTESIAN_POINT ( 'NONE',  ( 0.000000000000000000, -80.28980883073769803, 16.65972982744905551 ) ) ;
#38229=DIRECTION ( 'NONE',  ( 1.000000000000000000, 0.000000000000000000, 0.000000000000000000 ) ) ;
#38230=CARTESIAN_POINT ( 'NONE',  ( 11.99999999999999822, 0.000000000000000000, 0.000000000000000000 ) ) ;
#38236=FACE_BOUND ( 'NONE', #2242, .T. ) ;
#38241=LINE ( 'NONE', #1284, #5765 ) ;
#38244=VECTOR ( 'NONE', #10003, 1000.000000000000000 ) ;
#38245=DIRECTION ( 'NONE',  ( 0.000000000000000000, 0.000000000000000000, 1.000000000000000000 ) ) ;
#38247=ORIENTED_EDGE ( 'NONE', *, *, #21857, .T. ) ;
#38255=ORIENTED_EDGE ( 'NONE', *, *, #38026, .T. ) ;
#38259=ADVANCED_FACE ( 'NONE', ( #25049 ), #47095, .F. ) ;
#38262=VERTEX_POINT ( 'NONE', #43184 ) ;
#38263=FACE_OUTER_BOUND ( 'NONE', #38173, .T. ) ;
#38264=ORIENTED_EDGE ( 'NONE', *, *, #39876, .T. ) ;
#38265=ORIENTED_EDGE ( 'NONE', *, *, #38026, .F. ) ;
#38270=ORIENTED_EDGE ( 'NONE', *, *, #2297, .F. ) ;
#38272=PLANE ( 'NONE',  #32309 ) ;
#38274=DIRECTION ( 'NONE',  ( 0.000000000000000000, -0.3090169943749549453, 0.9510565162951511997 ) ) ;
#38276=CIRCLE ( 'NONE', #7766, 82.00000000000000000 ) ;
#38283=CARTESIAN_POINT ( 'NONE',  ( -10.00000000000000000, 0.000000000000000000, 0.000000000000000000 ) ) ;
#38284=ORIENTED_EDGE ( 'NONE', *, *, #8008, .F. ) ;
#38290=VERTEX_POINT ( 'NONE', #25534 ) ;
#38291=EDGE_CURVE ( 'NONE', #36740, #25081, #21135, .T. ) ;
#38297=VERTEX_POINT ( 'NONE', #40484 ) ;
#38298=VERTEX_POINT ( 'NONE', #6943 ) ;
#38299=ORIENTED_EDGE ( 'NONE', *, *, #35768, .T. ) ;
#38307=AXIS2_PLACEMENT_3D ( 'NONE', #30365, #41377, #34017 ) ;
#38309=LINE ( 'NONE', #19446, #9395 ) ;
#38310=EDGE_LOOP ( 'NONE', ( #7919, #26657, #33927, #2341 ) ) ;
#38317=ORIENTED_EDGE ( 'NONE', *, *, #44532, .T. ) ;
#38319=VERTEX_POINT ( 'NONE', #32179 ) ;
#38324=LINE ( 'NONE', #42234, #18590 ) ;
#38325=DIRECTION ( 'NONE',  ( 0.000000000000000000, -0.9781476007338041345, 0.2079116908177664480 ) ) ;
#38326=DIRECTION ( 'NONE',  ( -1.000000000000000000, 0.000000000000000000, 0.000000000000000000 ) ) ;
#38334=DIRECTION ( 'NONE',  ( -1.000000000000000000, -0.000000000000000000, -0.000000000000000000 ) ) ;
#38337=DIRECTION ( 'NONE',  ( -1.000000000000000000, -0.000000000000000000, 0.000000000000000000 ) ) ;
#38338=FACE_OUTER_BOUND ( 'NONE', #16655, .T. ) ;
#38343=EDGE_LOOP ( 'NONE', ( #8013, #23329, #42761, #7722 ) ) ;
#38347=ORIENTED_EDGE ( 'NONE', *, *, #1158, .F. ) ;
#38356=ORIENTED_EDGE ( 'NONE', *, *, #26139, .T. ) ;
#38357=CIRCLE ( 'NONE', #5508, 31.99999999999999289 ) ;
#38361=ORIENTED_EDGE ( 'NONE', *, *, #14608, .F. ) ;
#38362=CARTESIAN_POINT ( 'NONE',  ( 12.00000000000000000, -3.948201729842355068, -23.21447184625292692 ) ) ;
#38365=CARTESIAN_POINT ( 'NONE',  ( 11.99999999999999822, 0.000000000000000000, 0.000000000000000000 ) ) ;
#38370=LINE ( 'NONE', #15141, #25854 ) ;
#38371=ORIENTED_EDGE ( 'NONE', *, *, #32920, .F. ) ;
#38372=CIRCLE ( 'NONE', #29775, 31.99999999999998579 ) ;
#38373=ADVANCED_FACE ( 'NONE', ( #37763 ), #26514, .T. ) ;
#38375=CIRCLE ( 'NONE', #9439, 31.99999999999998579 ) ;
#38376=ORIENTED_EDGE ( 'NONE', *, *, #21316, .F. ) ;
#38381=AXIS2_PLACEMENT_3D ( 'NONE', #40590, #37165, #19283 ) ;
#38382=DIRECTION ( 'NONE',  ( 0.000000000000000000, 0.3090169943749480619, -0.9510565162951533091 ) ) ;
#38384=DIRECTION ( 'NONE',  ( -1.000000000000000000, 0.000000000000000000, 0.000000000000000000 ) ) ;
#38391=DIRECTION ( 'NONE',  ( -1.000000000000000000, 0.000000000000000000, 0.000000000000000000 ) ) ;
#38392=DIRECTION ( 'NONE',  ( -1.000000000000000000, -0.000000000000000000, 0.000000000000000000 ) ) ;
#38393=ORIENTED_EDGE ( 'NONE', *, *, #6737, .F. ) ;
#38397=CARTESIAN_POINT ( 'NONE',  ( 5.999999999999999112, -59.75363087400114637, 56.15606465354937171 ) ) ;
#38398=CARTESIAN_POINT ( 'NONE',  ( 15.00000000000000000, 0.000000000000000000, 0.000000000000000000 ) ) ;
#38400=DIRECTION ( 'NONE',  ( 1.000000000000000000, 0.000000000000000000, 0.000000000000000000 ) ) ;
#38401=CARTESIAN_POINT ( 'NONE',  ( 11.99999999999999822, 0.000000000000000000, 0.000000000000000000 ) ) ;
#38404=DIRECTION ( 'NONE',  ( -1.000000000000000000, -0.000000000000000000, -0.000000000000000000 ) ) ;
#38408=( NAMED_UNIT ( * ) PLANE_ANGLE_UNIT ( ) SI_UNIT ( $, .RADIAN. ) );
#38410=CIRCLE ( 'NONE', #29001, 77.49900000000000944 ) ;
#38412=CARTESIAN_POINT ( 'NONE',  ( 0.000000000000000000, -68.26794271651286294, 31.47745569255117104 ) ) ;
#38421=ORIENTED_EDGE ( 'NONE', *, *, #36125, .F. ) ;
#38426=EDGE_LOOP ( 'NONE', ( #42358, #16787, #16427, #13409 ) ) ;
#38427=ORIENTED_EDGE ( 'NONE', *, *, #38795, .T. ) ;
#38431=ORIENTED_EDGE ( 'NONE', *, *, #5257, .F. ) ;
#38433=VERTEX_POINT ( 'NONE', #37519 ) ;
#38434=CARTESIAN_POINT ( 'NONE',  ( 11.99999999999999822, -18.89407956138204980, -75.16055320797050854 ) ) ;
#38438=DIRECTION ( 'NONE',  ( -1.000000000000000000, 0.000000000000000000, 0.000000000000000000 ) ) ;
#38441=EDGE_CURVE ( 'NONE', #21097, #22223, #7898, .T. ) ;
#38443=ORIENTED_EDGE ( 'NONE', *, *, #27750, .T. ) ;
#38444=AXIS2_PLACEMENT_3D ( 'NONE', #24062, #5224, #24287 ) ;
#38467=CARTESIAN_POINT ( 'NONE',  ( 0.000000000000000000, -74.18225833017864090, -34.94270380257717790 ) ) ;
#38471=ORIENTED_EDGE ( 'NONE', *, *, #42563, .T. ) ;
#38472=EDGE_CURVE ( 'NONE', #46674, #32773, #40708, .T. ) ;
#38473=DIRECTION ( 'NONE',  ( 0.000000000000000000, -0.8910065241883626808, -0.4539904997395569075 ) ) ;
#38476=AXIS2_PLACEMENT_3D ( 'NONE', #17306, #2380, #5115 ) ;
#38478=EDGE_CURVE ( 'NONE', #26342, #19231, #35992, .T. ) ;
#38486=CARTESIAN_POINT ( 'NONE',  ( 0.000000000000000000, 59.03961581697399907, 46.53671651293969802 ) ) ;
#38488=CARTESIAN_POINT ( 'NONE',  ( -10.00000000000000000, 0.000000000000000000, 0.000000000000000000 ) ) ;
#38493=AXIS2_PLACEMENT_3D ( 'NONE', #44431, #18486, #10671 ) ;
#38494=ORIENTED_EDGE ( 'NONE', *, *, #21612, .F. ) ;
#38497=FACE_OUTER_BOUND ( 'NONE', #47815, .T. ) ;
#38508=AXIS2_PLACEMENT_3D ( 'NONE', #5401, #46527, #13000 ) ;
#38511=DIRECTION ( 'NONE',  ( 0.000000000000000000, 0.000000000000000000, 1.000000000000000000 ) ) ;
#38513=ORIENTED_EDGE ( 'NONE', *, *, #11694, .F. ) ;
#38518=CARTESIAN_POINT ( 'NONE',  ( 11.99999999999999822, -77.32052557432845674, 5.256550761632577284 ) ) ;
#38519=AXIS2_PLACEMENT_3D ( 'NONE', #47545, #28942, #10343 ) ;
#38524=CARTESIAN_POINT ( 'NONE',  ( 0.000000000000000000, 26.02418014898310261, 70.52718814184268581 ) ) ;
#38531=VECTOR ( 'NONE', #21230, 1000.000000000000000 ) ;
#38537=EDGE_LOOP ( 'NONE', ( #43739, #4447, #10551, #19638 ) ) ;
#38544=ORIENTED_EDGE ( 'NONE', *, *, #15588, .T. ) ;
#38545=ORIENTED_EDGE ( 'NONE', *, *, #40237, .T. ) ;
#38546=EDGE_LOOP ( 'NONE', ( #16988, #33824, #21964, #25181 ) ) ;
#38548=VERTEX_POINT ( 'NONE', #9114 ) ;
#38549=AXIS2_PLACEMENT_3D ( 'NONE', #4222, #19136, #3975 ) ;
#38556=DIRECTION ( 'NONE',  ( -1.000000000000000000, 0.000000000000000000, 0.000000000000000000 ) ) ;
#38560=VERTEX_POINT ( 'NONE', #42894 ) ;
#38562=CYLINDRICAL_SURFACE ( 'NONE', #27837, 31.99999999999998579 ) ;
#38563=FACE_OUTER_BOUND ( 'NONE', #9700, .T. ) ;
#38565=ORIENTED_EDGE ( 'NONE', *, *, #25801, .T. ) ;
#38567=CARTESIAN_POINT ( 'NONE',  ( 11.99999999999999822, 0.000000000000000000, 0.000000000000000000 ) ) ;
#38569=DIRECTION ( 'NONE',  ( 0.000000000000000000, 0.000000000000000000, -1.000000000000000000 ) ) ;
#38573=PLANE ( 'NONE',  #18160 ) ;
#38575=FACE_OUTER_BOUND ( 'NONE', #3034, .T. ) ;
#38577=EDGE_CURVE ( 'NONE', #25331, #11148, #25048, .T. ) ;
#38579=DIRECTION ( 'NONE',  ( -1.000000000000000000, -0.000000000000000000, -0.000000000000000000 ) ) ;
#38586=ORIENTED_EDGE ( 'NONE', *, *, #14475, .F. ) ;
#38587=CARTESIAN_POINT ( 'NONE',  ( 0.000000000000000000, 77.16300072079698680, -27.74655509720590985 ) ) ;
#38592=EDGE_CURVE ( 'NONE', #38028, #13081, #24279, .T. ) ;
#38596=CARTESIAN_POINT ( 'NONE',  ( 11.99999999999999822, 0.000000000000000000, 0.000000000000000000 ) ) ;
#38599=AXIS2_PLACEMENT_3D ( 'NONE', #30497, #4556, #37843 ) ;
#38604=ORIENTED_EDGE ( 'NONE', *, *, #48145, .F. ) ;
#38606=ORIENTED_EDGE ( 'NONE', *, *, #10431, .F. ) ;
#38607=CIRCLE ( 'NONE', #18241, 31.99999999999998579 ) ;
#38615=VERTEX_POINT ( 'NONE', #4955 ) ;
#38622=AXIS2_PLACEMENT_3D ( 'NONE', #47660, #44485, #11201 ) ;
#38632=EDGE_CURVE ( 'NONE', #36250, #17899, #8862, .T. ) ;
#38633=CARTESIAN_POINT ( 'NONE',  ( 0.000000000000000000, 73.72996012237440766, 14.67089635893739619 ) ) ;
#38637=VECTOR ( 'NONE', #5537, 1000.000000000000000 ) ;
#38639=EDGE_CURVE ( 'NONE', #25598, #24721, #29144, .T. ) ;
#38646=ORIENTED_EDGE ( 'NONE', *, *, #44815, .T. ) ;
#38654=DIRECTION ( 'NONE',  ( -1.000000000000000000, -0.000000000000000000, 0.000000000000000000 ) ) ;
#38655=ORIENTED_EDGE ( 'NONE', *, *, #24101, .F. ) ;
#38656=AXIS2_PLACEMENT_3D ( 'NONE', #22700, #8263, #26140 ) ;
#38658=CARTESIAN_POINT ( 'NONE',  ( 11.99999999999999822, 81.34940948281335693, 10.30890764327412334 ) ) ;
#38661=AXIS2_PLACEMENT_3D ( 'NONE', #38412, #4879, #27403 ) ;
#38667=ORIENTED_EDGE ( 'NONE', *, *, #17563, .F. ) ;
#38672=FACE_OUTER_BOUND ( 'NONE', #2307, .T. ) ;
#38676=EDGE_CURVE ( 'NONE', #21097, #4566, #29741, .T. ) ;
#38678=ORIENTED_EDGE ( 'NONE', *, *, #27014, .T. ) ;
#38682=CIRCLE ( 'NONE', #44121, 31.99999999999999289 ) ;
#38683=FACE_OUTER_BOUND ( 'NONE', #25496, .T. ) ;
#38691=VERTEX_POINT ( 'NONE', #25220 ) ;
#38693=LINE ( 'NONE', #46513, #8265 ) ;
#38697=CARTESIAN_POINT ( 'NONE',  ( 11.99999999999999822, 0.000000000000000000, 0.000000000000000000 ) ) ;
#38699=DIRECTION ( 'NONE',  ( -1.000000000000000000, 0.000000000000000000, 0.000000000000000000 ) ) ;
#38705=DIRECTION ( 'NONE',  ( -1.000000000000000000, -0.000000000000000000, -0.000000000000000000 ) ) ;
#38709=EDGE_LOOP ( 'NONE', ( #2381, #24689, #45383, #2117 ) ) ;
#38710=EDGE_CURVE ( 'NONE', #16517, #44620, #45351, .T. ) ;
#38712=AXIS2_PLACEMENT_3D ( 'NONE', #40987, #36336, #14791 ) ;
#38714=DIRECTION ( 'NONE',  ( -1.000000000000000000, 0.000000000000000000, 0.000000000000000000 ) ) ;
#38715=DIRECTION ( 'NONE',  ( 0.000000000000000000, 0.000000000000000000, 1.000000000000000000 ) ) ;
#38716=CARTESIAN_POINT ( 'NONE',  ( 11.99999999999999822, 26.02418014898407961, -70.52718814184231633 ) ) ;
#38728=FACE_OUTER_BOUND ( 'NONE', #1843, .T. ) ;
#38731=AXIS2_PLACEMENT_3D ( 'NONE', #4191, #45528, #738 ) ;
#38740=ORIENTED_EDGE ( 'NONE', *, *, #38577, .F. ) ;
#38743=DIRECTION ( 'NONE',  ( 0.000000000000000000, 0.4999999999999931166, -0.8660254037844427044 ) ) ;
#38744=ORIENTED_EDGE ( 'NONE', *, *, #2909, .F. ) ;
#38752=CIRCLE ( 'NONE', #41092, 31.99999999999998579 ) ;
#38756=AXIS2_PLACEMENT_3D ( 'NONE', #20802, #42349, #23742 ) ;
#38757=DIRECTION ( 'NONE',  ( -1.000000000000000000, -0.000000000000000000, -0.000000000000000000 ) ) ;
#38760=EDGE_CURVE ( 'NONE', #26898, #12813, #16940, .T. ) ;
#38761=CARTESIAN_POINT ( 'NONE',  ( 0.000000000000000000, -26.01480285779885904, 70.53064760720306481 ) ) ;
#38773=ORIENTED_EDGE ( 'NONE', *, *, #25228, .F. ) ;
#38776=CARTESIAN_POINT ( 'NONE',  ( 11.99999999999999822, 26.01480285779933510, -70.53064760720289428 ) ) ;
#38781=DIRECTION ( 'NONE',  ( 1.000000000000000000, 0.000000000000000000, 0.000000000000000000 ) ) ;
#38784=CARTESIAN_POINT ( 'NONE',  ( 15.00000000000000000, -11.95096189432345746, -23.69967320028757030 ) ) ;
#38786=ORIENTED_EDGE ( 'NONE', *, *, #7642, .T. ) ;
#38790=DIRECTION ( 'NONE',  ( -1.000000000000000000, 0.000000000000000000, 0.000000000000000000 ) ) ;
#38792=DIRECTION ( 'NONE',  ( -1.000000000000000000, -0.000000000000000000, 0.000000000000000000 ) ) ;
#38793=AXIS2_PLACEMENT_3D ( 'NONE', #42126, #19831, #20088 ) ;
#38795=EDGE_CURVE ( 'NONE', #34997, #45805, #2720, .T. ) ;
#38814=EDGE_CURVE ( 'NONE', #6843, #39485, #7053, .T. ) ;
#38816=CYLINDRICAL_SURFACE ( 'NONE', #14742, 31.99999999999998579 ) ;
#38825=CARTESIAN_POINT ( 'NONE',  ( 0.000000000000000000, 75.11764819372149304, 29.05362095685338275 ) ) ;
#38834=EDGE_CURVE ( 'NONE', #31692, #30064, #46944, .T. ) ;
#38835=DIRECTION ( 'NONE',  ( -1.000000000000000000, -0.000000000000000000, 0.000000000000000000 ) ) ;
#38837=ORIENTED_EDGE ( 'NONE', *, *, #18559, .T. ) ;
#38839=FACE_OUTER_BOUND ( 'NONE', #38343, .T. ) ;
#38840=DIRECTION ( 'NONE',  ( 0.000000000000000000, 0.000000000000000000, 1.000000000000000000 ) ) ;
#38842=CIRCLE ( 'NONE', #29456, 77.49900000000000944 ) ;
#38843=DIRECTION ( 'NONE',  ( -1.000000000000000000, -0.000000000000000000, 0.000000000000000000 ) ) ;
#38845=CIRCLE ( 'NONE', #2867, 31.99999999999999289 ) ;
#38847=DIRECTION ( 'NONE',  ( 0.000000000000000000, 0.000000000000000000, -1.000000000000000000 ) ) ;
#38849=EDGE_LOOP ( 'NONE', ( #25610, #30663, #8454, #30709 ) ) ;
#38852=EDGE_CURVE ( 'NONE', #41614, #2440, #8502, .T. ) ;
#38855=EDGE_CURVE ( 'NONE', #2592, #47874, #38370, .T. ) ;
#38857=CARTESIAN_POINT ( 'NONE',  ( 15.00000000000000000, -20.55727247249748402, -16.78983467731284307 ) ) ;
#38858=ORIENTED_EDGE ( 'NONE', *, *, #18228, .T. ) ;
#38861=CARTESIAN_POINT ( 'NONE',  ( 0.000000000000000000, 80.55351364060589958, 15.33399622253512540 ) ) ;
#38865=ORIENTED_EDGE ( 'NONE', *, *, #38632, .T. ) ;
#38872=VECTOR ( 'NONE', #20950, 1000.000000000000000 ) ;
#38875=VERTEX_POINT ( 'NONE', #19032 ) ;
#38877=EDGE_LOOP ( 'NONE', ( #45448, #11371, #57, #37139 ) ) ;
#38882=DIRECTION ( 'NONE',  ( 1.000000000000000000, 0.000000000000000000, 0.000000000000000000 ) ) ;
#38883=CARTESIAN_POINT ( 'NONE',  ( 0.000000000000000000, 0.000000000000000000, 0.000000000000000000 ) ) ;
#38889=CARTESIAN_POINT ( 'NONE',  ( 11.99999999999999822, -35.91791733033428358, -68.67312586195033930 ) ) ;
#38900=DIRECTION ( 'NONE',  ( 0.000000000000000000, 0.3826834323650840086, 0.9238795325112891810 ) ) ;
#38909=PLANE ( 'NONE',  #33946 ) ;
#38910=ORIENTED_EDGE ( 'NONE', *, *, #38021, .F. ) ;
#38912=CYLINDRICAL_SURFACE ( 'NONE', #34281, 31.99999999999998579 ) ;
#38920=VECTOR ( 'NONE', #9435, 1000.000000000000000 ) ;
#38930=EDGE_CURVE ( 'NONE', #11405, #43300, #8993, .T. ) ;
#38937=DIRECTION ( 'NONE',  ( 0.000000000000000000, 0.000000000000000000, 1.000000000000000000 ) ) ;
#38940=DIRECTION ( 'NONE',  ( 0.000000000000000000, 0.000000000000000000, 1.000000000000000000 ) ) ;
#38945=ORIENTED_EDGE ( 'NONE', *, *, #1548, .F. ) ;
#38947=DIRECTION ( 'NONE',  ( -1.000000000000000000, 0.000000000000000000, 0.000000000000000000 ) ) ;
#38953=DIRECTION ( 'NONE',  ( -1.000000000000000000, -0.000000000000000000, 0.000000000000000000 ) ) ;
#38961=CARTESIAN_POINT ( 'NONE',  ( 15.00000000000000000, 5.835314593368470248, -22.81335362449854642 ) ) ;
#38963=CYLINDRICAL_SURFACE ( 'NONE', #10042, 82.00000000000000000 ) ;
#38964=DIRECTION ( 'NONE',  ( -1.000000000000000000, 0.000000000000000000, -0.000000000000000000 ) ) ;
#38968=ADVANCED_FACE ( 'NONE', ( #39336 ), #35669, .T. ) ;
#38970=EDGE_CURVE ( 'NONE', #2738, #12730, #5562, .T. ) ;
#38973=ORIENTED_EDGE ( 'NONE', *, *, #3201, .F. ) ;
#38982=CARTESIAN_POINT ( 'NONE',  ( 15.00000000000000000, -22.67460108101782978, -6.353146135317906840 ) ) ;
#38985=ORIENTED_EDGE ( 'NONE', *, *, #506, .T. ) ;
#38990=CARTESIAN_POINT ( 'NONE',  ( 15.00000000000000000, 5.835314593368777558, 22.81335362449846471 ) ) ;
#38996=ORIENTED_EDGE ( 'NONE', *, *, #34515, .T. ) ;
#39001=ORIENTED_EDGE ( 'NONE', *, *, #21571, .T. ) ;
#39005=DIRECTION ( 'NONE',  ( 1.000000000000000000, 0.000000000000000000, 0.000000000000000000 ) ) ;
#39008=DIRECTION ( 'NONE',  ( 1.000000000000000000, 0.000000000000000000, 0.000000000000000000 ) ) ;
#39018=EDGE_CURVE ( 'NONE', #15250, #9384, #38375, .T. ) ;
#39021=ADVANCED_FACE ( 'NONE', ( #46926 ), #24168, .T. ) ;
#39024=ADVANCED_FACE ( 'NONE', ( #47161 ), #5088, .T. ) ;
#39025=DIRECTION ( 'NONE',  ( 0.000000000000000000, -0.9238795325112821866, -0.3826834323651008285 ) ) ;
#39028=ORIENTED_EDGE ( 'NONE', *, *, #35331, .T. ) ;
#39033=ORIENTED_EDGE ( 'NONE', *, *, #7150, .T. ) ;
#39035=ORIENTED_EDGE ( 'NONE', *, *, #26244, .T. ) ;
#39041=CARTESIAN_POINT ( 'NONE',  ( 11.99999999999999822, -68.55367621811173251, 44.99326035066031437 ) ) ;
#39044=VERTEX_POINT ( 'NONE', #20247 ) ;
#39048=CYLINDRICAL_SURFACE ( 'NONE', #35599, 77.49899999999999523 ) ;
#39051=DIRECTION ( 'NONE',  ( -1.000000000000000000, -0.000000000000000000, -0.000000000000000000 ) ) ;
#39056=ORIENTED_EDGE ( 'NONE', *, *, #26079, .F. ) ;
#39059=DIRECTION ( 'NONE',  ( 1.000000000000000000, 0.000000000000000000, -0.000000000000000000 ) ) ;
#39061=EDGE_CURVE ( 'NONE', #23445, #45870, #41489, .T. ) ;
#39062=VERTEX_POINT ( 'NONE', #12920 ) ;
#39064=DIRECTION ( 'NONE',  ( 0.000000000000000000, -0.8526401643540860720, -0.5224985647159590130 ) ) ;
#39068=EDGE_CURVE ( 'NONE', #43691, #34767, #40541, .T. ) ;
#39075=EDGE_LOOP ( 'NONE', ( #45661, #33170, #33432, #44317 ) ) ;
#39083=ORIENTED_EDGE ( 'NONE', *, *, #36476, .T. ) ;
#39086=ORIENTED_EDGE ( 'NONE', *, *, #16262, .F. ) ;
#39096=DIRECTION ( 'NONE',  ( -1.000000000000000000, -0.000000000000000000, 0.000000000000000000 ) ) ;
#39102=ORIENTED_EDGE ( 'NONE', *, *, #15469, .T. ) ;
#39106=ORIENTED_EDGE ( 'NONE', *, *, #6929, .T. ) ;
#39109=DIRECTION ( 'NONE',  ( 0.000000000000000000, 0.9238795325112851842, 0.3826834323650938896 ) ) ;
#39110=ORIENTED_EDGE ( 'NONE', *, *, #43649, .T. ) ;
#39116=ORIENTED_EDGE ( 'NONE', *, *, #40899, .F. ) ;
#39130=VERTEX_POINT ( 'NONE', #44218 ) ;
#39132=CIRCLE ( 'NONE', #14882, 31.99999999999998934 ) ;
#39134=DIRECTION ( 'NONE',  ( 0.000000000000000000, 0.3090169943749560555, 0.9510565162951506446 ) ) ;
#39136=ORIENTED_EDGE ( 'NONE', *, *, #2230, .F. ) ;
#39138=EDGE_CURVE ( 'NONE', #13341, #28312, #34438, .T. ) ;
#39139=ORIENTED_EDGE ( 'NONE', *, *, #25294, .T. ) ;
#39140=ORIENTED_EDGE ( 'NONE', *, *, #22224, .F. ) ;
#39147=VECTOR ( 'NONE', #39096, 1000.000000000000000 ) ;
#39152=VERTEX_POINT ( 'NONE', #22178 ) ;
#39158=VERTEX_POINT ( 'NONE', #36853 ) ;
#39161=FACE_OUTER_BOUND ( 'NONE', #14486, .T. ) ;
#39163=EDGE_LOOP ( 'NONE', ( #32872, #12487, #32774, #5954 ) ) ;
#39171=CARTESIAN_POINT ( 'NONE',  ( 15.00000000000000000, -18.13022148937263012, -15.02647892043543898 ) ) ;
#39174=EDGE_CURVE ( 'NONE', #48128, #33667, #14611, .T. ) ;
#39175=CARTESIAN_POINT ( 'NONE',  ( 11.99999999999999822, -34.44570377933647620, 69.42325613327427902 ) ) ;
#39177=CARTESIAN_POINT ( 'NONE',  ( 0.000000000000000000, 55.38113227695858143, -54.21277698773617715 ) ) ;
#39181=DIRECTION ( 'NONE',  ( -1.000000000000000000, -0.000000000000000000, 0.000000000000000000 ) ) ;
#39182=VECTOR ( 'NONE', #11321, 1000.000000000000000 ) ;
#39186=EDGE_CURVE ( 'NONE', #21863, #40723, #43821, .T. ) ;
#39191=CARTESIAN_POINT ( 'NONE',  ( 0.000000000000000000, 59.46389618802034960, -49.70050353004825894 ) ) ;
#39192=PLANE ( 'NONE',  #44919 ) ;
#39193=CARTESIAN_POINT ( 'NONE',  ( 0.000000000000000000, 27.74655509720780344, -77.16300072079631889 ) ) ;
#39194=CARTESIAN_POINT ( 'NONE',  ( 15.00000000000000000, -18.13022148937242761, 15.02647892043569122 ) ) ;
#39199=AXIS2_PLACEMENT_3D ( 'NONE', #48433, #41355, #33992 ) ;
#39201=DIRECTION ( 'NONE',  ( -1.000000000000000000, -0.000000000000000000, -0.000000000000000000 ) ) ;
#39202=EDGE_CURVE ( 'NONE', #39316, #2713, #9959, .T. ) ;
#39203=DIRECTION ( 'NONE',  ( 0.000000000000000000, 0.9969173337331281859, -0.07845909572784168229 ) ) ;
#39206=CARTESIAN_POINT ( 'NONE',  ( 11.99999999999999822, 0.000000000000000000, 0.000000000000000000 ) ) ;
#39208=EDGE_CURVE ( 'NONE', #4907, #1534, #21199, .T. ) ;
#39210=ORIENTED_EDGE ( 'NONE', *, *, #39391, .T. ) ;
#39212=ORIENTED_EDGE ( 'NONE', *, *, #33368, .F. ) ;
#39213=DIRECTION ( 'NONE',  ( -1.000000000000000000, 0.000000000000000000, 0.000000000000000000 ) ) ;
#39217=CARTESIAN_POINT ( 'NONE',  ( 0.000000000000000000, -30.41916302227061664, -71.27951684758058093 ) ) ;
#39221=CARTESIAN_POINT ( 'NONE',  ( 0.000000000000000000, -72.35160999960831418, 20.41045688087797672 ) ) ;
#39224=DIRECTION ( 'NONE',  ( -0.000000000000000000, 0.3090169943749573878, 0.9510565162951503115 ) ) ;
#39227=VERTEX_POINT ( 'NONE', #30487 ) ;
#39232=VERTEX_POINT ( 'NONE', #26576 ) ;
#39239=CARTESIAN_POINT ( 'NONE',  ( 11.99999999999999822, 12.93880638057315657, 76.41127070299278046 ) ) ;
#39244=DIRECTION ( 'NONE',  ( 0.000000000000000000, -0.2334453638559126354, 0.9723699203976748917 ) ) ;
#39263=ORIENTED_EDGE ( 'NONE', *, *, #14765, .F. ) ;
#39264=CIRCLE ( 'NONE', #43181, 31.99999999999998224 ) ;
#39265=ADVANCED_FACE ( 'NONE', ( #45660 ), #23144, .T. ) ;
#39266=DIRECTION ( 'NONE',  ( -1.000000000000000000, -0.000000000000000000, 0.000000000000000000 ) ) ;
#39267=CARTESIAN_POINT ( 'NONE',  ( 12.00000000000000000, -1.278221433540145391, 26.51162292216073979 ) ) ;
#39268=DIRECTION ( 'NONE',  ( -1.000000000000000000, 0.000000000000000000, 0.000000000000000000 ) ) ;
#39272=ORIENTED_EDGE ( 'NONE', *, *, #31512, .T. ) ;
#39273=CARTESIAN_POINT ( 'NONE',  ( 0.000000000000000000, 50.95692526931414790, -58.39081064771693974 ) ) ;
#39278=VERTEX_POINT ( 'NONE', #12150 ) ;
#39280=DIRECTION ( 'NONE',  ( -1.000000000000000000, 0.000000000000000000, -0.000000000000000000 ) ) ;
#39282=EDGE_CURVE ( 'NONE', #352, #5583, #36062, .T. ) ;
#39284=DIRECTION ( 'NONE',  ( 0.000000000000000000, 0.6494480483301793283, 0.7604059656000345946 ) ) ;
#39287=CARTESIAN_POINT ( 'NONE',  ( 11.99999999999999822, -11.30684508768284680, -76.66974797899850103 ) ) ;
#39295=DIRECTION ( 'NONE',  ( -1.000000000000000000, 0.000000000000000000, 0.000000000000000000 ) ) ;
#39298=EDGE_LOOP ( 'NONE', ( #6231, #27815, #26289, #10032 ) ) ;
#39299=DIRECTION ( 'NONE',  ( -1.000000000000000000, -0.000000000000000000, 0.000000000000000000 ) ) ;
#39300=EDGE_CURVE ( 'NONE', #11173, #21975, #44940, .T. ) ;
#39302=EDGE_CURVE ( 'NONE', #18, #22172, #8452, .T. ) ;
#39311=VERTEX_POINT ( 'NONE', #8213 ) ;
#39316=VERTEX_POINT ( 'NONE', #19449 ) ;
#39317=EDGE_CURVE ( 'NONE', #27585, #2609, #18733, .T. ) ;
#39321=AXIS2_PLACEMENT_3D ( 'NONE', #5222, #38757, #12555 ) ;
#39327=VECTOR ( 'NONE', #24794, 999.9999999999998863 ) ;
#39329=CIRCLE ( 'NONE', #29969, 82.00000000000000000 ) ;
#39332=ADVANCED_FACE ( 'NONE', ( #855 ), #11167, .T. ) ;
#39333=ORIENTED_EDGE ( 'NONE', *, *, #44203, .T. ) ;
#39335=DIRECTION ( 'NONE',  ( 0.000000000000000000, -0.7071067811865389130, -0.7071067811865562325 ) ) ;
#39336=FACE_OUTER_BOUND ( 'NONE', #33314, .T. ) ;
#39337=VERTEX_POINT ( 'NONE', #7500 ) ;
#39344=CARTESIAN_POINT ( 'NONE',  ( 11.99999999999999822, 0.000000000000000000, 0.000000000000000000 ) ) ;
#39351=EDGE_CURVE ( 'NONE', #40885, #16815, #41273, .T. ) ;
#39353=EDGE_LOOP ( 'NONE', ( #18506, #36241, #27835, #31363 ) ) ;
#39361=AXIS2_PLACEMENT_3D ( 'NONE', #39785, #21160, #2554 ) ;
#39370=VECTOR ( 'NONE', #23402, 1000.000000000000000 ) ;
#39373=VERTEX_POINT ( 'NONE', #1598 ) ;
#39374=VECTOR ( 'NONE', #35775, 1000.000000000000114 ) ;
#39378=DIRECTION ( 'NONE',  ( -1.000000000000000000, 0.000000000000000000, 0.000000000000000000 ) ) ;
#39383=CIRCLE ( 'NONE', #5770, 77.49899999999998101 ) ;
#39391=EDGE_CURVE ( 'NONE', #14588, #20955, #43096, .T. ) ;
#39393=AXIS2_PLACEMENT_3D ( 'NONE', #10934, #21468, #7255 ) ;
#39397=ORIENTED_EDGE ( 'NONE', *, *, #30412, .F. ) ;
#39400=EDGE_CURVE ( 'NONE', #42640, #45331, #4037, .T. ) ;
#39406=CYLINDRICAL_SURFACE ( 'NONE', #3576, 82.00000000000000000 ) ;
#39407=ORIENTED_EDGE ( 'NONE', *, *, #28339, .T. ) ;
#39418=ORIENTED_EDGE ( 'NONE', *, *, #11337, .F. ) ;
#39419=DIRECTION ( 'NONE',  ( -1.000000000000000000, -0.000000000000000000, 0.000000000000000000 ) ) ;
#39423=ORIENTED_EDGE ( 'NONE', *, *, #39068, .F. ) ;
#39426=ORIENTED_EDGE ( 'NONE', *, *, #5687, .F. ) ;
#39430=CARTESIAN_POINT ( 'NONE',  ( 15.00000000000000000, -22.32062822937469093, 14.36278369418830181 ) ) ;
#39437=AXIS2_PLACEMENT_3D ( 'NONE', #36540, #28724, #43650 ) ;
#39438=CARTESIAN_POINT ( 'NONE',  ( 11.99999999999999822, -59.75363087400113926, 56.15606465354937171 ) ) ;
#39440=AXIS2_PLACEMENT_3D ( 'NONE', #14233, #39948, #29153 ) ;
#39441=CARTESIAN_POINT ( 'NONE',  ( 12.00000000000000000, -10.45096189432344502, -21.10159698893425784 ) ) ;
#39443=CARTESIAN_POINT ( 'NONE',  ( 0.000000000000000000, -2.946379043145784582, -75.11764819372150725 ) ) ;
#39447=FACE_OUTER_BOUND ( 'NONE', #17134, .T. ) ;
#39448=VECTOR ( 'NONE', #6618, 1000.000000000000114 ) ;
#39449=AXIS2_PLACEMENT_3D ( 'NONE', #30034, #37375, #3343 ) ;
#39452=DIRECTION ( 'NONE',  ( -1.000000000000000000, 0.000000000000000000, 0.000000000000000000 ) ) ;
#39457=CYLINDRICAL_SURFACE ( 'NONE', #31270, 31.99999999999998579 ) ;
#39458=ORIENTED_EDGE ( 'NONE', *, *, #28786, .T. ) ;
#39469=CARTESIAN_POINT ( 'NONE',  ( 11.99999999999999822, 0.000000000000000000, 0.000000000000000000 ) ) ;
#39471=CIRCLE ( 'NONE', #18350, 82.00000000000000000 ) ;
#39473=DIRECTION ( 'NONE',  ( 0.000000000000000000, 0.000000000000000000, -1.000000000000000000 ) ) ;
#39474=ADVANCED_FACE ( 'NONE', ( #38563 ), #9180, .F. ) ;
#39475=DIRECTION ( 'NONE',  ( 1.000000000000000000, 0.000000000000000000, -0.000000000000000000 ) ) ;
#39476=LINE ( 'NONE', #13514, #30202 ) ;
#39478=CYLINDRICAL_SURFACE ( 'NONE', #28153, 31.99999999999998579 ) ;
#39480=AXIS2_PLACEMENT_3D ( 'NONE', #7179, #3508, #14286 ) ;
#39481=CIRCLE ( 'NONE', #13687, 82.00000000000000000 ) ;
#39482=ORIENTED_EDGE ( 'NONE', *, *, #19197, .T. ) ;
#39483=FACE_OUTER_BOUND ( 'NONE', #42087, .T. ) ;
#39484=ORIENTED_EDGE ( 'NONE', *, *, #5850, .F. ) ;
#39485=VERTEX_POINT ( 'NONE', #39041 ) ;
#39494=CYLINDRICAL_SURFACE ( 'NONE', #11980, 77.49899999999999523 ) ;
#39497=ADVANCED_FACE ( 'NONE', ( #42470 ), #14293, .T. ) ;
#39499=LINE ( 'NONE', #2056, #1980 ) ;
#39501=CYLINDRICAL_SURFACE ( 'NONE', #36493, 82.00000000000000000 ) ;
#39504=ORIENTED_EDGE ( 'NONE', *, *, #7567, .T. ) ;
#39507=ORIENTED_EDGE ( 'NONE', *, *, #6737, .T. ) ;
#39512=CARTESIAN_POINT ( 'NONE',  ( 11.99999999999999822, 73.73191006444572793, -14.66109333815486515 ) ) ;
#39517=DIRECTION ( 'NONE',  ( -1.000000000000000000, 0.000000000000000000, 0.000000000000000000 ) ) ;
#39533=CARTESIAN_POINT ( 'NONE',  ( 11.99999999999999822, 41.76106447765580043, -62.50884508063379741 ) ) ;
#39537=ORIENTED_EDGE ( 'NONE', *, *, #29303, .F. ) ;
#39546=DIRECTION ( 'NONE',  ( 0.000000000000000000, 0.000000000000000000, 1.000000000000000000 ) ) ;
#39555=CARTESIAN_POINT ( 'NONE',  ( 0.000000000000000000, -0.8261519478436571973, 77.49459641780886443 ) ) ;
#39563=VECTOR ( 'NONE', #39790, 1000.000000000000000 ) ;
#39568=EDGE_CURVE ( 'NONE', #30063, #4413, #17288, .T. ) ;
#39575=ORIENTED_EDGE ( 'NONE', *, *, #22772, .F. ) ;
#39582=EDGE_CURVE ( 'NONE', #31175, #17149, #17950, .T. ) ;
#39585=VERTEX_POINT ( 'NONE', #7187 ) ;
#39589=ADVANCED_FACE ( 'NONE', ( #6950 ), #21391, .T. ) ;
#39592=VERTEX_POINT ( 'NONE', #21867 ) ;
#39595=EDGE_LOOP ( 'NONE', ( #15962, #31091, #5504, #19339 ) ) ;
#39596=VERTEX_POINT ( 'NONE', #3264 ) ;
#39598=DIRECTION ( 'NONE',  ( 0.000000000000000000, 0.000000000000000000, 1.000000000000000000 ) ) ;
#39601=ORIENTED_EDGE ( 'NONE', *, *, #4365, .F. ) ;
#39603=VECTOR ( 'NONE', #46477, 1000.000000000000000 ) ;
#39611=DIRECTION ( 'NONE',  ( 0.000000000000000000, 0.000000000000000000, -1.000000000000000000 ) ) ;
#39615=DIRECTION ( 'NONE',  ( 0.000000000000000000, 0.000000000000000000, 1.000000000000000000 ) ) ;
#39617=DIRECTION ( 'NONE',  ( -1.000000000000000000, -0.000000000000000000, -0.000000000000000000 ) ) ;
#39618=ORIENTED_EDGE ( 'NONE', *, *, #36630, .F. ) ;
#39621=LINE ( 'NONE', #9736, #16821 ) ;
#39624=DIRECTION ( 'NONE',  ( -1.000000000000000000, 0.000000000000000000, -0.000000000000000000 ) ) ;
#39625=DIRECTION ( 'NONE',  ( 0.000000000000000000, 0.000000000000000000, 1.000000000000000000 ) ) ;
#39630=CARTESIAN_POINT ( 'NONE',  ( 0.000000000000000000, 2.543863470249533965, -81.96053171279901051 ) ) ;
#39641=EDGE_LOOP ( 'NONE', ( #12982, #16527 ) ) ;
#39642=CARTESIAN_POINT ( 'NONE',  ( 12.00000000000000000, 23.59884966291538078, 12.14883922797231008 ) ) ;
#39646=ORIENTED_EDGE ( 'NONE', *, *, #5301, .T. ) ;
#39648=VERTEX_POINT ( 'NONE', #76 ) ;
#39649=EDGE_CURVE ( 'NONE', #28383, #28563, #7441, .T. ) ;
#39652=ORIENTED_EDGE ( 'NONE', *, *, #22024, .F. ) ;
#39654=EDGE_CURVE ( 'NONE', #36243, #43300, #44690, .T. ) ;
#39664=CARTESIAN_POINT ( 'NONE',  ( 0.000000000000000000, -76.69515212745996280, -29.01471420065643869 ) ) ;
#39665=CARTESIAN_POINT ( 'NONE',  ( 0.000000000000000000, 75.54627589209944460, 17.28742895386110945 ) ) ;
#39666=ORIENTED_EDGE ( 'NONE', *, *, #27208, .F. ) ;
#39669=CARTESIAN_POINT ( 'NONE',  ( 0.000000000000000000, -81.50828551894234408, 8.966570791700414489 ) ) ;
#39671=CIRCLE ( 'NONE', #21685, 31.99999999999998579 ) ;
#39676=ORIENTED_EDGE ( 'NONE', *, *, #13886, .T. ) ;
#39678=DIRECTION ( 'NONE',  ( -1.000000000000000000, 0.000000000000000000, -0.000000000000000000 ) ) ;
#39679=FACE_OUTER_BOUND ( 'NONE', #5194, .T. ) ;
#39682=DIRECTION ( 'NONE',  ( 0.000000000000000000, 0.000000000000000000, -1.000000000000000000 ) ) ;
#39683=ADVANCED_FACE ( 'NONE', ( #30433 ), #26027, .T. ) ;
#39686=ADVANCED_FACE ( 'NONE', ( #11594 ), #33847, .F. ) ;
#39687=DIRECTION ( 'NONE',  ( -1.000000000000000000, -0.000000000000000000, 0.000000000000000000 ) ) ;
#39694=ORIENTED_EDGE ( 'NONE', *, *, #21984, .T. ) ;
#39695=VECTOR ( 'NONE', #45300, 1000.000000000000000 ) ;
#39697=CARTESIAN_POINT ( 'NONE',  ( 5.999999999999999112, -40.65526001592663619, 71.21200624218782593 ) ) ;
#39700=DIRECTION ( 'NONE',  ( -1.000000000000000000, 0.000000000000000000, -0.000000000000000000 ) ) ;
#39703=EDGE_CURVE ( 'NONE', #23034, #13690, #7169, .T. ) ;
#39706=LINE ( 'NONE', #21069, #46115 ) ;
#39707=DIRECTION ( 'NONE',  ( -1.000000000000000000, 0.000000000000000000, 0.000000000000000000 ) ) ;
#39713=DIRECTION ( 'NONE',  ( 0.000000000000000000, 0.9135454576426055295, 0.4067366430757899387 ) ) ;
#39718=VERTEX_POINT ( 'NONE', #18449 ) ;
#39723=ORIENTED_EDGE ( 'NONE', *, *, #41282, .F. ) ;
#39727=DIRECTION ( 'NONE',  ( -1.000000000000000000, 0.000000000000000000, -0.000000000000000000 ) ) ;
#39730=DIRECTION ( 'NONE',  ( 0.000000000000000000, 0.5877852522924743583, -0.8090169943749465631 ) ) ;
#39733=ORIENTED_EDGE ( 'NONE', *, *, #25183, .F. ) ;
#39736=DIRECTION ( 'NONE',  ( 0.000000000000000000, 0.000000000000000000, 1.000000000000000000 ) ) ;
#39737=CYLINDRICAL_SURFACE ( 'NONE', #28240, 31.99999999999998579 ) ;
#39741=CARTESIAN_POINT ( 'NONE',  ( 12.00000000000000000, 16.61724383029390140, 20.69703378468902955 ) ) ;
#39744=CARTESIAN_POINT ( 'NONE',  ( 6.000000000000000000, 78.73519480814985627, -22.90783923731547489 ) ) ;
#39745=ADVANCED_FACE ( 'NONE', ( #38024 ), #321, .T. ) ;
#39746=CARTESIAN_POINT ( 'NONE',  ( 11.99999999999999822, 50.95692526931414790, -58.39081064771693974 ) ) ;
#39747=DIRECTION ( 'NONE',  ( -1.000000000000000000, 0.000000000000000000, -0.000000000000000000 ) ) ;
#39749=ADVANCED_FACE ( 'NONE', ( #41449 ), #4492, .F. ) ;
#39760=CARTESIAN_POINT ( 'NONE',  ( 0.000000000000000000, 68.27212725128275395, 31.46837873495001503 ) ) ;
#39771=ORIENTED_EDGE ( 'NONE', *, *, #11398, .T. ) ;
#39772=DIRECTION ( 'NONE',  ( 1.000000000000000000, -0.000000000000000000, -0.000000000000000000 ) ) ;
#39774=LINE ( 'NONE', #40009, #40555 ) ;
#39775=CARTESIAN_POINT ( 'NONE',  ( 0.000000000000000000, 71.21200624218795383, 40.65526001592638039 ) ) ;
#39784=DIRECTION ( 'NONE',  ( 0.000000000000000000, 0.5224985647159500202, -0.8526401643540915121 ) ) ;
#39785=CARTESIAN_POINT ( 'NONE',  ( 15.00000000000000000, 14.60985201121729737, 18.46759930825687235 ) ) ;
#39788=CARTESIAN_POINT ( 'NONE',  ( 11.99999999999999822, -5.256550761632340141, -77.32052557432847095 ) ) ;
#39790=DIRECTION ( 'NONE',  ( -1.000000000000000000, 0.000000000000000000, -0.000000000000000000 ) ) ;
#39798=CARTESIAN_POINT ( 'NONE',  ( 0.000000000000000000, 46.11716303203186840, 67.80270845531904911 ) ) ;
#39802=CARTESIAN_POINT ( 'NONE',  ( 12.00000000000000000, -22.67460108101782978, -6.353146135317906840 ) ) ;
#39807=CARTESIAN_POINT ( 'NONE',  ( 0.000000000000000000, -28.89263327155795480, 71.91182617369177876 ) ) ;
#39811=STYLED_ITEM ( 'NONE', ( #7819 ), #20448 ) ;
#39817=ADVANCED_FACE ( 'NONE', ( #46326 ), #1039, .T. ) ;
#39819=CIRCLE ( 'NONE', #17882, 77.49900000000000944 ) ;
#39822=VERTEX_POINT ( 'NONE', #34823 ) ;
#39826=ORIENTED_EDGE ( 'NONE', *, *, #29087, .T. ) ;
#39834=DIRECTION ( 'NONE',  ( 1.000000000000000000, 0.000000000000000000, 0.000000000000000000 ) ) ;
#39836=DIRECTION ( 'NONE',  ( -1.000000000000000000, -0.000000000000000000, 0.000000000000000000 ) ) ;
#39843=ORIENTED_EDGE ( 'NONE', *, *, #19034, .F. ) ;
#39844=ADVANCED_FACE ( 'NONE', ( #31170 ), #9124, .T. ) ;
#39846=ORIENTED_EDGE ( 'NONE', *, *, #44723, .T. ) ;
#39847=DIRECTION ( 'NONE',  ( 0.000000000000000000, 0.9969173337331276308, 0.07845909572784864894 ) ) ;
#39849=DIRECTION ( 'NONE',  ( 1.000000000000000000, -0.000000000000000000, 0.000000000000000000 ) ) ;
#39851=CARTESIAN_POINT ( 'NONE',  ( 0.000000000000000000, -6.903761155837269570, -77.19088730480530103 ) ) ;
#39853=CARTESIAN_POINT ( 'NONE',  ( 0.000000000000000000, 0.000000000000000000, 0.000000000000000000 ) ) ;
#39855=CARTESIAN_POINT ( 'NONE',  ( 11.99999999999999822, 0.000000000000000000, 0.000000000000000000 ) ) ;
#39859=ADVANCED_FACE ( 'NONE', ( #46091 ), #34563, .F. ) ;
#39871=EDGE_CURVE ( 'NONE', #45060, #6106, #8396, .T. ) ;
#39876=EDGE_CURVE ( 'NONE', #4851, #18715, #41373, .T. ) ;
#39881=DIRECTION ( 'NONE',  ( -1.000000000000000000, 0.000000000000000000, -0.000000000000000000 ) ) ;
#39883=DIRECTION ( 'NONE',  ( -0.000000000000000000, -0.6691306063588670083, -0.7431448254773863615 ) ) ;
#39891=CIRCLE ( 'NONE', #4818, 82.00000000000000000 ) ;
#39897=EDGE_CURVE ( 'NONE', #36121, #36422, #1028, .T. ) ;
#39901=VERTEX_POINT ( 'NONE', #33762 ) ;
#39910=CARTESIAN_POINT ( 'NONE',  ( 15.00000000000000000, 6.762365576493310826, -25.66652317338401090 ) ) ;
#39913=CARTESIAN_POINT ( 'NONE',  ( 0.000000000000000000, 31.47745569255237896, -68.26794271651228030 ) ) ;
#39918=ORIENTED_EDGE ( 'NONE', *, *, #43427, .F. ) ;
#39919=ORIENTED_EDGE ( 'NONE', *, *, #29700, .T. ) ;
#39930=ORIENTED_EDGE ( 'NONE', *, *, #2941, .T. ) ;
#39935=EDGE_LOOP ( 'NONE', ( #10965, #9428, #3868, #41455 ) ) ;
#39938=ORIENTED_EDGE ( 'NONE', *, *, #44436, .T. ) ;
#39947=EDGE_CURVE ( 'NONE', #4851, #38433, #39383, .T. ) ;
#39948=DIRECTION ( 'NONE',  ( 1.000000000000000000, 0.000000000000000000, 0.000000000000000000 ) ) ;
#39949=DIRECTION ( 'NONE',  ( 0.000000000000000000, -0.7431448254773954654, -0.6691306063588569053 ) ) ;
#39951=DIRECTION ( 'NONE',  ( -1.000000000000000000, 0.000000000000000000, -0.000000000000000000 ) ) ;
#39953=DIRECTION ( 'NONE',  ( 0.000000000000000000, 0.5877852522924742473, -0.8090169943749466741 ) ) ;
#39954=VERTEX_POINT ( 'NONE', #952 ) ;
#39955=AXIS2_PLACEMENT_3D ( 'NONE', #10195, #33438, #48361 ) ;
#39963=AXIS2_PLACEMENT_3D ( 'NONE', #12257, #27179, #23492 ) ;
#39972=EDGE_CURVE ( 'NONE', #26898, #14427, #41862, .T. ) ;
#39974=FACE_OUTER_BOUND ( 'NONE', #19452, .T. ) ;
#39977=ORIENTED_EDGE ( 'NONE', *, *, #38291, .F. ) ;
#39980=DIRECTION ( 'NONE',  ( -1.000000000000000000, -0.000000000000000000, -0.000000000000000000 ) ) ;
#39987=EDGE_LOOP ( 'NONE', ( #32016, #26357, #7110, #32382 ) ) ;
#39993=AXIS2_PLACEMENT_3D ( 'NONE', #5090, #35171, #5565 ) ;
#39995=ORIENTED_EDGE ( 'NONE', *, *, #26918, .F. ) ;
#39999=LINE ( 'NONE', #40705, #44813 ) ;
#40000=VERTEX_POINT ( 'NONE', #34010 ) ;
#40003=VECTOR ( 'NONE', #40187, 1000.000000000000114 ) ;
#40005=ORIENTED_EDGE ( 'NONE', *, *, #30133, .F. ) ;
#40006=CARTESIAN_POINT ( 'NONE',  ( 11.99999999999999822, -76.41127070299280888, 12.93880638057290788 ) ) ;
#40007=ADVANCED_FACE ( 'NONE', ( #45277 ), #27532, .F. ) ;
#40008=ORIENTED_EDGE ( 'NONE', *, *, #11608, .F. ) ;
#40009=CARTESIAN_POINT ( 'NONE',  ( 15.00000000000000000, -19.89357724625003598, -12.59942793731059041 ) ) ;
#40010=CARTESIAN_POINT ( 'NONE',  ( 15.00000000000000000, -18.13022148937263012, -15.02647892043543898 ) ) ;
#40012=EDGE_LOOP ( 'NONE', ( #40601, #4731, #16924, #11035 ) ) ;
#40013=LINE ( 'NONE', #19637, #16968 ) ;
#40015=VERTEX_POINT ( 'NONE', #31458 ) ;
#40022=ADVANCED_FACE ( 'NONE', ( #47093 ), #1586, .F. ) ;
#40028=VECTOR ( 'NONE', #47810, 1000.000000000000000 ) ;
#40031=AXIS2_PLACEMENT_3D ( 'NONE', #33318, #13764, #12023 ) ;
#40036=CARTESIAN_POINT ( 'NONE',  ( 11.99999999999999822, -18.89407956138310496, 75.16055320797023853 ) ) ;
#40039=DIRECTION ( 'NONE',  ( -1.000000000000000000, 0.000000000000000000, 0.000000000000000000 ) ) ;
#40042=CIRCLE ( 'NONE', #36116, 31.99999999999998579 ) ;
#40044=CARTESIAN_POINT ( 'NONE',  ( 11.99999999999999822, -66.50666863321974631, -39.78640506895675344 ) ) ;
#40048=DIRECTION ( 'NONE',  ( -1.000000000000000000, 0.000000000000000000, 0.000000000000000000 ) ) ;
#40049=ORIENTED_EDGE ( 'NONE', *, *, #30411, .F. ) ;
#40053=CARTESIAN_POINT ( 'NONE',  ( 11.99999999999999822, -46.53671651293907274, -59.03961581697448935 ) ) ;
#40055=CARTESIAN_POINT ( 'NONE',  ( 0.000000000000000000, 12.93880638057315302, 76.41127070299275204 ) ) ;
#40057=VERTEX_POINT ( 'NONE', #42711 ) ;
#40063=DIRECTION ( 'NONE',  ( -1.000000000000000000, 0.000000000000000000, -0.000000000000000000 ) ) ;
#40067=ORIENTED_EDGE ( 'NONE', *, *, #35683, .F. ) ;
#40069=FACE_OUTER_BOUND ( 'NONE', #47585, .T. ) ;
#40074=ORIENTED_EDGE ( 'NONE', *, *, #21864, .T. ) ;
#40077=EDGE_CURVE ( 'NONE', #20184, #7124, #31713, .T. ) ;
#40082=ADVANCED_FACE ( 'NONE', ( #13089 ), #20664, .F. ) ;
#40088=CYLINDRICAL_SURFACE ( 'NONE', #15887, 31.99999999999998579 ) ;
#40090=CARTESIAN_POINT ( 'NONE',  ( 6.000000000000000000, 74.18225833017937987, -34.94270380257559339 ) ) ;
#40092=EDGE_CURVE ( 'NONE', #42537, #14617, #29203, .T. ) ;
#40095=DIRECTION ( 'NONE',  ( -1.000000000000000000, 0.000000000000000000, 0.000000000000000000 ) ) ;
#40096=CARTESIAN_POINT ( 'NONE',  ( 11.99999999999999822, 3.894527615417885169, 81.90746397400390322 ) ) ;
#40097=DIRECTION ( 'NONE',  ( -1.000000000000000000, 0.000000000000000000, 0.000000000000000000 ) ) ;
#40099=AXIS2_PLACEMENT_3D ( 'NONE', #14901, #22492, #26644 ) ;
#40101=DIRECTION ( 'NONE',  ( -0.000000000000000000, 0.1045284632676569680, 0.9945218953682730678 ) ) ;
#40106=VERTEX_POINT ( 'NONE', #42947 ) ;
#40107=AXIS2_PLACEMENT_3D ( 'NONE', #12591, #41484, #30970 ) ;
#40108=DIRECTION ( 'NONE',  ( -1.000000000000000000, -0.000000000000000000, 0.000000000000000000 ) ) ;
#40111=CARTESIAN_POINT ( 'NONE',  ( 11.99999999999999822, 0.000000000000000000, 0.000000000000000000 ) ) ;
#40112=EDGE_CURVE ( 'NONE', #31521, #10773, #20181, .T. ) ;
#40113=ORIENTED_EDGE ( 'NONE', *, *, #37069, .T. ) ;
#40114=ORIENTED_EDGE ( 'NONE', *, *, #35704, .F. ) ;
#40122=EDGE_CURVE ( 'NONE', #17270, #27718, #37802, .T. ) ;
#40131=LINE ( 'NONE', #47230, #9569 ) ;
#40134=EDGE_LOOP ( 'NONE', ( #5350, #33194, #14613, #47340 ) ) ;
#40136=DIRECTION ( 'NONE',  ( 0.000000000000000000, 0.000000000000000000, 1.000000000000000000 ) ) ;
#40138=VECTOR ( 'NONE', #13596, 1000.000000000000000 ) ;
#40139=ORIENTED_EDGE ( 'NONE', *, *, #33329, .T. ) ;
#40147=LINE ( 'NONE', #36462, #26921 ) ;
#40151=VECTOR ( 'NONE', #43437, 1000.000000000000000 ) ;
#40152=DIRECTION ( 'NONE',  ( -1.000000000000000000, 0.000000000000000000, 0.000000000000000000 ) ) ;
#40154=VERTEX_POINT ( 'NONE', #44387 ) ;
#40165=AXIS2_PLACEMENT_3D ( 'NONE', #34836, #35076, #1556 ) ;
#40168=CYLINDRICAL_SURFACE ( 'NONE', #18292, 77.49899999999999523 ) ;
#40177=VERTEX_POINT ( 'NONE', #3015 ) ;
#40181=EDGE_CURVE ( 'NONE', #14655, #19593, #39999, .T. ) ;
#40182=EDGE_LOOP ( 'NONE', ( #21570, #17082, #20245, #21660 ) ) ;
#40183=DIRECTION ( 'NONE',  ( 0.000000000000000000, 0.000000000000000000, 1.000000000000000000 ) ) ;
#40187=DIRECTION ( 'NONE',  ( -0.000000000000000000, 0.4999999999999921174, -0.8660254037844432595 ) ) ;
#40188=VERTEX_POINT ( 'NONE', #17940 ) ;
#40190=ORIENTED_EDGE ( 'NONE', *, *, #5426, .F. ) ;
#40201=ORIENTED_EDGE ( 'NONE', *, *, #17633, .T. ) ;
#40203=CIRCLE ( 'NONE', #32375, 77.49899999999999523 ) ;
#40204=LINE ( 'NONE', #47755, #16810 ) ;
#40207=LINE ( 'NONE', #47307, #23491 ) ;
#40212=DIRECTION ( 'NONE',  ( 1.000000000000000000, -0.000000000000000000, -0.000000000000000000 ) ) ;
#40215=VERTEX_POINT ( 'NONE', #17462 ) ;
#40216=AXIS2_PLACEMENT_3D ( 'NONE', #7363, #23922, #33773 ) ;
#40230=VERTEX_POINT ( 'NONE', #18179 ) ;
#40231=CARTESIAN_POINT ( 'NONE',  ( 11.99999999999999822, -23.16143007188376757, -73.95703589263997912 ) ) ;
#40234=FACE_OUTER_BOUND ( 'NONE', #9600, .T. ) ;
#40237=EDGE_CURVE ( 'NONE', #14950, #26390, #29972, .T. ) ;
#40240=FACE_OUTER_BOUND ( 'NONE', #32599, .T. ) ;
#40243=EDGE_CURVE ( 'NONE', #28195, #46892, #27641, .T. ) ;
#40248=AXIS2_PLACEMENT_3D ( 'NONE', #34903, #35815, #9613 ) ;
#40249=EDGE_CURVE ( 'NONE', #27199, #38067, #37034, .T. ) ;
#40250=CARTESIAN_POINT ( 'NONE',  ( 5.999999999999999112, 67.80270845531956070, -46.11716303203111522 ) ) ;
#40258=AXIS2_PLACEMENT_3D ( 'NONE', #47823, #47374, #43926 ) ;
#40261=DIRECTION ( 'NONE',  ( -1.000000000000000000, -0.000000000000000000, 0.000000000000000000 ) ) ;
#40262=ORIENTED_EDGE ( 'NONE', *, *, #4232, .F. ) ;
#40263=DIRECTION ( 'NONE',  ( 1.000000000000000000, 0.000000000000000000, 0.000000000000000000 ) ) ;
#40264=ORIENTED_EDGE ( 'NONE', *, *, #33696, .F. ) ;
#40266=CARTESIAN_POINT ( 'NONE',  ( 11.99999999999999822, -73.44644590900077219, 24.73286445877677764 ) ) ;
#40270=ORIENTED_EDGE ( 'NONE', *, *, #5732, .T. ) ;
#40273=CARTESIAN_POINT ( 'NONE',  ( 0.000000000000000000, 69.42325613327440692, 34.44570377933622041 ) ) ;
#40283=AXIS2_PLACEMENT_3D ( 'NONE', #39533, #35105, #16516 ) ;
#40284=AXIS2_PLACEMENT_3D ( 'NONE', #29694, #14779, #22108 ) ;
#40285=DIRECTION ( 'NONE',  ( -1.000000000000000000, 0.000000000000000000, 0.000000000000000000 ) ) ;
#40286=DIRECTION ( 'NONE',  ( 0.000000000000000000, 0.9135454576426010886, -0.4067366430757998752 ) ) ;
#40290=AXIS2_PLACEMENT_3D ( 'NONE', #27326, #12880, #4564 ) ;
#40291=ADVANCED_FACE ( 'NONE', ( #18902 ), #41439, .F. ) ;
#40293=VECTOR ( 'NONE', #21156, 1000.000000000000000 ) ;
#40296=ORIENTED_EDGE ( 'NONE', *, *, #30016, .F. ) ;
#40299=CIRCLE ( 'NONE', #9777, 82.00000000000000000 ) ;
#40301=EDGE_CURVE ( 'NONE', #12455, #9769, #24568, .T. ) ;
#40305=ORIENTED_EDGE ( 'NONE', *, *, #7021, .F. ) ;
#40310=ORIENTED_EDGE ( 'NONE', *, *, #39061, .F. ) ;
#40312=ORIENTED_EDGE ( 'NONE', *, *, #17548, .F. ) ;
#40313=ORIENTED_EDGE ( 'NONE', *, *, #12334, .T. ) ;
#40315=DIRECTION ( 'NONE',  ( 0.000000000000000000, 0.000000000000000000, 1.000000000000000000 ) ) ;
#40316=EDGE_CURVE ( 'NONE', #42776, #43483, #9699, .T. ) ;
#40318=ORIENTED_EDGE ( 'NONE', *, *, #23190, .F. ) ;
#40319=CARTESIAN_POINT ( 'NONE',  ( 15.00000000000000000, 8.688484142253932063, -21.88630264137371029 ) ) ;
#40320=CIRCLE ( 'NONE', #19199, 31.99999999999998579 ) ;
#40321=AXIS2_PLACEMENT_3D ( 'NONE', #5627, #21259, #36194 ) ;
#40323=ORIENTED_EDGE ( 'NONE', *, *, #38855, .T. ) ;
#40326=EDGE_LOOP ( 'NONE', ( #15554, #42997, #21672, #48036 ) ) ;
#40329=CARTESIAN_POINT ( 'NONE',  ( 15.00000000000000000, 9.615535125378766423, -24.73947219025917121 ) ) ;
#40331=EDGE_LOOP ( 'NONE', ( #34076, #17538, #29931, #12504 ) ) ;
#40332=CARTESIAN_POINT ( 'NONE',  ( 11.99999999999999822, 0.000000000000000000, 0.000000000000000000 ) ) ;
#40339=DIRECTION ( 'NONE',  ( 0.000000000000000000, 0.4539904997395413644, 0.8910065241883706744 ) ) ;
#40340=DIRECTION ( 'NONE',  ( -1.000000000000000000, 0.000000000000000000, -0.000000000000000000 ) ) ;
#40343=LINE ( 'NONE', #36411, #18208 ) ;
#40344=CARTESIAN_POINT ( 'NONE',  ( 11.99999999999999822, -81.90746397400386059, -3.894527615418766242 ) ) ;
#40345=DIRECTION ( 'NONE',  ( 0.000000000000000000, -0.3090169943749551673, -0.9510565162951510887 ) ) ;
#40349=CARTESIAN_POINT ( 'NONE',  ( 0.000000000000000000, -59.46389618801999433, 49.70050353004867816 ) ) ;
#40354=ORIENTED_EDGE ( 'NONE', *, *, #10622, .T. ) ;
#40360=DIRECTION ( 'NONE',  ( -1.000000000000000000, 0.000000000000000000, -0.000000000000000000 ) ) ;
#40361=VERTEX_POINT ( 'NONE', #4713 ) ;
#40362=EDGE_CURVE ( 'NONE', #35973, #36385, #12831, .T. ) ;
#40374=DIRECTION ( 'NONE',  ( -1.000000000000000000, -0.000000000000000000, -0.000000000000000000 ) ) ;
#40375=DIRECTION ( 'NONE',  ( 1.000000000000000000, -0.000000000000000000, 0.000000000000000000 ) ) ;
#40382=AXIS2_PLACEMENT_3D ( 'NONE', #33488, #48414, #20251 ) ;
#40394=DIRECTION ( 'NONE',  ( -1.000000000000000000, 0.000000000000000000, -0.000000000000000000 ) ) ;
#40397=CARTESIAN_POINT ( 'NONE',  ( 12.00000000000000000, -13.04903810567646971, 19.60159698893442126 ) ) ;
#40398=EDGE_CURVE ( 'NONE', #39130, #40215, #302, .T. ) ;
#40399=CARTESIAN_POINT ( 'NONE',  ( 0.000000000000000000, -80.55351364060578589, -15.33399622253570094 ) ) ;
#40400=CARTESIAN_POINT ( 'NONE',  ( 15.00000000000000000, -0.9646360437372099028, 23.52805723605590771 ) ) ;
#40412=FACE_OUTER_BOUND ( 'NONE', #20787, .T. ) ;
#40413=ORIENTED_EDGE ( 'NONE', *, *, #44995, .T. ) ;
#40423=ORIENTED_EDGE ( 'NONE', *, *, #28175, .T. ) ;
#40425=CYLINDRICAL_SURFACE ( 'NONE', #25052, 31.99999999999998579 ) ;
#40436=EDGE_CURVE ( 'NONE', #7287, #10250, #10479, .T. ) ;
#40454=VECTOR ( 'NONE', #10639, 1000.000000000000000 ) ;
#40461=CIRCLE ( 'NONE', #5272, 77.49899999999999523 ) ;
#40464=CARTESIAN_POINT ( 'NONE',  ( 11.99999999999999822, 76.69515212746057387, -29.01471420065479379 ) ) ;
#40465=CARTESIAN_POINT ( 'NONE',  ( 11.99999999999999822, 0.000000000000000000, 0.000000000000000000 ) ) ;
#40479=CARTESIAN_POINT ( 'NONE',  ( 11.99999999999999822, 0.000000000000000000, 0.000000000000000000 ) ) ;
#40480=ORIENTED_EDGE ( 'NONE', *, *, #1233, .F. ) ;
#40481=VECTOR ( 'NONE', #9129, 1000.000000000000227 ) ;
#40483=VERTEX_POINT ( 'NONE', #5211 ) ;
#40484=CARTESIAN_POINT ( 'NONE',  ( 12.00000000000000000, 23.59884966291521735, -12.14883922797262805 ) ) ;
#40491=CARTESIAN_POINT ( 'NONE',  ( 0.000000000000000000, 23.16143007188426850, 73.95703589263983702 ) ) ;
#40493=CARTESIAN_POINT ( 'NONE',  ( 15.00000000000000000, 22.07842321921480888, -8.187992925817425771 ) ) ;
#40494=EDGE_LOOP ( 'NONE', ( #27137, #12705, #11792, #6058 ) ) ;
#40497=ORIENTED_EDGE ( 'NONE', *, *, #17835, .T. ) ;
#40502=ORIENTED_EDGE ( 'NONE', *, *, #30109, .F. ) ;
#40507=DIRECTION ( 'NONE',  ( -1.000000000000000000, 0.000000000000000000, -0.000000000000000000 ) ) ;
#40515=CARTESIAN_POINT ( 'NONE',  ( 15.00000000000000000, -18.13022148937263012, -15.02647892043543898 ) ) ;
#40518=ORIENTED_EDGE ( 'NONE', *, *, #33918, .T. ) ;
#40519=EDGE_CURVE ( 'NONE', #20542, #21097, #19819, .T. ) ;
#40521=AXIS2_PLACEMENT_3D ( 'NONE', #14362, #13402, #2857 ) ;
#40522=ADVANCED_FACE ( 'NONE', ( #27235 ), #23548, .T. ) ;
#40529=ORIENTED_EDGE ( 'NONE', *, *, #23272, .F. ) ;
#40533=DIRECTION ( 'NONE',  ( 0.000000000000000000, 0.000000000000000000, 1.000000000000000000 ) ) ;
#40541=LINE ( 'NONE', #7244, #25092 ) ;
#40543=EDGE_CURVE ( 'NONE', #35058, #29586, #8903, .T. ) ;
#40544=VERTEX_POINT ( 'NONE', #35780 ) ;
#40546=DIRECTION ( 'NONE',  ( 0.000000000000000000, -0.4067366430758009854, -0.9135454576426004225 ) ) ;
#40555=VECTOR ( 'NONE', #2309, 1000.000000000000000 ) ;
#40556=EDGE_CURVE ( 'NONE', #17607, #22223, #29241, .T. ) ;
#40557=DIRECTION ( 'NONE',  ( 0.000000000000000000, 0.000000000000000000, 1.000000000000000000 ) ) ;
#40558=DIRECTION ( 'NONE',  ( 0.000000000000000000, 0.2334453638559060851, -0.9723699203976764460 ) ) ;
#40560=ORIENTED_EDGE ( 'NONE', *, *, #24733, .F. ) ;
#40561=DIRECTION ( 'NONE',  ( 0.000000000000000000, 0.000000000000000000, 1.000000000000000000 ) ) ;
#40562=CARTESIAN_POINT ( 'NONE',  ( 11.99999999999999822, -74.65491531819111515, -8.830959090343204920 ) ) ;
#40564=CARTESIAN_POINT ( 'NONE',  ( 0.000000000000000000, -76.41127070299262414, -12.93880638057396304 ) ) ;
#40566=ADVANCED_FACE ( 'NONE', ( #8612 ), #20354, .T. ) ;
#40569=COLOUR_RGB ( '', 0.72549020, 0.75294118, 0.79215686) ;
#40570=DIRECTION ( 'NONE',  ( 0.000000000000000000, 0.4539904997395477482, -0.8910065241883674547 ) ) ;
#40572=CARTESIAN_POINT ( 'NONE',  ( 11.99999999999999822, 65.58780272294129077, -36.73666225445822420 ) ) ;
#40576=DIRECTION ( 'NONE',  ( 0.000000000000000000, 0.000000000000000000, 1.000000000000000000 ) ) ;
#40587=ORIENTED_EDGE ( 'NONE', *, *, #35912, .T. ) ;
#40590=CARTESIAN_POINT ( 'NONE',  ( 0.000000000000000000, 75.11725578898467859, 2.956366410620910656 ) ) ;
#40591=ADVANCED_FACE ( 'NONE', ( #17400 ), #13755, .T. ) ;
#40594=VERTEX_POINT ( 'NONE', #25474 ) ;
#40597=DIRECTION ( 'NONE',  ( -1.000000000000000000, -0.000000000000000000, 0.000000000000000000 ) ) ;
#40600=ORIENTED_EDGE ( 'NONE', *, *, #12240, .T. ) ;
#40601=ORIENTED_EDGE ( 'NONE', *, *, #14464, .F. ) ;
#40602=DIRECTION ( 'NONE',  ( -1.000000000000000000, 0.000000000000000000, 0.000000000000000000 ) ) ;
#40605=VERTEX_POINT ( 'NONE', #24991 ) ;
#40606=ORIENTED_EDGE ( 'NONE', *, *, #34034, .F. ) ;
#40607=FACE_OUTER_BOUND ( 'NONE', #9327, .T. ) ;
#40609=ADVANCED_FACE ( 'NONE', ( #6646 ), #36492, .F. ) ;
#40614=PLANE ( 'NONE',  #15741 ) ;
#40615=LINE ( 'NONE', #4148, #26130 ) ;
#40618=EDGE_CURVE ( 'NONE', #35941, #27912, #8633, .T. ) ;
#40619=ADVANCED_FACE ( 'NONE', ( #43839 ), #40425, .T. ) ;
#40621=FACE_OUTER_BOUND ( 'NONE', #30972, .T. ) ;
#40622=CARTESIAN_POINT ( 'NONE',  ( 11.99999999999999822, -78.73519480814938731, -22.90783923731713045 ) ) ;
#40632=CARTESIAN_POINT ( 'NONE',  ( 11.99999999999999822, 0.000000000000000000, 0.000000000000000000 ) ) ;
#40633=ORIENTED_EDGE ( 'NONE', *, *, #28410, .T. ) ;
#40637=CARTESIAN_POINT ( 'NONE',  ( 11.99999999999999822, -2.946379043146863719, 75.11764819372146462 ) ) ;
#40645=CIRCLE ( 'NONE', #22691, 82.00000000000000000 ) ;
#40646=CIRCLE ( 'NONE', #25795, 82.00000000000000000 ) ;
#40659=PLANE ( 'NONE',  #7527 ) ;
#40661=DIRECTION ( 'NONE',  ( -1.000000000000000000, -0.000000000000000000, 0.000000000000000000 ) ) ;
#40662=ORIENTED_EDGE ( 'NONE', *, *, #27290, .F. ) ;
#40672=DIRECTION ( 'NONE',  ( -1.000000000000000000, -0.000000000000000000, 0.000000000000000000 ) ) ;
#40675=CARTESIAN_POINT ( 'NONE',  ( 15.00000000000000000, -11.95096189432312350, 23.69967320028773372 ) ) ;
#40676=CARTESIAN_POINT ( 'NONE',  ( 11.99999999999999822, 0.000000000000000000, 0.000000000000000000 ) ) ;
#40683=LINE ( 'NONE', #7153, #30600 ) ;
#40685=CARTESIAN_POINT ( 'NONE',  ( 11.99999999999999822, 0.000000000000000000, 0.000000000000000000 ) ) ;
#40686=AXIS2_PLACEMENT_3D ( 'NONE', #42735, #20687, #24125 ) ;
#40690=LINE ( 'NONE', #18652, #25622 ) ;
#40693=ADVANCED_FACE ( 'NONE', ( #10300 ), #25218, .T. ) ;
#40698=CYLINDRICAL_SURFACE ( 'NONE', #26797, 77.49899999999999523 ) ;
#40700=FACE_OUTER_BOUND ( 'NONE', #13964, .T. ) ;
#40705=CARTESIAN_POINT ( 'NONE',  ( 11.99999999999999822, 59.46389618801966037, 49.70050353004911159 ) ) ;
#40708=LINE ( 'NONE', #26750, #37532 ) ;
#40709=DIRECTION ( 'NONE',  ( 0.000000000000000000, 0.6494480483301793283, 0.7604059656000345946 ) ) ;
#40719=CYLINDRICAL_SURFACE ( 'NONE', #28840, 31.99999999999998579 ) ;
#40723=VERTEX_POINT ( 'NONE', #23261 ) ;
#40725=( GEOMETRIC_REPRESENTATION_CONTEXT ( 3 ) GLOBAL_UNCERTAINTY_ASSIGNED_CONTEXT ( ( #30114 ) ) GLOBAL_UNIT_ASSIGNED_CONTEXT ( ( #4857, #34221, #27144 ) ) REPRESENTATION_CONTEXT ( 'NONE', 'WORKASPACE' ) );
#40727=VERTEX_POINT ( 'NONE', #19335 ) ;
#40730=DIRECTION ( 'NONE',  ( -1.000000000000000000, 0.000000000000000000, 0.000000000000000000 ) ) ;
#40737=CARTESIAN_POINT ( 'NONE',  ( 6.000000000000000000, 71.21200624218852226, -40.65526001592539984 ) ) ;
#40746=VECTOR ( 'NONE', #33573, 1000.000000000000000 ) ;
#40749=FACE_OUTER_BOUND ( 'NONE', #17175, .T. ) ;
#40755=ADVANCED_FACE ( 'NONE', ( #37701 ), #41383, .T. ) ;
#40756=CYLINDRICAL_SURFACE ( 'NONE', #17374, 31.99999999999998579 ) ;
#40758=ORIENTED_EDGE ( 'NONE', *, *, #30194, .F. ) ;
#40765=ORIENTED_EDGE ( 'NONE', *, *, #4161, .T. ) ;
#40776=ORIENTED_EDGE ( 'NONE', *, *, #7215, .F. ) ;
#40784=ORIENTED_EDGE ( 'NONE', *, *, #45215, .F. ) ;
#40788=AXIS2_PLACEMENT_3D ( 'NONE', #24059, #13046, #24998 ) ;
#40794=CIRCLE ( 'NONE', #20452, 31.99999999999998579 ) ;
#40795=CIRCLE ( 'NONE', #12644, 31.99999999999998934 ) ;
#40796=CARTESIAN_POINT ( 'NONE',  ( 0.000000000000000000, 77.32052557432841411, 5.256550761633121738 ) ) ;
#40800=ORIENTED_EDGE ( 'NONE', *, *, #47922, .T. ) ;
#40801=DIRECTION ( 'NONE',  ( -1.000000000000000000, 0.000000000000000000, 0.000000000000000000 ) ) ;
#40817=ORIENTED_EDGE ( 'NONE', *, *, #31623, .T. ) ;
#40818=ORIENTED_EDGE ( 'NONE', *, *, #24861, .T. ) ;
#40820=AXIS2_PLACEMENT_3D ( 'NONE', #27189, #41626, #15677 ) ;
#40822=ORIENTED_EDGE ( 'NONE', *, *, #12483, .T. ) ;
#40823=DIRECTION ( 'NONE',  ( 1.000000000000000000, 0.000000000000000000, 0.000000000000000000 ) ) ;
#40824=DIRECTION ( 'NONE',  ( -1.000000000000000000, 0.000000000000000000, 0.000000000000000000 ) ) ;
#40825=VERTEX_POINT ( 'NONE', #44803 ) ;
#40827=VECTOR ( 'NONE', #40507, 1000.000000000000000 ) ;
#40828=VERTEX_POINT ( 'NONE', #23017 ) ;
#40837=EDGE_LOOP ( 'NONE', ( #39482, #47776, #13617, #32464 ) ) ;
#40842=AXIS2_PLACEMENT_3D ( 'NONE', #19055, #38654, #20503 ) ;
#40843=EDGE_CURVE ( 'NONE', #29618, #39337, #42597, .T. ) ;
#40844=DIRECTION ( 'NONE',  ( 0.000000000000000000, 0.000000000000000000, 1.000000000000000000 ) ) ;
#40852=ORIENTED_EDGE ( 'NONE', *, *, #4912, .T. ) ;
#40856=VERTEX_POINT ( 'NONE', #43072 ) ;
#40860=CIRCLE ( 'NONE', #45527, 31.99999999999998579 ) ;
#40861=CARTESIAN_POINT ( 'NONE',  ( 11.99999999999999822, 26.01480285779933510, -70.53064760720289428 ) ) ;
#40862=CARTESIAN_POINT ( 'NONE',  ( 0.000000000000000000, -2.543863470248951320, 81.96053171279901051 ) ) ;
#40865=AXIS2_PLACEMENT_3D ( 'NONE', #1061, #16010, #8643 ) ;
#40868=DIRECTION ( 'NONE',  ( 0.000000000000000000, -0.5877852522924802425, 0.8090169943749422332 ) ) ;
#40874=ORIENTED_EDGE ( 'NONE', *, *, #13722, .F. ) ;
#40875=ORIENTED_EDGE ( 'NONE', *, *, #5360, .F. ) ;
#40880=VECTOR ( 'NONE', #30909, 1000.000000000000000 ) ;
#40881=FACE_OUTER_BOUND ( 'NONE', #15769, .T. ) ;
#40885=VERTEX_POINT ( 'NONE', #9288 ) ;
#40887=AXIS2_PLACEMENT_3D ( 'NONE', #28326, #33677, #33449 ) ;
#40891=ORIENTED_EDGE ( 'NONE', *, *, #12173, .T. ) ;
#40892=AXIS2_PLACEMENT_3D ( 'NONE', #12870, #31236, #8944 ) ;
#40896=DIRECTION ( 'NONE',  ( -1.000000000000000000, 0.000000000000000000, 0.000000000000000000 ) ) ;
#40899=EDGE_CURVE ( 'NONE', #27089, #44062, #1968, .T. ) ;
#40902=ORIENTED_EDGE ( 'NONE', *, *, #13487, .T. ) ;
#40905=CIRCLE ( 'NONE', #8900, 31.99999999999998579 ) ;
#40908=DIRECTION ( 'NONE',  ( -1.000000000000000000, -0.000000000000000000, 0.000000000000000000 ) ) ;
#40915=DIRECTION ( 'NONE',  ( 0.000000000000000000, 0.000000000000000000, -1.000000000000000000 ) ) ;
#40916=DIRECTION ( 'NONE',  ( 0.000000000000000000, 0.000000000000000000, 1.000000000000000000 ) ) ;
#40921=CARTESIAN_POINT ( 'NONE',  ( 0.000000000000000000, 0.000000000000000000, 0.000000000000000000 ) ) ;
#40926=CARTESIAN_POINT ( 'NONE',  ( 15.00000000000000000, -20.55727247249726020, 16.78983467731313084 ) ) ;
#40928=CARTESIAN_POINT ( 'NONE',  ( 12.00000000000000000, 23.49999999999999645, 1.499999999999995337 ) ) ;
#40931=ORIENTED_EDGE ( 'NONE', *, *, #31936, .F. ) ;
#40934=DIRECTION ( 'NONE',  ( 0.000000000000000000, -0.8660254037844363761, 0.5000000000000038858 ) ) ;
#40942=DIRECTION ( 'NONE',  ( 1.000000000000000000, -0.000000000000000000, -0.000000000000000000 ) ) ;
#40944=EDGE_CURVE ( 'NONE', #33903, #1311, #22719, .T. ) ;
#40948=AXIS2_PLACEMENT_3D ( 'NONE', #38716, #27686, #12516 ) ;
#40949=LINE ( 'NONE', #29681, #43228 ) ;
#40951=EDGE_CURVE ( 'NONE', #26872, #17933, #35478, .T. ) ;
#40953=CARTESIAN_POINT ( 'NONE',  ( 12.00000000000000000, -18.13022148937242761, 15.02647892043569122 ) ) ;
#40971=ORIENTED_EDGE ( 'NONE', *, *, #28242, .F. ) ;
#40975=FACE_OUTER_BOUND ( 'NONE', #2308, .T. ) ;
#40976=DIRECTION ( 'NONE',  ( 0.000000000000000000, 0.000000000000000000, 1.000000000000000000 ) ) ;
#40980=VECTOR ( 'NONE', #6208, 1000.000000000000000 ) ;
#40982=DIRECTION ( 'NONE',  ( -1.000000000000000000, 0.000000000000000000, 0.000000000000000000 ) ) ;
#40986=AXIS2_PLACEMENT_3D ( 'NONE', #33711, #40824, #45228 ) ;
#40987=CARTESIAN_POINT ( 'NONE',  ( 11.99999999999999822, 0.000000000000000000, 0.000000000000000000 ) ) ;
#40993=CARTESIAN_POINT ( 'NONE',  ( 6.000000000000000000, 76.69515212746016175, 29.01471420065590578 ) ) ;
#40994=LINE ( 'NONE', #48084, #5651 ) ;
#41003=CARTESIAN_POINT ( 'NONE',  ( 6.000000000000000000, -8.966570791700160470, -81.50828551894237251 ) ) ;
#41006=LINE ( 'NONE', #6980, #30033 ) ;
#41007=CARTESIAN_POINT ( 'NONE',  ( 11.99999999999999822, 2.956366410620650420, 75.11725578898469280 ) ) ;
#41009=CARTESIAN_POINT ( 'NONE',  ( 0.000000000000000000, 62.50329211542435104, 41.76937507738811917 ) ) ;
#41012=EDGE_CURVE ( 'NONE', #14039, #21975, #46209, .T. ) ;
#41015=EDGE_CURVE ( 'NONE', #11748, #15250, #10012, .T. ) ;
#41016=ORIENTED_EDGE ( 'NONE', *, *, #13925, .T. ) ;
#41022=CIRCLE ( 'NONE', #41709, 31.99999999999998934 ) ;
#41026=CIRCLE ( 'NONE', #19902, 77.49899999999999523 ) ;
#41031=DIRECTION ( 'NONE',  ( -1.000000000000000000, -0.000000000000000000, -0.000000000000000000 ) ) ;
#41039=DIRECTION ( 'NONE',  ( 0.000000000000000000, 0.000000000000000000, 1.000000000000000000 ) ) ;
#41043=ORIENTED_EDGE ( 'NONE', *, *, #34907, .F. ) ;
#41044=ORIENTED_EDGE ( 'NONE', *, *, #15154, .T. ) ;
#41047=CIRCLE ( 'NONE', #38712, 77.49899999999999523 ) ;
#41049=DIRECTION ( 'NONE',  ( 0.000000000000000000, 0.7604059656000322631, -0.6494480483301821039 ) ) ;
#41050=CARTESIAN_POINT ( 'NONE',  ( 0.000000000000000000, -51.02545421589285723, -55.20638768913812555 ) ) ;
#41054=DIRECTION ( 'NONE',  ( 0.000000000000000000, -6.982962677686266711E-15, 1.000000000000000000 ) ) ;
#41056=CARTESIAN_POINT ( 'NONE',  ( 0.000000000000000000, 46.53671651294032330, -59.03961581697353012 ) ) ;
#41066=DIRECTION ( 'NONE',  ( 0.000000000000000000, 0.9238795325112877377, -0.3826834323650873948 ) ) ;
#41069=DIRECTION ( 'NONE',  ( 0.000000000000000000, 0.000000000000000000, 1.000000000000000000 ) ) ;
#41073=DIRECTION ( 'NONE',  ( 0.000000000000000000, 0.000000000000000000, 1.000000000000000000 ) ) ;
#41075=EDGE_LOOP ( 'NONE', ( #42794, #517, #24157, #9687 ) ) ;
#41081=ORIENTED_EDGE ( 'NONE', *, *, #17097, .F. ) ;
#41083=EDGE_LOOP ( 'NONE', ( #34330, #15161 ) ) ;
#41089=AXIS2_PLACEMENT_3D ( 'NONE', #32598, #17900, #32825 ) ;
#41092=AXIS2_PLACEMENT_3D ( 'NONE', #3536, #7691, #33400 ) ;
#41094=VECTOR ( 'NONE', #47109, 1000.000000000000000 ) ;
#41096=DIRECTION ( 'NONE',  ( -0.000000000000000000, -0.6691306063588570163, 0.7431448254773953543 ) ) ;
#41099=ORIENTED_EDGE ( 'NONE', *, *, #32063, .F. ) ;
#41104=DIRECTION ( 'NONE',  ( -1.000000000000000000, 0.000000000000000000, 0.000000000000000000 ) ) ;
#41105=CYLINDRICAL_SURFACE ( 'NONE', #40099, 31.99999999999998579 ) ;
#41114=EDGE_LOOP ( 'NONE', ( #16275, #19982, #23730, #33304 ) ) ;
#41117=LINE ( 'NONE', #11730, #24333 ) ;
#41119=DIRECTION ( 'NONE',  ( 0.000000000000000000, -0.8526401643540970632, 0.5224985647159410274 ) ) ;
#41124=DIRECTION ( 'NONE',  ( -1.000000000000000000, 0.000000000000000000, -0.000000000000000000 ) ) ;
#41131=CIRCLE ( 'NONE', #47343, 77.49900000000002365 ) ;
#41138=EDGE_CURVE ( 'NONE', #21018, #15597, #21743, .T. ) ;
#41140=CIRCLE ( 'NONE', #47390, 82.00000000000000000 ) ;
#41142=ORIENTED_EDGE ( 'NONE', *, *, #11218, .T. ) ;
#41144=DIRECTION ( 'NONE',  ( -1.000000000000000000, 0.000000000000000000, 0.000000000000000000 ) ) ;
#41146=EDGE_CURVE ( 'NONE', #18512, #16815, #31381, .T. ) ;
#41147=ORIENTED_EDGE ( 'NONE', *, *, #31764, .T. ) ;
#41151=VECTOR ( 'NONE', #15861, 1000.000000000000000 ) ;
#41158=CIRCLE ( 'NONE', #5206, 31.99999999999998934 ) ;
#41159=DIRECTION ( 'NONE',  ( -1.000000000000000000, 0.000000000000000000, 0.000000000000000000 ) ) ;
#41160=DIRECTION ( 'NONE',  ( 0.000000000000000000, 0.5224985647159500202, -0.8526401643540915121 ) ) ;
#41167=ORIENTED_EDGE ( 'NONE', *, *, #33079, .T. ) ;
#41173=ORIENTED_EDGE ( 'NONE', *, *, #13214, .T. ) ;
#41174=CARTESIAN_POINT ( 'NONE',  ( 11.99999999999999822, 66.50666863322000211, 39.78640506895628448 ) ) ;
#41181=VECTOR ( 'NONE', #33463, 1000.000000000000000 ) ;
#41201=ORIENTED_EDGE ( 'NONE', *, *, #9850, .F. ) ;
#41202=CARTESIAN_POINT ( 'NONE',  ( 12.00000000000000000, 22.07842321921480888, -8.187992925817425771 ) ) ;
#41210=CARTESIAN_POINT ( 'NONE',  ( 0.000000000000000000, 0.000000000000000000, 0.000000000000000000 ) ) ;
#41213=ORIENTED_EDGE ( 'NONE', *, *, #20793, .F. ) ;
#41215=FACE_OUTER_BOUND ( 'NONE', #28633, .T. ) ;
#41220=ORIENTED_EDGE ( 'NONE', *, *, #35938, .F. ) ;
#41228=VECTOR ( 'NONE', #2169, 1000.000000000000000 ) ;
#41234=EDGE_CURVE ( 'NONE', #45891, #22916, #11021, .T. ) ;
#41236=DIRECTION ( 'NONE',  ( -1.000000000000000000, 0.000000000000000000, 0.000000000000000000 ) ) ;
#41237=DIRECTION ( 'NONE',  ( -0.000000000000000000, 0.8090169943749426773, -0.5877852522924796874 ) ) ;
#41241=CYLINDRICAL_SURFACE ( 'NONE', #23216, 82.00000000000000000 ) ;
#41243=DIRECTION ( 'NONE',  ( -1.000000000000000000, 0.000000000000000000, -0.000000000000000000 ) ) ;
#41245=EDGE_CURVE ( 'NONE', #40727, #44946, #18031, .T. ) ;
#41248=DIRECTION ( 'NONE',  ( -1.000000000000000000, -0.000000000000000000, -0.000000000000000000 ) ) ;
#41252=DIRECTION ( 'NONE',  ( -1.000000000000000000, 0.000000000000000000, 0.000000000000000000 ) ) ;
#41257=ORIENTED_EDGE ( 'NONE', *, *, #45642, .T. ) ;
#41260=CIRCLE ( 'NONE', #22522, 31.99999999999998224 ) ;
#41265=CARTESIAN_POINT ( 'NONE',  ( 15.00000000000000000, -22.67460108101782978, -6.353146135317906840 ) ) ;
#41269=ORIENTED_EDGE ( 'NONE', *, *, #30510, .F. ) ;
#41271=VERTEX_POINT ( 'NONE', #33966 ) ;
#41273=LINE ( 'NONE', #22656, #25117 ) ;
#41274=AXIS2_PLACEMENT_3D ( 'NONE', #30745, #8222, #23153 ) ;
#41275=DIRECTION ( 'NONE',  ( -1.000000000000000000, -0.000000000000000000, -0.000000000000000000 ) ) ;
#41276=ORIENTED_EDGE ( 'NONE', *, *, #24319, .F. ) ;
#41278=VERTEX_POINT ( 'NONE', #48181 ) ;
#41279=DIRECTION ( 'NONE',  ( -1.000000000000000000, -0.000000000000000000, -0.000000000000000000 ) ) ;
#41281=FACE_OUTER_BOUND ( 'NONE', #39353, .T. ) ;
#41282=EDGE_CURVE ( 'NONE', #26682, #36257, #36790, .T. ) ;
#41288=EDGE_CURVE ( 'NONE', #31890, #7607, #13369, .T. ) ;
#41289=LINE ( 'NONE', #7744, #9235 ) ;
#41290=VERTEX_POINT ( 'NONE', #41569 ) ;
#41291=DIRECTION ( 'NONE',  ( 0.000000000000000000, -0.8090169943749530024, 0.5877852522924653655 ) ) ;
#41295=VECTOR ( 'NONE', #9534, 1000.000000000000000 ) ;
#41302=CIRCLE ( 'NONE', #25626, 82.00000000000000000 ) ;
#41304=CARTESIAN_POINT ( 'NONE',  ( 0.000000000000000000, 0.000000000000000000, 0.000000000000000000 ) ) ;
#41312=ORIENTED_EDGE ( 'NONE', *, *, #14530, .F. ) ;
#41319=VERTEX_POINT ( 'NONE', #12434 ) ;
#41324=ORIENTED_EDGE ( 'NONE', *, *, #4809, .F. ) ;
#41328=DIRECTION ( 'NONE',  ( 0.000000000000000000, 0.000000000000000000, 1.000000000000000000 ) ) ;
#41333=CARTESIAN_POINT ( 'NONE',  ( 0.000000000000000000, -55.16347631942998220, -60.67117009219196433 ) ) ;
#41334=ORIENTED_EDGE ( 'NONE', *, *, #31623, .F. ) ;
#41338=ADVANCED_FACE ( 'NONE', ( #1652 ), #31783, .F. ) ;
#41339=DIRECTION ( 'NONE',  ( 0.000000000000000000, 0.000000000000000000, 1.000000000000000000 ) ) ;
#41342=ORIENTED_EDGE ( 'NONE', *, *, #25275, .T. ) ;
#41343=EDGE_CURVE ( 'NONE', #33371, #20366, #1419, .T. ) ;
#41355=DIRECTION ( 'NONE',  ( -1.000000000000000000, 0.000000000000000000, 0.000000000000000000 ) ) ;
#41356=CARTESIAN_POINT ( 'NONE',  ( 11.99999999999999822, 0.000000000000000000, 0.000000000000000000 ) ) ;
#41365=LINE ( 'NONE', #37679, #18359 ) ;
#41371=DIRECTION ( 'NONE',  ( 1.000000000000000000, 0.000000000000000000, 0.000000000000000000 ) ) ;
#41372=AXIS2_PLACEMENT_3D ( 'NONE', #2618, #13418, #2388 ) ;
#41373=LINE ( 'NONE', #11745, #29038 ) ;
#41377=DIRECTION ( 'NONE',  ( -1.000000000000000000, 0.000000000000000000, 0.000000000000000000 ) ) ;
#41380=ORIENTED_EDGE ( 'NONE', *, *, #3062, .T. ) ;
#41381=VERTEX_POINT ( 'NONE', #42536 ) ;
#41383=CYLINDRICAL_SURFACE ( 'NONE', #26614, 31.99999999999998579 ) ;
#41384=VECTOR ( 'NONE', #29999, 1000.000000000000000 ) ;
#41386=ORIENTED_EDGE ( 'NONE', *, *, #28749, .F. ) ;
#41389=ORIENTED_EDGE ( 'NONE', *, *, #39947, .T. ) ;
#41393=DIRECTION ( 'NONE',  ( 0.000000000000000000, 0.000000000000000000, -1.000000000000000000 ) ) ;
#41395=DIRECTION ( 'NONE',  ( -1.000000000000000000, 0.000000000000000000, 0.000000000000000000 ) ) ;
#41396=CARTESIAN_POINT ( 'NONE',  ( 15.00000000000000000, -3.948201729842032215, 23.21447184625297666 ) ) ;
#41400=ORIENTED_EDGE ( 'NONE', *, *, #12599, .T. ) ;
#41401=CARTESIAN_POINT ( 'NONE',  ( 11.99999999999999822, -39.78640506895651896, 66.50666863321988842 ) ) ;
#41404=ADVANCED_FACE ( 'NONE', ( #8743 ), #34685, .T. ) ;
#41408=EDGE_CURVE ( 'NONE', #48128, #17814, #26679, .T. ) ;
#41410=CARTESIAN_POINT ( 'NONE',  ( 11.99999999999999822, 68.55367621811204515, -44.99326035065983120 ) ) ;
#41418=CYLINDRICAL_SURFACE ( 'NONE', #38549, 31.99999999999998579 ) ;
#41419=CARTESIAN_POINT ( 'NONE',  ( 12.00000000000000000, 20.85821328998756385, 10.92862929874494249 ) ) ;
#41420=DIRECTION ( 'NONE',  ( -1.000000000000000000, 0.000000000000000000, 0.000000000000000000 ) ) ;
#41423=ORIENTED_EDGE ( 'NONE', *, *, #28463, .F. ) ;
#41439=PLANE ( 'NONE',  #19065 ) ;
#41443=VERTEX_POINT ( 'NONE', #23202 ) ;
#41447=CARTESIAN_POINT ( 'NONE',  ( -10.00000000000000000, 0.000000000000000000, 0.000000000000000000 ) ) ;
#41448=CARTESIAN_POINT ( 'NONE',  ( 15.00000000000000000, 16.61724383029390140, 20.69703378468902955 ) ) ;
#41449=FACE_OUTER_BOUND ( 'NONE', #17658, .T. ) ;
#41451=DIRECTION ( 'NONE',  ( 0.000000000000000000, -0.3090169943749549453, 0.9510565162951511997 ) ) ;
#41455=ORIENTED_EDGE ( 'NONE', *, *, #2709, .T. ) ;
#41471=CARTESIAN_POINT ( 'NONE',  ( 0.000000000000000000, 0.000000000000000000, 0.000000000000000000 ) ) ;
#41474=DIRECTION ( 'NONE',  ( 0.000000000000000000, -0.5877852522924708056, 0.8090169943749490056 ) ) ;
#41477=CYLINDRICAL_SURFACE ( 'NONE', #22827, 31.99999999999998579 ) ;
#41484=DIRECTION ( 'NONE',  ( -1.000000000000000000, 0.000000000000000000, 0.000000000000000000 ) ) ;
#41485=EDGE_LOOP ( 'NONE', ( #44278, #36791, #15075, #5697 ) ) ;
#41489=CIRCLE ( 'NONE', #47718, 31.99999999999998934 ) ;
#41491=EDGE_CURVE ( 'NONE', #2023, #2304, #25360, .T. ) ;
#41492=DIRECTION ( 'NONE',  ( 0.000000000000000000, -0.9781476007338067991, -0.2079116908177533196 ) ) ;
#41493=VERTEX_POINT ( 'NONE', #36617 ) ;
#41496=VECTOR ( 'NONE', #27992, 1000.000000000000000 ) ;
#41498=AXIS2_PLACEMENT_3D ( 'NONE', #29588, #13940, #37175 ) ;
#41500=DIRECTION ( 'NONE',  ( -1.000000000000000000, 0.000000000000000000, 0.000000000000000000 ) ) ;
#41505=ORIENTED_EDGE ( 'NONE', *, *, #46739, .F. ) ;
#41508=DIRECTION ( 'NONE',  ( 0.000000000000000000, 0.000000000000000000, 1.000000000000000000 ) ) ;
#41510=PLANE ( 'NONE',  #22829 ) ;
#41520=CARTESIAN_POINT ( 'NONE',  ( 11.99999999999999822, 0.000000000000000000, 0.000000000000000000 ) ) ;
#41525=DIRECTION ( 'NONE',  ( 0.000000000000000000, 0.000000000000000000, 1.000000000000000000 ) ) ;
#41528=DIRECTION ( 'NONE',  ( 0.000000000000000000, -0.3090169943749350168, -0.9510565162951576390 ) ) ;
#41530=EDGE_LOOP ( 'NONE', ( #8863, #34815, #21802, #11773 ) ) ;
#41534=VECTOR ( 'NONE', #2597, 1000.000000000000114 ) ;
#41538=AXIS2_PLACEMENT_3D ( 'NONE', #43084, #14181, #9533 ) ;
#41540=DIRECTION ( 'NONE',  ( 0.000000000000000000, 0.000000000000000000, 1.000000000000000000 ) ) ;
#41543=LINE ( 'NONE', #19006, #18577 ) ;
#41548=EDGE_CURVE ( 'NONE', #10384, #15864, #30585, .T. ) ;
#41552=DIRECTION ( 'NONE',  ( 0.000000000000000000, 0.000000000000000000, 1.000000000000000000 ) ) ;
#41558=CIRCLE ( 'NONE', #40031, 31.99999999999998579 ) ;
#41561=VECTOR ( 'NONE', #12872, 999.9999999999998863 ) ;
#41565=EDGE_CURVE ( 'NONE', #43990, #8879, #47163, .T. ) ;
#41569=CARTESIAN_POINT ( 'NONE',  ( 11.99999999999999822, 15.33399622253482342, 80.55351364060595643 ) ) ;
#41580=ORIENTED_EDGE ( 'NONE', *, *, #31711, .F. ) ;
#41581=ADVANCED_FACE ( 'NONE', ( #7002 ), #44942, .T. ) ;
#41586=ORIENTED_EDGE ( 'NONE', *, *, #44100, .T. ) ;
#41589=CARTESIAN_POINT ( 'NONE',  ( 11.99999999999999822, -8.840884882375609877, 74.65374052328647281 ) ) ;
#41590=DIRECTION ( 'NONE',  ( 1.000000000000000000, 0.000000000000000000, -0.000000000000000000 ) ) ;
#41594=CIRCLE ( 'NONE', #32985, 77.49900000000000944 ) ;
#41602=ORIENTED_EDGE ( 'NONE', *, *, #28932, .F. ) ;
#41603=CARTESIAN_POINT ( 'NONE',  ( 11.99999999999999822, 46.54456581323805153, 59.03342792756280488 ) ) ;
#41607=EDGE_CURVE ( 'NONE', #30536, #923, #33666, .T. ) ;
#41611=EDGE_CURVE ( 'NONE', #37953, #2290, #45184, .T. ) ;
#41612=ADVANCED_FACE ( 'NONE', ( #10923 ), #41510, .F. ) ;
#41614=VERTEX_POINT ( 'NONE', #37833 ) ;
#41617=AXIS2_PLACEMENT_3D ( 'NONE', #18881, #3230, #26253 ) ;
#41621=ORIENTED_EDGE ( 'NONE', *, *, #45687, .F. ) ;
#41623=AXIS2_PLACEMENT_3D ( 'NONE', #45736, #5345, #20495 ) ;
#41626=DIRECTION ( 'NONE',  ( -1.000000000000000000, 0.000000000000000000, 0.000000000000000000 ) ) ;
#41631=ADVANCED_FACE ( 'NONE', ( #22897 ), #14843, .T. ) ;
#41633=ORIENTED_EDGE ( 'NONE', *, *, #16357, .F. ) ;
#41634=VECTOR ( 'NONE', #42974, 1000.000000000000000 ) ;
#41639=DIRECTION ( 'NONE',  ( 0.000000000000000000, 0.000000000000000000, 1.000000000000000000 ) ) ;
#41642=DIRECTION ( 'NONE',  ( -1.000000000000000000, 0.000000000000000000, 0.000000000000000000 ) ) ;
#41644=CARTESIAN_POINT ( 'NONE',  ( 15.00000000000000000, 23.59884966291521380, -12.14883922797262805 ) ) ;
#41654=CARTESIAN_POINT ( 'NONE',  ( 0.000000000000000000, -8.830959090341869100, -74.65491531819127147 ) ) ;
#41656=DIRECTION ( 'NONE',  ( 0.000000000000000000, 0.000000000000000000, 1.000000000000000000 ) ) ;
#41658=EDGE_CURVE ( 'NONE', #15777, #2920, #138, .T. ) ;
#41663=VERTEX_POINT ( 'NONE', #17170 ) ;
#41664=EDGE_CURVE ( 'NONE', #16116, #2031, #7936, .T. ) ;
#41666=VECTOR ( 'NONE', #19759, 999.9999999999998863 ) ;
#41676=VECTOR ( 'NONE', #1079, 1000.000000000000000 ) ;
#41677=DIRECTION ( 'NONE',  ( -1.000000000000000000, 0.000000000000000000, 0.000000000000000000 ) ) ;
#41678=ORIENTED_EDGE ( 'NONE', *, *, #8373, .F. ) ;
#41683=VERTEX_POINT ( 'NONE', #5946 ) ;
#41687=DIRECTION ( 'NONE',  ( 0.000000000000000000, -0.9945218953682742891, -0.1045284632676449360 ) ) ;
#41689=DIRECTION ( 'NONE',  ( -1.000000000000000000, 0.000000000000000000, 0.000000000000000000 ) ) ;
#41695=DIRECTION ( 'NONE',  ( 0.000000000000000000, 0.000000000000000000, 1.000000000000000000 ) ) ;
#41703=DIRECTION ( 'NONE',  ( 0.000000000000000000, 0.1564344650402244852, 0.9876883405951387696 ) ) ;
#41705=CARTESIAN_POINT ( 'NONE',  ( 0.000000000000000000, -46.53671651293991118, 59.03961581697383565 ) ) ;
#41707=DIRECTION ( 'NONE',  ( 0.000000000000000000, 0.000000000000000000, -1.000000000000000000 ) ) ;
#41709=AXIS2_PLACEMENT_3D ( 'NONE', #27233, #30421, #46074 ) ;
#41710=VECTOR ( 'NONE', #15768, 999.9999999999998863 ) ;
#41718=AXIS2_PLACEMENT_3D ( 'NONE', #16280, #46133, #12850 ) ;
#41720=CYLINDRICAL_SURFACE ( 'NONE', #42781, 31.99999999999998579 ) ;
#41722=DIRECTION ( 'NONE',  ( -1.000000000000000000, -0.000000000000000000, -0.000000000000000000 ) ) ;
#41724=ADVANCED_FACE ( 'NONE', ( #31902 ), #43137, .T. ) ;
#41731=ORIENTED_EDGE ( 'NONE', *, *, #8069, .T. ) ;
#41740=VECTOR ( 'NONE', #40896, 1000.000000000000000 ) ;
#41741=AXIS2_PLACEMENT_3D ( 'NONE', #35580, #39747, #6442 ) ;
#41743=AXIS2_PLACEMENT_3D ( 'NONE', #48434, #30096, #45023 ) ;
#41744=DIRECTION ( 'NONE',  ( -1.000000000000000000, 0.000000000000000000, -0.000000000000000000 ) ) ;
#41745=AXIS2_PLACEMENT_3D ( 'NONE', #46070, #12538, #27473 ) ;
#41747=DIRECTION ( 'NONE',  ( 0.000000000000000000, 0.000000000000000000, 1.000000000000000000 ) ) ;
#41748=ORIENTED_EDGE ( 'NONE', *, *, #3075, .T. ) ;
#41750=VERTEX_POINT ( 'NONE', #16708 ) ;
#41751=ORIENTED_EDGE ( 'NONE', *, *, #22758, .F. ) ;
#41753=DIRECTION ( 'NONE',  ( 0.000000000000000000, 0.000000000000000000, 1.000000000000000000 ) ) ;
#41766=FACE_OUTER_BOUND ( 'NONE', #15208, .T. ) ;
#41767=CARTESIAN_POINT ( 'NONE',  ( 15.00000000000000000, 16.61724383029390140, 20.69703378468902955 ) ) ;
#41770=AXIS2_PLACEMENT_3D ( 'NONE', #13948, #2676, #6850 ) ;
#41771=CARTESIAN_POINT ( 'NONE',  ( 11.99999999999999822, 0.000000000000000000, 0.000000000000000000 ) ) ;
#41772=ADVANCED_FACE ( 'NONE', ( #31658 ), #20132, .T. ) ;
#41773=VERTEX_POINT ( 'NONE', #42663 ) ;
#41775=FACE_OUTER_BOUND ( 'NONE', #17531, .T. ) ;
#41777=EDGE_CURVE ( 'NONE', #44508, #11246, #46281, .T. ) ;
#41778=CARTESIAN_POINT ( 'NONE',  ( 11.99999999999999822, 0.000000000000000000, 0.000000000000000000 ) ) ;
#41782=EDGE_CURVE ( 'NONE', #4110, #15076, #44569, .T. ) ;
#41784=DIRECTION ( 'NONE',  ( -1.000000000000000000, 0.000000000000000000, -0.000000000000000000 ) ) ;
#41785=ORIENTED_EDGE ( 'NONE', *, *, #39174, .F. ) ;
#41787=CIRCLE ( 'NONE', #12849, 31.99999999999999289 ) ;
#41791=VERTEX_POINT ( 'NONE', #47741 ) ;
#41797=EDGE_CURVE ( 'NONE', #29191, #44743, #22013, .T. ) ;
#41800=EDGE_LOOP ( 'NONE', ( #46742, #7434, #43563, #30367 ) ) ;
#41804=CYLINDRICAL_SURFACE ( 'NONE', #40986, 31.99999999999998579 ) ;
#41805=ORIENTED_EDGE ( 'NONE', *, *, #12341, .F. ) ;
#41807=DIRECTION ( 'NONE',  ( 0.000000000000000000, 0.000000000000000000, 1.000000000000000000 ) ) ;
#41812=CARTESIAN_POINT ( 'NONE',  ( 11.99999999999999822, 62.50884508063487033, -41.76106447765422303 ) ) ;
#41816=ORIENTED_EDGE ( 'NONE', *, *, #42506, .T. ) ;
#41827=ORIENTED_EDGE ( 'NONE', *, *, #28651, .F. ) ;
#41829=CARTESIAN_POINT ( 'NONE',  ( 11.99999999999999822, 77.32052557432849937, -5.256550761632002633 ) ) ;
#41841=DIRECTION ( 'NONE',  ( -1.000000000000000000, -0.000000000000000000, 0.000000000000000000 ) ) ;
#41845=CARTESIAN_POINT ( 'NONE',  ( 11.99999999999999822, 55.16347631943042984, 60.67117009219156643 ) ) ;
#41846=DIRECTION ( 'NONE',  ( -1.000000000000000000, 0.000000000000000000, -0.000000000000000000 ) ) ;
#41847=EDGE_LOOP ( 'NONE', ( #2468, #26526, #1662, #7418 ) ) ;
#41849=DIRECTION ( 'NONE',  ( -1.000000000000000000, 0.000000000000000000, 0.000000000000000000 ) ) ;
#41851=( LENGTH_UNIT ( ) NAMED_UNIT ( * ) SI_UNIT ( .MILLI., .METRE. ) );
#41856=ORIENTED_EDGE ( 'NONE', *, *, #46752, .F. ) ;
#41857=CIRCLE ( 'NONE', #33244, 82.00000000000000000 ) ;
#41861=VECTOR ( 'NONE', #30507, 1000.000000000000000 ) ;
#41862=LINE ( 'NONE', #27168, #35458 ) ;
#41863=FACE_OUTER_BOUND ( 'NONE', #37522, .T. ) ;
#41864=AXIS2_PLACEMENT_3D ( 'NONE', #19456, #12157, #860 ) ;
#41866=AXIS2_PLACEMENT_3D ( 'NONE', #1974, #13456, #46759 ) ;
#41872=AXIS2_PLACEMENT_3D ( 'NONE', #5507, #1841, #46872 ) ;
#41883=CARTESIAN_POINT ( 'NONE',  ( 11.99999999999999822, -11.30684508768284680, -76.66974797899850103 ) ) ;
#41884=EDGE_LOOP ( 'NONE', ( #8676, #41081, #12398, #7649 ) ) ;
#41885=CARTESIAN_POINT ( 'NONE',  ( 11.99999999999999822, -80.55351364060599906, 15.33399622253457295 ) ) ;
#41886=VERTEX_POINT ( 'NONE', #2963 ) ;
#41893=ORIENTED_EDGE ( 'NONE', *, *, #14475, .T. ) ;
#41895=LINE ( 'NONE', #8103, #6741 ) ;
#41898=CARTESIAN_POINT ( 'NONE',  ( 0.000000000000000000, 74.74816331893477184, -33.71516098798660011 ) ) ;
#41910=ADVANCED_FACE ( 'NONE', ( #43845 ), #17892, .T. ) ;
#41911=CARTESIAN_POINT ( 'NONE',  ( 15.00000000000000000, -10.45096189432344502, -21.10159698893425784 ) ) ;
#41913=ORIENTED_EDGE ( 'NONE', *, *, #26306, .T. ) ;
#41917=LINE ( 'NONE', #27702, #11566 ) ;
#41920=ORIENTED_EDGE ( 'NONE', *, *, #32542, .F. ) ;
#41921=EDGE_CURVE ( 'NONE', #24099, #1474, #7170, .T. ) ;
#41922=EDGE_LOOP ( 'NONE', ( #15021, #13335, #3417, #2132 ) ) ;
#41924=ORIENTED_EDGE ( 'NONE', *, *, #29689, .F. ) ;
#41929=AXIS2_PLACEMENT_3D ( 'NONE', #42981, #9429, #6260 ) ;
#41930=ORIENTED_EDGE ( 'NONE', *, *, #7394, .F. ) ;
#41931=EDGE_CURVE ( 'NONE', #33596, #24133, #41558, .T. ) ;
#41935=VERTEX_POINT ( 'NONE', #34503 ) ;
#41937=CARTESIAN_POINT ( 'NONE',  ( 15.00000000000000000, 0.000000000000000000, 0.000000000000000000 ) ) ;
#41939=DIRECTION ( 'NONE',  ( -1.000000000000000000, 0.000000000000000000, 0.000000000000000000 ) ) ;
#41945=VECTOR ( 'NONE', #48440, 1000.000000000000114 ) ;
#41948=ORIENTED_EDGE ( 'NONE', *, *, #40556, .T. ) ;
#41951=ORIENTED_EDGE ( 'NONE', *, *, #20906, .F. ) ;
#41952=EDGE_CURVE ( 'NONE', #35782, #39822, #25156, .T. ) ;
#41957=CARTESIAN_POINT ( 'NONE',  ( 11.99999999999999822, -10.30890764327323872, -81.34940948281347062 ) ) ;
#41960=CARTESIAN_POINT ( 'NONE',  ( 11.99999999999999822, 0.000000000000000000, 0.000000000000000000 ) ) ;
#41962=EDGE_CURVE ( 'NONE', #25331, #6202, #20447, .T. ) ;
#41965=CARTESIAN_POINT ( 'NONE',  ( 0.000000000000000000, 0.000000000000000000, 0.000000000000000000 ) ) ;
#41966=AXIS2_PLACEMENT_3D ( 'NONE', #28038, #16529, #24836 ) ;
#41967=LINE ( 'NONE', #12346, #44205 ) ;
#41976=PLANE ( 'NONE',  #29527 ) ;
#41978=ORIENTED_EDGE ( 'NONE', *, *, #25294, .F. ) ;
#41985=ORIENTED_EDGE ( 'NONE', *, *, #14130, .F. ) ;
#41986=ORIENTED_EDGE ( 'NONE', *, *, #14321, .T. ) ;
#41988=ORIENTED_EDGE ( 'NONE', *, *, #1441, .T. ) ;
#41991=DIRECTION ( 'NONE',  ( -1.000000000000000000, -0.000000000000000000, 0.000000000000000000 ) ) ;
#41992=CARTESIAN_POINT ( 'NONE',  ( 11.99999999999999822, 46.53671651294032330, -59.03961581697353012 ) ) ;
#41997=ORIENTED_EDGE ( 'NONE', *, *, #4905, .F. ) ;
#41999=DIRECTION ( 'NONE',  ( 0.000000000000000000, -0.5224985647159380298, -0.8526401643540988395 ) ) ;
#42006=DIRECTION ( 'NONE',  ( 1.000000000000000000, 0.000000000000000000, 0.000000000000000000 ) ) ;
#42007=DIRECTION ( 'NONE',  ( -1.000000000000000000, 0.000000000000000000, 0.000000000000000000 ) ) ;
#42010=LINE ( 'NONE', #23388, #12639 ) ;
#42015=DIRECTION ( 'NONE',  ( -1.000000000000000000, 0.000000000000000000, -0.000000000000000000 ) ) ;
#42017=AXIS2_PLACEMENT_3D ( 'NONE', #25324, #40285, #14323 ) ;
#42018=CARTESIAN_POINT ( 'NONE',  ( 11.99999999999999822, 55.20638768913831029, -51.02545421589267960 ) ) ;
#42029=AXIS2_PLACEMENT_3D ( 'NONE', #46819, #35067, #47055 ) ;
#42031=DIRECTION ( 'NONE',  ( 0.000000000000000000, -0.9723699203976789995, 0.2334453638558957322 ) ) ;
#42032=CARTESIAN_POINT ( 'NONE',  ( 11.99999999999999822, -18.89407956138204980, -75.16055320797050854 ) ) ;
#42038=EDGE_LOOP ( 'NONE', ( #40067, #1572, #32371, #17507 ) ) ;
#42039=DIRECTION ( 'NONE',  ( 0.000000000000000000, -0.1045284632676558301, -0.9945218953682731788 ) ) ;
#42043=ADVANCED_FACE ( 'NONE', ( #34032 ), #14959, .T. ) ;
#42047=ORIENTED_EDGE ( 'NONE', *, *, #37382, .T. ) ;
#42048=VERTEX_POINT ( 'NONE', #41883 ) ;
#42050=CARTESIAN_POINT ( 'NONE',  ( 0.000000000000000000, 0.000000000000000000, 0.000000000000000000 ) ) ;
#42051=CARTESIAN_POINT ( 'NONE',  ( 11.99999999999999822, -41.76937507738831812, 62.50329211542423025 ) ) ;
#42056=ORIENTED_EDGE ( 'NONE', *, *, #34471, .F. ) ;
#42061=CIRCLE ( 'NONE', #5311, 31.99999999999998224 ) ;
#42068=ORIENTED_EDGE ( 'NONE', *, *, #34867, .F. ) ;
#42074=LINE ( 'NONE', #5845, #46522 ) ;
#42076=FACE_OUTER_BOUND ( 'NONE', #25440, .T. ) ;
#42079=AXIS2_PLACEMENT_3D ( 'NONE', #4160, #11741, #22994 ) ;
#42082=CARTESIAN_POINT ( 'NONE',  ( 12.00000000000000000, 8.688484142254226938, 21.88630264137359305 ) ) ;
#42087=EDGE_LOOP ( 'NONE', ( #16158, #1365, #4264, #15515 ) ) ;
#42097=ORIENTED_EDGE ( 'NONE', *, *, #4100, .F. ) ;
#42098=EDGE_CURVE ( 'NONE', #488, #12997, #15807, .T. ) ;
#42104=VECTOR ( 'NONE', #40942, 1000.000000000000000 ) ;
#42108=ORIENTED_EDGE ( 'NONE', *, *, #22162, .T. ) ;
#42109=CARTESIAN_POINT ( 'NONE',  ( 11.99999999999999822, 77.49459641780886443, -0.8261519478433960728 ) ) ;
#42110=ORIENTED_EDGE ( 'NONE', *, *, #22026, .F. ) ;
#42112=DIRECTION ( 'NONE',  ( 0.000000000000000000, 0.8910065241883690090, -0.4539904997395446395 ) ) ;
#42113=ORIENTED_EDGE ( 'NONE', *, *, #6957, .F. ) ;
#42116=EDGE_CURVE ( 'NONE', #16392, #1080, #18122, .T. ) ;
#42120=VERTEX_POINT ( 'NONE', #1480 ) ;
#42121=CARTESIAN_POINT ( 'NONE',  ( 0.000000000000000000, 0.000000000000000000, 0.000000000000000000 ) ) ;
#42122=ORIENTED_EDGE ( 'NONE', *, *, #19217, .F. ) ;
#42125=FACE_OUTER_BOUND ( 'NONE', #28246, .T. ) ;
#42126=CARTESIAN_POINT ( 'NONE',  ( 11.99999999999999822, 46.54456581323888997, -59.03342792756214408 ) ) ;
#42132=CARTESIAN_POINT ( 'NONE',  ( 11.99999999999999822, 75.11764819372149304, 29.05362095685338275 ) ) ;
#42134=EDGE_CURVE ( 'NONE', #37030, #28298, #11132, .T. ) ;
#42137=CARTESIAN_POINT ( 'NONE',  ( 11.99999999999999822, -74.65374052328654386, 8.840884882374837161 ) ) ;
#42145=EDGE_LOOP ( 'NONE', ( #10256, #37336, #14209, #14215 ) ) ;
#42149=AXIS2_PLACEMENT_3D ( 'NONE', #14983, #6908, #29899 ) ;
#42153=VECTOR ( 'NONE', #27346, 1000.000000000000000 ) ;
#42158=AXIS2_PLACEMENT_3D ( 'NONE', #9966, #9716, #6070 ) ;
#42164=EDGE_CURVE ( 'NONE', #30064, #14957, #12706, .T. ) ;
#42168=DIRECTION ( 'NONE',  ( 0.000000000000000000, 0.000000000000000000, 1.000000000000000000 ) ) ;
#42169=LINE ( 'NONE', #34099, #10897 ) ;
#42170=ORIENTED_EDGE ( 'NONE', *, *, #25136, .F. ) ;
#42177=DIRECTION ( 'NONE',  ( 0.000000000000000000, 0.000000000000000000, 1.000000000000000000 ) ) ;
#42178=CARTESIAN_POINT ( 'NONE',  ( 11.99999999999999822, -66.50666863322028632, 39.78640506895582973 ) ) ;
#42180=LINE ( 'NONE', #5462, #21381 ) ;
#42186=CIRCLE ( 'NONE', #7795, 31.99999999999998579 ) ;
#42187=CIRCLE ( 'NONE', #48426, 82.00000000000000000 ) ;
#42189=DIRECTION ( 'NONE',  ( 0.000000000000000000, 0.000000000000000000, 1.000000000000000000 ) ) ;
#42191=LINE ( 'NONE', #46116, #26773 ) ;
#42192=CARTESIAN_POINT ( 'NONE',  ( 15.00000000000000000, -0.9646360437375368635, -23.52805723605589705 ) ) ;
#42196=CYLINDRICAL_SURFACE ( 'NONE', #23804, 31.99999999999998579 ) ;
#42198=ORIENTED_EDGE ( 'NONE', *, *, #28398, .F. ) ;
#42209=CIRCLE ( 'NONE', #7051, 31.99999999999998224 ) ;
#42211=EDGE_CURVE ( 'NONE', #26390, #43790, #174, .T. ) ;
#42215=LINE ( 'NONE', #8673, #43359 ) ;
#42219=ORIENTED_EDGE ( 'NONE', *, *, #4232, .T. ) ;
#42220=ORIENTED_EDGE ( 'NONE', *, *, #37069, .F. ) ;
#42221=VECTOR ( 'NONE', #28431, 1000.000000000000000 ) ;
#42223=CARTESIAN_POINT ( 'NONE',  ( 11.99999999999999822, 75.11764819372149304, -2.946379043146603482 ) ) ;
#42228=ORIENTED_EDGE ( 'NONE', *, *, #38814, .T. ) ;
#42233=CYLINDRICAL_SURFACE ( 'NONE', #23856, 77.49899999999999523 ) ;
#42234=CARTESIAN_POINT ( 'NONE',  ( 11.99999999999999822, 50.95692526931329525, 58.39081064771768581 ) ) ;
#42240=CARTESIAN_POINT ( 'NONE',  ( 11.99999999999999822, 20.41045688087930898, -72.35160999960793049 ) ) ;
#42243=EDGE_CURVE ( 'NONE', #39592, #48218, #17598, .T. ) ;
#42244=CARTESIAN_POINT ( 'NONE',  ( 15.00000000000000000, 16.61724383029390140, 20.69703378468902955 ) ) ;
#42245=ORIENTED_EDGE ( 'NONE', *, *, #2355, .F. ) ;
#42248=DIRECTION ( 'NONE',  ( 0.000000000000000000, 0.000000000000000000, 1.000000000000000000 ) ) ;
#42250=CARTESIAN_POINT ( 'NONE',  ( 12.00000000000000000, -10.45096189432314127, 21.10159698893440350 ) ) ;
#42253=DIRECTION ( 'NONE',  ( 0.000000000000000000, 0.000000000000000000, -1.000000000000000000 ) ) ;
#42257=CARTESIAN_POINT ( 'NONE',  ( 11.99999999999999822, 49.70050353004975818, -59.46389618801909904 ) ) ;
#42259=EDGE_LOOP ( 'NONE', ( #22020, #29080, #38393, #2635 ) ) ;
#42260=VECTOR ( 'NONE', #3528, 1000.000000000000000 ) ;
#42263=DIRECTION ( 'NONE',  ( -1.000000000000000000, -0.000000000000000000, -0.000000000000000000 ) ) ;
#42264=CIRCLE ( 'NONE', #32921, 21.00000000000000000 ) ;
#42266=AXIS2_PLACEMENT_3D ( 'NONE', #32380, #6671, #21600 ) ;
#42275=ORIENTED_EDGE ( 'NONE', *, *, #48451, .T. ) ;
#42276=EDGE_CURVE ( 'NONE', #43286, #11880, #32988, .T. ) ;
#42279=EDGE_LOOP ( 'NONE', ( #17688, #39056, #21195, #42373 ) ) ;
#42284=VECTOR ( 'NONE', #1836, 1000.000000000000000 ) ;
#42291=ORIENTED_EDGE ( 'NONE', *, *, #43924, .T. ) ;
#42296=VERTEX_POINT ( 'NONE', #9779 ) ;
#42303=CIRCLE ( 'NONE', #846, 31.99999999999999289 ) ;
#42306=VERTEX_POINT ( 'NONE', #39665 ) ;
#42311=CYLINDRICAL_SURFACE ( 'NONE', #31824, 77.49899999999999523 ) ;
#42314=DIRECTION ( 'NONE',  ( -1.000000000000000000, 0.000000000000000000, 0.000000000000000000 ) ) ;
#42315=CARTESIAN_POINT ( 'NONE',  ( 11.99999999999999822, 59.75363087400153006, -56.15606465354896670 ) ) ;
#42324=ORIENTED_EDGE ( 'NONE', *, *, #4537, .F. ) ;
#42329=EDGE_CURVE ( 'NONE', #45805, #33355, #44002, .T. ) ;
#42332=AXIS2_PLACEMENT_3D ( 'NONE', #7260, #36636, #3097 ) ;
#42333=EDGE_CURVE ( 'NONE', #44620, #12035, #40131, .T. ) ;
#42334=AXIS2_PLACEMENT_3D ( 'NONE', #33860, #26766, #34332 ) ;
#42347=VERTEX_POINT ( 'NONE', #4610 ) ;
#42349=DIRECTION ( 'NONE',  ( -1.000000000000000000, -0.000000000000000000, -0.000000000000000000 ) ) ;
#42350=DIRECTION ( 'NONE',  ( -1.000000000000000000, 0.000000000000000000, 0.000000000000000000 ) ) ;
#42356=CARTESIAN_POINT ( 'NONE',  ( 15.00000000000000000, 20.85821328998756385, 10.92862929874494249 ) ) ;
#42358=ORIENTED_EDGE ( 'NONE', *, *, #4645, .T. ) ;
#42360=CARTESIAN_POINT ( 'NONE',  ( 11.99999999999999822, -46.53671651293991118, 59.03961581697383565 ) ) ;
#42367=DIRECTION ( 'NONE',  ( -1.000000000000000000, 0.000000000000000000, 0.000000000000000000 ) ) ;
#42370=DIRECTION ( 'NONE',  ( 0.000000000000000000, -0.8090169943749401238, -0.5877852522924831291 ) ) ;
#42373=ORIENTED_EDGE ( 'NONE', *, *, #667, .T. ) ;
#42374=EDGE_CURVE ( 'NONE', #1298, #4855, #27586, .T. ) ;
#42381=DIRECTION ( 'NONE',  ( 0.000000000000000000, 1.000000000000000000, 3.491481338843133355E-15 ) ) ;
#42383=DIRECTION ( 'NONE',  ( -0.000000000000000000, 0.5000000000000038858, 0.8660254037844363761 ) ) ;
#42384=ADVANCED_FACE ( 'NONE', ( #45476 ), #41105, .T. ) ;
#42390=SHAPE_DEFINITION_REPRESENTATION ( #2266, #37520 ) ;
#42392=VERTEX_POINT ( 'NONE', #15398 ) ;
#42400=CYLINDRICAL_SURFACE ( 'NONE', #16446, 31.99999999999998579 ) ;
#42403=DIRECTION ( 'NONE',  ( 0.000000000000000000, -0.07845909572783058006, -0.9969173337331290741 ) ) ;
#42406=ORIENTED_EDGE ( 'NONE', *, *, #26790, .F. ) ;
#42407=DIRECTION ( 'NONE',  ( -0.000000000000000000, -1.000000000000000000, -1.445602896647339656E-16 ) ) ;
#42409=AXIS2_PLACEMENT_3D ( 'NONE', #28066, #31506, #46425 ) ;
#42412=CARTESIAN_POINT ( 'NONE',  ( 11.99999999999999822, -58.39081064771713869, -50.95692526931392052 ) ) ;
#42413=DIRECTION ( 'NONE',  ( -0.000000000000000000, -1.000000000000000000, -1.445602896647339656E-16 ) ) ;
#42417=CARTESIAN_POINT ( 'NONE',  ( 6.000000000000000000, 74.18225833017888249, 34.94270380257665209 ) ) ;
#42418=ORIENTED_EDGE ( 'NONE', *, *, #1225, .F. ) ;
#42423=LINE ( 'NONE', #42178, #2407 ) ;
#42426=DIRECTION ( 'NONE',  ( 0.000000000000000000, -0.9135454576426050854, -0.4067366430757908824 ) ) ;
#42427=DIRECTION ( 'NONE',  ( 0.000000000000000000, 0.000000000000000000, -1.000000000000000000 ) ) ;
#42431=VECTOR ( 'NONE', #7627, 1000.000000000000000 ) ;
#42432=EDGE_CURVE ( 'NONE', #21150, #40230, #3882, .T. ) ;
#42436=CIRCLE ( 'NONE', #7235, 31.99999999999999289 ) ;
#42440=DIRECTION ( 'NONE',  ( -1.000000000000000000, -0.000000000000000000, -0.000000000000000000 ) ) ;
#42463=CARTESIAN_POINT ( 'NONE',  ( 11.99999999999999822, 0.000000000000000000, 0.000000000000000000 ) ) ;
#42470=FACE_OUTER_BOUND ( 'NONE', #30378, .T. ) ;
#42474=ORIENTED_EDGE ( 'NONE', *, *, #33585, .T. ) ;
#42483=CARTESIAN_POINT ( 'NONE',  ( 0.000000000000000000, 65.64334221924909230, 41.19522573413756561 ) ) ;
#42485=AXIS2_PLACEMENT_3D ( 'NONE', #36072, #10623, #47800 ) ;
#42487=ORIENTED_EDGE ( 'NONE', *, *, #5850, .T. ) ;
#42492=ORIENTED_EDGE ( 'NONE', *, *, #7540, .F. ) ;
#42496=DIRECTION ( 'NONE',  ( 1.000000000000000000, 0.000000000000000000, -0.000000000000000000 ) ) ;
#42497=EDGE_CURVE ( 'NONE', #13195, #40856, #46707, .T. ) ;
#42498=ADVANCED_FACE ( 'NONE', ( #9247 ), #4854, .T. ) ;
#42499=CARTESIAN_POINT ( 'NONE',  ( 50.00005079999999680, 0.000000000000000000, 0.000000000000000000 ) ) ;
#42502=ADVANCED_FACE ( 'NONE', ( #9009 ), #31297, .T. ) ;
#42504=DIRECTION ( 'NONE',  ( -1.000000000000000000, 0.000000000000000000, 0.000000000000000000 ) ) ;
#42506=EDGE_CURVE ( 'NONE', #37720, #47426, #42436, .T. ) ;
#42507=CIRCLE ( 'NONE', #11230, 31.99999999999998579 ) ;
#42508=AXIS2_PLACEMENT_3D ( 'NONE', #41520, #38326, #45193 ) ;
#42511=DIRECTION ( 'NONE',  ( 0.000000000000000000, 0.000000000000000000, 1.000000000000000000 ) ) ;
#42516=AXIS2_PLACEMENT_3D ( 'NONE', #14262, #14752, #48274 ) ;
#42518=AXIS2_PLACEMENT_3D ( 'NONE', #37728, #4207, #34052 ) ;
#42519=EDGE_LOOP ( 'NONE', ( #17294, #42877, #14376, #12267 ) ) ;
#42525=ADVANCED_FACE ( 'NONE', ( #15870 ), #16356, .T. ) ;
#42531=VECTOR ( 'NONE', #29795, 1000.000000000000000 ) ;
#42534=EDGE_CURVE ( 'NONE', #28171, #10773, #1181, .T. ) ;
#42536=CARTESIAN_POINT ( 'NONE',  ( 12.00000000000000000, -25.60904388321915803, 6.976881207771517879 ) ) ;
#42537=VERTEX_POINT ( 'NONE', #5835 ) ;
#42540=VERTEX_POINT ( 'NONE', #1921 ) ;
#42547=CARTESIAN_POINT ( 'NONE',  ( 12.00000000000000000, 14.60985201121729737, 18.46759930825687590 ) ) ;
#42549=DIRECTION ( 'NONE',  ( 0.000000000000000000, 0.000000000000000000, 1.000000000000000000 ) ) ;
#42550=ORIENTED_EDGE ( 'NONE', *, *, #45939, .F. ) ;
#42556=VERTEX_POINT ( 'NONE', #16591 ) ;
#42561=CIRCLE ( 'NONE', #33942, 31.99999999999999289 ) ;
#42562=DIRECTION ( 'NONE',  ( 0.000000000000000000, 0.000000000000000000, 1.000000000000000000 ) ) ;
#42563=EDGE_CURVE ( 'NONE', #18691, #34257, #12213, .T. ) ;
#42568=ADVANCED_FACE ( 'NONE', ( #922 ), #20753, .F. ) ;
#42572=DIRECTION ( 'NONE',  ( 0.000000000000000000, 0.7604059656000276002, 0.6494480483301875440 ) ) ;
#42574=LINE ( 'NONE', #37929, #20580 ) ;
#42577=VERTEX_POINT ( 'NONE', #35429 ) ;
#42578=VERTEX_POINT ( 'NONE', #13165 ) ;
#42581=AXIS2_PLACEMENT_3D ( 'NONE', #8670, #26804, #19216 ) ;
#42584=CARTESIAN_POINT ( 'NONE',  ( 0.000000000000000000, 65.64334221924964652, -41.19522573413665611 ) ) ;
#42585=ORIENTED_EDGE ( 'NONE', *, *, #4365, .T. ) ;
#42587=VECTOR ( 'NONE', #30642, 1000.000000000000000 ) ;
#42597=LINE ( 'NONE', #42835, #20341 ) ;
#42604=EDGE_LOOP ( 'NONE', ( #24872, #8866, #4605, #2721 ) ) ;
#42606=ORIENTED_EDGE ( 'NONE', *, *, #10228, .F. ) ;
#42610=CARTESIAN_POINT ( 'NONE',  ( 0.000000000000000000, 50.95692526931329525, 58.39081064771768581 ) ) ;
#42614=ORIENTED_EDGE ( 'NONE', *, *, #2164, .T. ) ;
#42617=AXIS2_PLACEMENT_3D ( 'NONE', #43396, #20146, #39730 ) ;
#42619=ORIENTED_EDGE ( 'NONE', *, *, #28013, .T. ) ;
#42620=DIRECTION ( 'NONE',  ( -1.000000000000000000, -0.000000000000000000, -0.000000000000000000 ) ) ;
#42631=CARTESIAN_POINT ( 'NONE',  ( 11.99999999999999822, 0.000000000000000000, 0.000000000000000000 ) ) ;
#42635=DIRECTION ( 'NONE',  ( 0.000000000000000000, 0.5877852522924684742, 0.8090169943749506709 ) ) ;
#42638=CARTESIAN_POINT ( 'NONE',  ( 11.99999999999999822, -76.69515212746036070, 29.01471420065536932 ) ) ;
#42640=VERTEX_POINT ( 'NONE', #43266 ) ;
#42645=AXIS2_PLACEMENT_3D ( 'NONE', #30346, #11738, #8051 ) ;
#42646=DIRECTION ( 'NONE',  ( 0.000000000000000000, 0.000000000000000000, 1.000000000000000000 ) ) ;
#42647=VERTEX_POINT ( 'NONE', #13891 ) ;
#42663=CARTESIAN_POINT ( 'NONE',  ( 11.99999999999999822, -74.65491531819111515, 23.16904090965678265 ) ) ;
#42665=VECTOR ( 'NONE', #39727, 1000.000000000000000 ) ;
#42667=CARTESIAN_POINT ( 'NONE',  ( 5.999999999999999112, -56.15606465354916566, -59.75363087400133111 ) ) ;
#42668=CARTESIAN_POINT ( 'NONE',  ( 11.99999999999999822, 0.000000000000000000, 0.000000000000000000 ) ) ;
#42671=CARTESIAN_POINT ( 'NONE',  ( 15.00000000000000000, -23.29833615347109088, -3.418703333116486665 ) ) ;
#42672=ORIENTED_EDGE ( 'NONE', *, *, #20947, .T. ) ;
#42676=AXIS2_PLACEMENT_3D ( 'NONE', #17318, #40097, #32271 ) ;
#42678=CARTESIAN_POINT ( 'NONE',  ( 0.000000000000000000, 41.19522573413732403, 65.64334221924923440 ) ) ;
#42680=LINE ( 'NONE', #4506, #44870 ) ;
#42681=ADVANCED_FACE ( 'NONE', ( #17067 ), #6541, .T. ) ;
#42684=ADVANCED_FACE ( 'NONE', ( #2371 ), #2863, .F. ) ;
#42686=DIRECTION ( 'NONE',  ( -1.000000000000000000, 0.000000000000000000, -0.000000000000000000 ) ) ;
#42687=CARTESIAN_POINT ( 'NONE',  ( 0.000000000000000000, -5.256550761632340141, -77.32052557432847095 ) ) ;
#42696=DIRECTION ( 'NONE',  ( -1.000000000000000000, 0.000000000000000000, 0.000000000000000000 ) ) ;
#42697=ORIENTED_EDGE ( 'NONE', *, *, #41611, .T. ) ;
#42700=FACE_OUTER_BOUND ( 'NONE', #42519, .T. ) ;
#42704=AXIS2_PLACEMENT_3D ( 'NONE', #44120, #37004, #3482 ) ;
#42709=CIRCLE ( 'NONE', #46624, 31.99999999999998579 ) ;
#42711=CARTESIAN_POINT ( 'NONE',  ( 0.000000000000000000, -81.34940948281328588, -10.30890764327469000 ) ) ;
#42718=ORIENTED_EDGE ( 'NONE', *, *, #41921, .T. ) ;
#42723=DIRECTION ( 'NONE',  ( 0.000000000000000000, 0.000000000000000000, 1.000000000000000000 ) ) ;
#42724=AXIS2_PLACEMENT_3D ( 'NONE', #24172, #32485, #43257 ) ;
#42727=ORIENTED_EDGE ( 'NONE', *, *, #2709, .F. ) ;
#42730=CARTESIAN_POINT ( 'NONE',  ( 11.99999999999999822, 0.000000000000000000, 0.000000000000000000 ) ) ;
#42732=DIRECTION ( 'NONE',  ( 0.000000000000000000, 0.9510565162951521989, 0.3090169943749515591 ) ) ;
#42733=DIRECTION ( 'NONE',  ( -1.000000000000000000, -0.000000000000000000, 0.000000000000000000 ) ) ;
#42735=CARTESIAN_POINT ( 'NONE',  ( 15.00000000000000000, -3.948201729842032215, 23.21447184625297666 ) ) ;
#42738=ADVANCED_FACE ( 'NONE', ( #46937 ), #13405, .T. ) ;
#42739=ORIENTED_EDGE ( 'NONE', *, *, #28784, .T. ) ;
#42745=ORIENTED_EDGE ( 'NONE', *, *, #3798, .F. ) ;
#42747=CARTESIAN_POINT ( 'NONE',  ( 0.000000000000000000, 0.000000000000000000, 0.000000000000000000 ) ) ;
#42749=LINE ( 'NONE', #23897, #39370 ) ;
#42754=AXIS2_PLACEMENT_3D ( 'NONE', #39855, #2623, #36417 ) ;
#42759=ORIENTED_EDGE ( 'NONE', *, *, #35475, .T. ) ;
#42761=ORIENTED_EDGE ( 'NONE', *, *, #5715, .T. ) ;
#42767=CIRCLE ( 'NONE', #36489, 82.00000000000000000 ) ;
#42772=FACE_OUTER_BOUND ( 'NONE', #15437, .T. ) ;
#42776=VERTEX_POINT ( 'NONE', #3587 ) ;
#42781=AXIS2_PLACEMENT_3D ( 'NONE', #15531, #30465, #11860 ) ;
#42784=FACE_OUTER_BOUND ( 'NONE', #18572, .T. ) ;
#42787=ORIENTED_EDGE ( 'NONE', *, *, #32023, .F. ) ;
#42788=CYLINDRICAL_SURFACE ( 'NONE', #45474, 82.00000000000000000 ) ;
#42789=CARTESIAN_POINT ( 'NONE',  ( -10.00000000000000000, 0.000000000000000000, 0.000000000000000000 ) ) ;
#42791=CARTESIAN_POINT ( 'NONE',  ( 11.99999999999999822, 76.41127070299290835, -12.93880638057234123 ) ) ;
#42793=CARTESIAN_POINT ( 'NONE',  ( 12.00000000000000000, 16.83928648764945635, 16.46020748918027010 ) ) ;
#42794=ORIENTED_EDGE ( 'NONE', *, *, #47052, .T. ) ;
#42799=AXIS2_PLACEMENT_3D ( 'NONE', #20930, #5760, #39546 ) ;
#42807=CARTESIAN_POINT ( 'NONE',  ( 15.00000000000000000, -11.95096189432345746, -23.69967320028757030 ) ) ;
#42828=CYLINDRICAL_SURFACE ( 'NONE', #12466, 31.99999999999998579 ) ;
#42831=ORIENTED_EDGE ( 'NONE', *, *, #664, .T. ) ;
#42832=VERTEX_POINT ( 'NONE', #30022 ) ;
#42834=ADVANCED_FACE ( 'NONE', ( #37362 ), #44953, .F. ) ;
#42835=CARTESIAN_POINT ( 'NONE',  ( 6.000000000000000000, 71.87247863392413194, 39.47590169984871267 ) ) ;
#42856=ORIENTED_EDGE ( 'NONE', *, *, #318, .T. ) ;
#42859=DIRECTION ( 'NONE',  ( -1.000000000000000000, 0.000000000000000000, 0.000000000000000000 ) ) ;
#42861=DIRECTION ( 'NONE',  ( -1.000000000000000000, -0.000000000000000000, -0.000000000000000000 ) ) ;
#42864=CIRCLE ( 'NONE', #10001, 77.49899999999999523 ) ;
#42874=AXIS2_PLACEMENT_3D ( 'NONE', #46195, #12919, #3078 ) ;
#42877=ORIENTED_EDGE ( 'NONE', *, *, #47304, .T. ) ;
#42880=CARTESIAN_POINT ( 'NONE',  ( 11.99999999999999822, 0.000000000000000000, 0.000000000000000000 ) ) ;
#42883=ORIENTED_EDGE ( 'NONE', *, *, #5577, .F. ) ;
#42888=CARTESIAN_POINT ( 'NONE',  ( 11.99999999999999822, -2.946379043145784582, -75.11764819372150725 ) ) ;
#42889=ORIENTED_EDGE ( 'NONE', *, *, #11104, .T. ) ;
#42894=CARTESIAN_POINT ( 'NONE',  ( 15.00000000000000000, 6.762365576493647445, 25.66652317338391498 ) ) ;
#42903=DIRECTION ( 'NONE',  ( -1.000000000000000000, 0.000000000000000000, 0.000000000000000000 ) ) ;
#42904=LINE ( 'NONE', #42667, #45827 ) ;
#42911=DIRECTION ( 'NONE',  ( 0.000000000000000000, 0.000000000000000000, 1.000000000000000000 ) ) ;
#42914=DIRECTION ( 'NONE',  ( -1.000000000000000000, 0.000000000000000000, 0.000000000000000000 ) ) ;
#42916=ORIENTED_EDGE ( 'NONE', *, *, #17712, .F. ) ;
#42917=DIRECTION ( 'NONE',  ( -1.000000000000000000, 0.000000000000000000, -0.000000000000000000 ) ) ;
#42928=CARTESIAN_POINT ( 'NONE',  ( 11.99999999999999822, 0.000000000000000000, 0.000000000000000000 ) ) ;
#42929=ORIENTED_EDGE ( 'NONE', *, *, #41343, .F. ) ;
#42931=AXIS2_PLACEMENT_3D ( 'NONE', #32526, #44264, #10740 ) ;
#42935=AXIS2_PLACEMENT_3D ( 'NONE', #26388, #45227, #3863 ) ;
#42939=CARTESIAN_POINT ( 'NONE',  ( 11.99999999999999822, -2.946379043145784582, -75.11764819372150725 ) ) ;
#42940=ORIENTED_EDGE ( 'NONE', *, *, #17459, .T. ) ;
#42943=ORIENTED_EDGE ( 'NONE', *, *, #45578, .F. ) ;
#42947=CARTESIAN_POINT ( 'NONE',  ( 11.99999999999999822, 16.65972982744933972, 80.28980883073764119 ) ) ;
#42948=EDGE_CURVE ( 'NONE', #22205, #38319, #33051, .T. ) ;
#42954=EDGE_CURVE ( 'NONE', #36873, #14595, #8846, .T. ) ;
#42955=ORIENTED_EDGE ( 'NONE', *, *, #32793, .T. ) ;
#42957=FACE_OUTER_BOUND ( 'NONE', #39987, .T. ) ;
#42960=CIRCLE ( 'NONE', #48397, 77.49899999999999523 ) ;
#42962=ORIENTED_EDGE ( 'NONE', *, *, #9724, .F. ) ;
#42969=CARTESIAN_POINT ( 'NONE',  ( 0.000000000000000000, 54.21277698773752007, -55.38113227695726692 ) ) ;
#42970=LINE ( 'NONE', #31732, #33822 ) ;
#42973=DIRECTION ( 'NONE',  ( -1.000000000000000000, 0.000000000000000000, 0.000000000000000000 ) ) ;
#42974=DIRECTION ( 'NONE',  ( -1.000000000000000000, 0.000000000000000000, 0.000000000000000000 ) ) ;
#42977=CARTESIAN_POINT ( 'NONE',  ( 11.99999999999999822, 77.19088730480532945, -6.903761155836932062 ) ) ;
#42981=CARTESIAN_POINT ( 'NONE',  ( 11.99999999999999822, -41.76937507738745836, -62.50329211542482710 ) ) ;
#42987=EDGE_CURVE ( 'NONE', #19565, #16881, #18199, .T. ) ;
#42990=ORIENTED_EDGE ( 'NONE', *, *, #17024, .T. ) ;
#42991=DIRECTION ( 'NONE',  ( -0.000000000000000000, -0.6691306063588570163, 0.7431448254773953543 ) ) ;
#42995=CYLINDRICAL_SURFACE ( 'NONE', #42409, 82.00000000000000000 ) ;
#42997=ORIENTED_EDGE ( 'NONE', *, *, #34867, .T. ) ;
#42998=AXIS2_PLACEMENT_3D ( 'NONE', #4778, #19679, #12371 ) ;
#43000=AXIS2_PLACEMENT_3D ( 'NONE', #12002, #15906, #18837 ) ;
#43007=VECTOR ( 'NONE', #47522, 1000.000000000000000 ) ;
#43012=ORIENTED_EDGE ( 'NONE', *, *, #31637, .T. ) ;
#43020=DIRECTION ( 'NONE',  ( 0.000000000000000000, 0.3826834323650904479, -0.9238795325112865164 ) ) ;
#43024=CARTESIAN_POINT ( 'NONE',  ( 0.000000000000000000, 71.87247863392471459, -39.47590169984771080 ) ) ;
#43026=DIRECTION ( 'NONE',  ( -1.000000000000000000, 0.000000000000000000, 0.000000000000000000 ) ) ;
#43035=ORIENTED_EDGE ( 'NONE', *, *, #15878, .F. ) ;
#43040=CARTESIAN_POINT ( 'NONE',  ( 11.99999999999999822, 0.000000000000000000, 0.000000000000000000 ) ) ;
#43046=CARTESIAN_POINT ( 'NONE',  ( 15.00000000000000000, 16.83928648764945635, 16.46020748918027010 ) ) ;
#43049=EDGE_CURVE ( 'NONE', #5583, #1751, #25074, .T. ) ;
#43056=ORIENTED_EDGE ( 'NONE', *, *, #11218, .F. ) ;
#43057=EDGE_CURVE ( 'NONE', #36518, #44612, #36339, .T. ) ;
#43058=ADVANCED_FACE ( 'NONE', ( #28760 ), #32197, .T. ) ;
#43068=ORIENTED_EDGE ( 'NONE', *, *, #43443, .F. ) ;
#43070=AXIS2_PLACEMENT_3D ( 'NONE', #12752, #27685, #15943 ) ;
#43072=CARTESIAN_POINT ( 'NONE',  ( 15.00000000000000000, -22.67460108101774452, 6.353146135318220367 ) ) ;
#43075=CARTESIAN_POINT ( 'NONE',  ( 0.000000000000000000, 81.50828551894227303, 8.966570791700986476 ) ) ;
#43084=CARTESIAN_POINT ( 'NONE',  ( 15.00000000000000000, -19.89357724624986545, 12.59942793731086219 ) ) ;
#43085=CARTESIAN_POINT ( 'NONE',  ( 5.999999999999999112, -56.15606465355000410, 59.75363087400056372 ) ) ;
#43089=DIRECTION ( 'NONE',  ( 0.000000000000000000, 0.000000000000000000, 1.000000000000000000 ) ) ;
#43095=FACE_OUTER_BOUND ( 'NONE', #35394, .T. ) ;
#43096=CIRCLE ( 'NONE', #36827, 82.00000000000000000 ) ;
#43103=DIRECTION ( 'NONE',  ( 0.000000000000000000, 0.8660254037844421493, 0.4999999999999938938 ) ) ;
#43107=ADVANCED_FACE ( 'NONE', ( #32898 ), #14308, .F. ) ;
#43109=ORIENTED_EDGE ( 'NONE', *, *, #45225, .F. ) ;
#43116=FACE_OUTER_BOUND ( 'NONE', #12009, .T. ) ;
#43118=EDGE_CURVE ( 'NONE', #4884, #39718, #2098, .T. ) ;
#43125=ORIENTED_EDGE ( 'NONE', *, *, #9402, .F. ) ;
#43126=DIRECTION ( 'NONE',  ( 0.000000000000000000, 0.000000000000000000, -1.000000000000000000 ) ) ;
#43128=ADVANCED_FACE ( 'NONE', ( #36096 ), #9917, .F. ) ;
#43134=AXIS2_PLACEMENT_3D ( 'NONE', #1539, #16461, #27733 ) ;
#43135=ORIENTED_EDGE ( 'NONE', *, *, #17548, .T. ) ;
#43137=CYLINDRICAL_SURFACE ( 'NONE', #31446, 77.49899999999999523 ) ;
#43138=VERTEX_POINT ( 'NONE', #17488 ) ;
#43140=LINE ( 'NONE', #21584, #21427 ) ;
#43150=VECTOR ( 'NONE', #11710, 1000.000000000000000 ) ;
#43151=DIRECTION ( 'NONE',  ( 0.000000000000000000, -0.5224985647159381408, -0.8526401643540988395 ) ) ;
#43156=CARTESIAN_POINT ( 'NONE',  ( 15.00000000000000000, -26.23277895567251505, -4.042438405569750870 ) ) ;
#43161=DIRECTION ( 'NONE',  ( -1.000000000000000000, -0.000000000000000000, 0.000000000000000000 ) ) ;
#43169=AXIS2_PLACEMENT_3D ( 'NONE', #48327, #30459, #38050 ) ;
#43171=ORIENTED_EDGE ( 'NONE', *, *, #27014, .F. ) ;
#43174=DIRECTION ( 'NONE',  ( -1.000000000000000000, -0.000000000000000000, -0.000000000000000000 ) ) ;
#43179=ORIENTED_EDGE ( 'NONE', *, *, #6528, .T. ) ;
#43181=AXIS2_PLACEMENT_3D ( 'NONE', #17313, #16605, #12955 ) ;
#43184=CARTESIAN_POINT ( 'NONE',  ( 0.000000000000000000, -18.89407956138310496, 75.16055320797023853 ) ) ;
#43185=CARTESIAN_POINT ( 'NONE',  ( 11.99999999999999822, -49.70050353004932475, 59.46389618801947563 ) ) ;
#43199=ORIENTED_EDGE ( 'NONE', *, *, #23038, .T. ) ;
#43202=CARTESIAN_POINT ( 'NONE',  ( 0.000000000000000000, -71.91182617369207719, 28.89263327155721228 ) ) ;
#43207=DIRECTION ( 'NONE',  ( -1.000000000000000000, 0.000000000000000000, -0.000000000000000000 ) ) ;
#43209=LINE ( 'NONE', #5525, #147 ) ;
#43215=EDGE_CURVE ( 'NONE', #17270, #13555, #14565, .T. ) ;
#43222=CARTESIAN_POINT ( 'NONE',  ( 5.999999999999999112, -46.11716303203136391, -67.80270845531939017 ) ) ;
#43228=VECTOR ( 'NONE', #14763, 1000.000000000000000 ) ;
#43230=EDGE_LOOP ( 'NONE', ( #29292, #26410, #6605, #18239 ) ) ;
#43236=AXIS2_PLACEMENT_3D ( 'NONE', #29466, #45122, #14551 ) ;
#43237=AXIS2_PLACEMENT_3D ( 'NONE', #22438, #30019, #38092 ) ;
#43239=ORIENTED_EDGE ( 'NONE', *, *, #24869, .T. ) ;
#43241=ADVANCED_FACE ( 'NONE', ( #15290 ), #10879, .T. ) ;
#43242=EDGE_LOOP ( 'NONE', ( #4862, #27176, #24886, #18558 ) ) ;
#43243=LINE ( 'NONE', #27592, #24198 ) ;
#43245=DIRECTION ( 'NONE',  ( 0.000000000000000000, 0.000000000000000000, 1.000000000000000000 ) ) ;
#43252=VERTEX_POINT ( 'NONE', #37308 ) ;
#43254=ADVANCED_FACE ( 'NONE', ( #19184 ), #37786, .T. ) ;
#43255=VERTEX_POINT ( 'NONE', #25556 ) ;
#43257=DIRECTION ( 'NONE',  ( 0.000000000000000000, 0.000000000000000000, -1.000000000000000000 ) ) ;
#43266=CARTESIAN_POINT ( 'NONE',  ( 0.000000000000000000, 50.23322058963348979, 64.81221759200361987 ) ) ;
#43279=CARTESIAN_POINT ( 'NONE',  ( 0.000000000000000000, -63.18004540532994184, -44.88180994100444821 ) ) ;
#43281=AXIS2_PLACEMENT_3D ( 'NONE', #22680, #33695, #159 ) ;
#43282=EDGE_CURVE ( 'NONE', #2837, #29636, #42507, .T. ) ;
#43284=DIRECTION ( 'NONE',  ( -1.000000000000000000, -0.000000000000000000, 0.000000000000000000 ) ) ;
#43286=VERTEX_POINT ( 'NONE', #9139 ) ;
#43293=CIRCLE ( 'NONE', #41745, 31.99999999999998934 ) ;
#43300=VERTEX_POINT ( 'NONE', #12572 ) ;
#43301=CARTESIAN_POINT ( 'NONE',  ( 0.000000000000000000, -34.44570377933549565, -69.42325613327476219 ) ) ;
#43315=EDGE_CURVE ( 'NONE', #39130, #25331, #42180, .T. ) ;
#43322=DIRECTION ( 'NONE',  ( -1.000000000000000000, -0.000000000000000000, 0.000000000000000000 ) ) ;
#43330=LINE ( 'NONE', #21267, #18057 ) ;
#43332=CARTESIAN_POINT ( 'NONE',  ( 11.99999999999999822, -75.16055320797016748, -18.89407956138335365 ) ) ;
#43334=VERTEX_POINT ( 'NONE', #45608 ) ;
#43339=DIRECTION ( 'NONE',  ( 0.000000000000000000, 0.000000000000000000, 1.000000000000000000 ) ) ;
#43341=DIRECTION ( 'NONE',  ( -1.000000000000000000, 0.000000000000000000, 0.000000000000000000 ) ) ;
#43343=DIRECTION ( 'NONE',  ( -1.000000000000000000, -0.000000000000000000, -0.000000000000000000 ) ) ;
#43344=EDGE_CURVE ( 'NONE', #30381, #4357, #12805, .T. ) ;
#43348=CARTESIAN_POINT ( 'NONE',  ( 15.00000000000000000, 5.835314593368777558, 22.81335362449846471 ) ) ;
#43349=AXIS2_PLACEMENT_3D ( 'NONE', #36093, #16533, #28757 ) ;
#43354=CARTESIAN_POINT ( 'NONE',  ( 11.99999999999999822, 2.956366410620650420, 75.11725578898469280 ) ) ;
#43359=VECTOR ( 'NONE', #30480, 1000.000000000000000 ) ;
#43360=DIRECTION ( 'NONE',  ( 0.000000000000000000, 0.000000000000000000, 1.000000000000000000 ) ) ;
#43361=CIRCLE ( 'NONE', #33939, 31.99999999999998579 ) ;
#43364=CIRCLE ( 'NONE', #2704, 31.99999999999998934 ) ;
#43366=DIRECTION ( 'NONE',  ( -1.000000000000000000, 0.000000000000000000, 0.000000000000000000 ) ) ;
#43367=CIRCLE ( 'NONE', #38661, 31.99999999999998579 ) ;
#43377=VERTEX_POINT ( 'NONE', #31431 ) ;
#43382=ORIENTED_EDGE ( 'NONE', *, *, #16983, .F. ) ;
#43385=DIRECTION ( 'NONE',  ( -1.000000000000000000, 0.000000000000000000, 0.000000000000000000 ) ) ;
#43389=AXIS2_PLACEMENT_3D ( 'NONE', #47566, #14046, #10368 ) ;
#43395=CARTESIAN_POINT ( 'NONE',  ( 0.000000000000000000, 0.000000000000000000, 0.000000000000000000 ) ) ;
#43396=CARTESIAN_POINT ( 'NONE',  ( 11.99999999999999822, 73.72996012237440766, 14.67089635893739619 ) ) ;
#43406=EDGE_CURVE ( 'NONE', #9901, #14655, #20651, .T. ) ;
#43410=EDGE_CURVE ( 'NONE', #15076, #11714, #42680, .T. ) ;
#43412=CARTESIAN_POINT ( 'NONE',  ( 0.000000000000000000, -71.87247863392443037, 39.47590169984818687 ) ) ;
#43417=ORIENTED_EDGE ( 'NONE', *, *, #29253, .F. ) ;
#43422=EDGE_LOOP ( 'NONE', ( #30531, #3267, #4711, #46204 ) ) ;
#43427=EDGE_CURVE ( 'NONE', #6120, #4472, #12841, .T. ) ;
#43433=VERTEX_POINT ( 'NONE', #16005 ) ;
#43435=AXIS2_PLACEMENT_3D ( 'NONE', #25653, #28631, #44510 ) ;
#43437=DIRECTION ( 'NONE',  ( -1.000000000000000000, -0.000000000000000000, -0.000000000000000000 ) ) ;
#43441=DIRECTION ( 'NONE',  ( 0.000000000000000000, -0.1564344650402381687, 0.9876883405951365491 ) ) ;
#43443=EDGE_CURVE ( 'NONE', #8637, #30376, #14408, .T. ) ;
#43444=DIRECTION ( 'NONE',  ( 0.000000000000000000, 0.000000000000000000, 1.000000000000000000 ) ) ;
#43445=VECTOR ( 'NONE', #39378, 1000.000000000000000 ) ;
#43450=FACE_OUTER_BOUND ( 'NONE', #2626, .T. ) ;
#43451=CARTESIAN_POINT ( 'NONE',  ( -10.00000000000000000, 0.000000000000000000, 0.000000000000000000 ) ) ;
#43453=ORIENTED_EDGE ( 'NONE', *, *, #6354, .F. ) ;
#43454=CARTESIAN_POINT ( 'NONE',  ( 11.99999999999999822, -73.95703589263958122, -23.16143007188505010 ) ) ;
#43460=CARTESIAN_POINT ( 'NONE',  ( 11.99999999999999822, 56.15606465354957777, 59.75363087400094031 ) ) ;
#43469=CARTESIAN_POINT ( 'NONE',  ( 12.00000000000000000, 6.762365576493649222, 25.66652317338391853 ) ) ;
#43470=AXIS2_PLACEMENT_3D ( 'NONE', #26484, #22567, #33574 ) ;
#43473=AXIS2_PLACEMENT_3D ( 'NONE', #19892, #4972, #41695 ) ;
#43475=ADVANCED_FACE ( 'NONE', ( #31917 ), #13527, .T. ) ;
#43477=CARTESIAN_POINT ( 'NONE',  ( 0.000000000000000000, -59.03342792756297541, 46.54456581323783126 ) ) ;
#43483=VERTEX_POINT ( 'NONE', #25017 ) ;
#43484=VERTEX_POINT ( 'NONE', #16962 ) ;
#43491=EDGE_LOOP ( 'NONE', ( #22430, #39919, #8940, #43505 ) ) ;
#43492=EDGE_CURVE ( 'NONE', #21764, #28312, #4247, .T. ) ;
#43500=CARTESIAN_POINT ( 'NONE',  ( 0.000000000000000000, 0.000000000000000000, 0.000000000000000000 ) ) ;
#43504=AXIS2_PLACEMENT_3D ( 'NONE', #47185, #13415, #20507 ) ;
#43505=ORIENTED_EDGE ( 'NONE', *, *, #24528, .F. ) ;
#43506=CARTESIAN_POINT ( 'NONE',  ( 0.000000000000000000, 20.40083707022987625, -72.35432306680462489 ) ) ;
#43508=EDGE_CURVE ( 'NONE', #32773, #41443, #19844, .T. ) ;
#43512=CARTESIAN_POINT ( 'NONE',  ( 0.000000000000000000, 28.89263327155848415, -71.91182617369156560 ) ) ;
#43513=DIRECTION ( 'NONE',  ( 0.000000000000000000, 0.000000000000000000, 1.000000000000000000 ) ) ;
#43521=LINE ( 'NONE', #21226, #11346 ) ;
#43522=LINE ( 'NONE', #22137, #24740 ) ;
#43525=DIRECTION ( 'NONE',  ( -1.000000000000000000, -0.000000000000000000, 0.000000000000000000 ) ) ;
#43528=CIRCLE ( 'NONE', #20065, 82.00000000000000000 ) ;
#43535=DIRECTION ( 'NONE',  ( 1.000000000000000000, -0.000000000000000000, -0.000000000000000000 ) ) ;
#43542=CARTESIAN_POINT ( 'NONE',  ( 11.99999999999999822, 0.000000000000000000, 0.000000000000000000 ) ) ;
#43546=LINE ( 'NONE', #2896, #38244 ) ;
#43548=VERTEX_POINT ( 'NONE', #17679 ) ;
#43549=EDGE_LOOP ( 'NONE', ( #42619, #20816, #9621, #30320 ) ) ;
#43550=EDGE_CURVE ( 'NONE', #22912, #41381, #32610, .T. ) ;
#43551=EDGE_CURVE ( 'NONE', #38691, #19053, #47063, .T. ) ;
#43563=ORIENTED_EDGE ( 'NONE', *, *, #23862, .T. ) ;
#43564=CARTESIAN_POINT ( 'NONE',  ( 11.99999999999999822, -65.59268652807237743, 36.72794159290217664 ) ) ;
#43565=ORIENTED_EDGE ( 'NONE', *, *, #13214, .F. ) ;
#43567=FACE_OUTER_BOUND ( 'NONE', #33886, .T. ) ;
#43569=ORIENTED_EDGE ( 'NONE', *, *, #664, .F. ) ;
#43572=CARTESIAN_POINT ( 'NONE',  ( 0.000000000000000000, 0.000000000000000000, 0.000000000000000000 ) ) ;
#43591=CARTESIAN_POINT ( 'NONE',  ( 15.00000000000000000, 14.60985201121729737, 18.46759930825687235 ) ) ;
#43592=EDGE_CURVE ( 'NONE', #41683, #34932, #36038, .T. ) ;
#43595=DIRECTION ( 'NONE',  ( -1.000000000000000000, 0.000000000000000000, 0.000000000000000000 ) ) ;
#43597=ORIENTED_EDGE ( 'NONE', *, *, #45219, .F. ) ;
#43598=AXIS2_PLACEMENT_3D ( 'NONE', #19720, #42504, #38114 ) ;
#43602=ORIENTED_EDGE ( 'NONE', *, *, #32751, .F. ) ;
#43604=EDGE_CURVE ( 'NONE', #3463, #40000, #40203, .T. ) ;
#43607=ORIENTED_EDGE ( 'NONE', *, *, #41146, .F. ) ;
#43611=CYLINDRICAL_SURFACE ( 'NONE', #13726, 31.99999999999998579 ) ;
#43626=ORIENTED_EDGE ( 'NONE', *, *, #27757, .T. ) ;
#43633=CIRCLE ( 'NONE', #21741, 31.99999999999998224 ) ;
#43635=LINE ( 'NONE', #35808, #25884 ) ;
#43641=FACE_OUTER_BOUND ( 'NONE', #42279, .T. ) ;
#43644=DIRECTION ( 'NONE',  ( -1.000000000000000000, -0.000000000000000000, -0.000000000000000000 ) ) ;
#43649=EDGE_CURVE ( 'NONE', #41886, #45830, #48005, .T. ) ;
#43650=DIRECTION ( 'NONE',  ( 0.000000000000000000, 0.000000000000000000, 1.000000000000000000 ) ) ;
#43654=CARTESIAN_POINT ( 'NONE',  ( 11.99999999999999822, -76.66974797899844418, 11.30684508768314522 ) ) ;
#43672=CARTESIAN_POINT ( 'NONE',  ( 0.000000000000000000, 8.830959090343430518, -74.65491531819107252 ) ) ;
#43675=DIRECTION ( 'NONE',  ( 0.000000000000000000, 0.000000000000000000, 1.000000000000000000 ) ) ;
#43680=VERTEX_POINT ( 'NONE', #11971 ) ;
#43681=CARTESIAN_POINT ( 'NONE',  ( 11.99999999999999822, 77.49459641780886443, -0.8261519478433960728 ) ) ;
#43682=CARTESIAN_POINT ( 'NONE',  ( 12.00000000000000000, 26.50000000000000355, -1.500000000000000000 ) ) ;
#43684=CARTESIAN_POINT ( 'NONE',  ( 11.99999999999999822, 46.53671651293948486, 59.03961581697416250 ) ) ;
#43690=CARTESIAN_POINT ( 'NONE',  ( 15.00000000000000000, 0.000000000000000000, 0.000000000000000000 ) ) ;
#43691=VERTEX_POINT ( 'NONE', #26903 ) ;
#43693=DIRECTION ( 'NONE',  ( -1.000000000000000000, 0.000000000000000000, 0.000000000000000000 ) ) ;
#43699=CARTESIAN_POINT ( 'NONE',  ( 0.000000000000000000, 0.000000000000000000, 0.000000000000000000 ) ) ;
#43708=DIRECTION ( 'NONE',  ( 0.000000000000000000, 0.000000000000000000, 1.000000000000000000 ) ) ;
#43719=ORIENTED_EDGE ( 'NONE', *, *, #31077, .T. ) ;
#43721=AXIS2_PLACEMENT_3D ( 'NONE', #40053, #3311, #40533 ) ;
#43724=DIRECTION ( 'NONE',  ( -1.000000000000000000, 0.000000000000000000, 0.000000000000000000 ) ) ;
#43725=ORIENTED_EDGE ( 'NONE', *, *, #1233, .T. ) ;
#43726=AXIS2_PLACEMENT_3D ( 'NONE', #9697, #36600, #21188 ) ;
#43730=ORIENTED_EDGE ( 'NONE', *, *, #38676, .T. ) ;
#43733=EDGE_CURVE ( 'NONE', #41791, #40361, #18496, .T. ) ;
#43739=ORIENTED_EDGE ( 'NONE', *, *, #9219, .F. ) ;
#43741=LINE ( 'NONE', #10933, #15882 ) ;
#43743=DIRECTION ( 'NONE',  ( 0.000000000000000000, 0.000000000000000000, 1.000000000000000000 ) ) ;
#43757=ORIENTED_EDGE ( 'NONE', *, *, #2133, .T. ) ;
#43759=LINE ( 'NONE', #21005, #12183 ) ;
#43760=ADVANCED_FACE ( 'NONE', ( #22417 ), #13204, .T. ) ;
#43761=AXIS2_PLACEMENT_3D ( 'NONE', #32468, #47396, #29271 ) ;
#43766=ORIENTED_EDGE ( 'NONE', *, *, #24042, .T. ) ;
#43767=ORIENTED_EDGE ( 'NONE', *, *, #43508, .F. ) ;
#43768=CIRCLE ( 'NONE', #1574, 31.99999999999998579 ) ;
#43771=CARTESIAN_POINT ( 'NONE',  ( 15.00000000000000000, 24.81905959214260804, -9.408202855044828894 ) ) ;
#43778=AXIS2_PLACEMENT_3D ( 'NONE', #4057, #30255, #30483 ) ;
#43779=DIRECTION ( 'NONE',  ( -1.000000000000000000, 0.000000000000000000, 0.000000000000000000 ) ) ;
#43780=ORIENTED_EDGE ( 'NONE', *, *, #29700, .F. ) ;
#43784=ORIENTED_EDGE ( 'NONE', *, *, #44263, .F. ) ;
#43785=CARTESIAN_POINT ( 'NONE',  ( 11.99999999999999822, -59.03961581697367933, -46.53671651294010303 ) ) ;
#43786=AXIS2_PLACEMENT_3D ( 'NONE', #18205, #33151, #39784 ) ;
#43788=CARTESIAN_POINT ( 'NONE',  ( 11.99999999999999822, 59.75363087400075557, 56.15606465354979093 ) ) ;
#43790=VERTEX_POINT ( 'NONE', #36378 ) ;
#43792=CYLINDRICAL_SURFACE ( 'NONE', #7901, 31.99999999999998579 ) ;
#43797=ORIENTED_EDGE ( 'NONE', *, *, #1264, .F. ) ;
#43802=VERTEX_POINT ( 'NONE', #32694 ) ;
#43807=CARTESIAN_POINT ( 'NONE',  ( 11.99999999999999822, 2.543863470249544623, -81.96053171279901051 ) ) ;
#43808=DIRECTION ( 'NONE',  ( 1.000000000000000000, 0.000000000000000000, 0.000000000000000000 ) ) ;
#43812=CARTESIAN_POINT ( 'NONE',  ( 15.00000000000000000, -26.23277895567245466, 4.042438405570107918 ) ) ;
#43817=ORIENTED_EDGE ( 'NONE', *, *, #9626, .T. ) ;
#43820=CIRCLE ( 'NONE', #24288, 82.00000000000000000 ) ;
#43821=CIRCLE ( 'NONE', #39955, 31.99999999999998579 ) ;
#43823=EDGE_CURVE ( 'NONE', #24762, #923, #48113, .T. ) ;
#43828=ORIENTED_EDGE ( 'NONE', *, *, #23601, .F. ) ;
#43835=ORIENTED_EDGE ( 'NONE', *, *, #19197, .F. ) ;
#43839=FACE_OUTER_BOUND ( 'NONE', #22288, .T. ) ;
#43845=FACE_OUTER_BOUND ( 'NONE', #1978, .T. ) ;
#43848=ADVANCED_FACE ( 'NONE', ( #19678 ), #16040, .T. ) ;
#43850=DIRECTION ( 'NONE',  ( 0.000000000000000000, 0.000000000000000000, 1.000000000000000000 ) ) ;
#43855=CARTESIAN_POINT ( 'NONE',  ( 0.000000000000000000, -16.65972982744876774, -80.28980883073775487 ) ) ;
#43858=CARTESIAN_POINT ( 'NONE',  ( 0.000000000000000000, 0.000000000000000000, 0.000000000000000000 ) ) ;
#43859=CARTESIAN_POINT ( 'NONE',  ( 15.00000000000000000, 8.688484142254226938, 21.88630264137359305 ) ) ;
#43860=AXIS2_PLACEMENT_3D ( 'NONE', #44701, #400, #18984 ) ;
#43861=ORIENTED_EDGE ( 'NONE', *, *, #12945, .F. ) ;
#43864=DIRECTION ( 'NONE',  ( 0.000000000000000000, -0.9238795325112906243, 0.3826834323650805669 ) ) ;
#43869=DIRECTION ( 'NONE',  ( 0.000000000000000000, 0.000000000000000000, -1.000000000000000000 ) ) ;
#43881=EDGE_CURVE ( 'NONE', #11259, #17933, #45647, .T. ) ;
#43883=EDGE_CURVE ( 'NONE', #13636, #45738, #11637, .T. ) ;
#43884=ORIENTED_EDGE ( 'NONE', *, *, #16223, .F. ) ;
#43887=DIRECTION ( 'NONE',  ( 0.000000000000000000, 0.000000000000000000, 1.000000000000000000 ) ) ;
#43889=FACE_OUTER_BOUND ( 'NONE', #35534, .T. ) ;
#43891=ORIENTED_EDGE ( 'NONE', *, *, #35294, .F. ) ;
#43892=DIRECTION ( 'NONE',  ( -1.000000000000000000, -0.000000000000000000, -0.000000000000000000 ) ) ;
#43894=EDGE_CURVE ( 'NONE', #10618, #11777, #45901, .T. ) ;
#43898=CARTESIAN_POINT ( 'NONE',  ( 11.99999999999999822, -2.956366410620109519, -75.11725578898472122 ) ) ;
#43905=VECTOR ( 'NONE', #15674, 1000.000000000000000 ) ;
#43907=CARTESIAN_POINT ( 'NONE',  ( 11.99999999999999822, 0.000000000000000000, 0.000000000000000000 ) ) ;
#43914=DIRECTION ( 'NONE',  ( 0.000000000000000000, 0.000000000000000000, -1.000000000000000000 ) ) ;
#43915=ORIENTED_EDGE ( 'NONE', *, *, #22024, .T. ) ;
#43916=EDGE_LOOP ( 'NONE', ( #21190, #40201, #7542, #12975 ) ) ;
#43918=ADVANCED_FACE ( 'NONE', ( #15067 ), #26563, .T. ) ;
#43919=CYLINDRICAL_SURFACE ( 'NONE', #27775, 82.00000000000000000 ) ;
#43923=DIRECTION ( 'NONE',  ( -1.000000000000000000, 0.000000000000000000, 0.000000000000000000 ) ) ;
#43924=EDGE_CURVE ( 'NONE', #20356, #36250, #44138, .T. ) ;
#43926=DIRECTION ( 'NONE',  ( 0.000000000000000000, 0.000000000000000000, 1.000000000000000000 ) ) ;
#43929=CARTESIAN_POINT ( 'NONE',  ( 0.000000000000000000, 51.29473840253317007, -63.97538442413369353 ) ) ;
#43931=DIRECTION ( 'NONE',  ( 0.000000000000000000, 0.9876883405951371042, 0.1564344650402346715 ) ) ;
#43937=DIRECTION ( 'NONE',  ( 0.000000000000000000, 0.000000000000000000, 1.000000000000000000 ) ) ;
#43940=DIRECTION ( 'NONE',  ( 0.000000000000000000, -0.9723699203976789995, 0.2334453638558957045 ) ) ;
#43941=ORIENTED_EDGE ( 'NONE', *, *, #39582, .F. ) ;
#43943=AXIS2_PLACEMENT_3D ( 'NONE', #30547, #15396, #11483 ) ;
#43949=ORIENTED_EDGE ( 'NONE', *, *, #16829, .F. ) ;
#43950=AXIS2_PLACEMENT_3D ( 'NONE', #15164, #18806, #26656 ) ;
#43951=CARTESIAN_POINT ( 'NONE',  ( 6.000000000000000000, -68.55367621811173251, 44.99326035066031437 ) ) ;
#43952=VERTEX_POINT ( 'NONE', #1606 ) ;
#43955=CIRCLE ( 'NONE', #35359, 82.00000000000000000 ) ;
#43959=CARTESIAN_POINT ( 'NONE',  ( 0.000000000000000000, -56.15606465355000410, 59.75363087400056372 ) ) ;
#43961=LINE ( 'NONE', #18004, #24260 ) ;
#43967=DIRECTION ( 'NONE',  ( -1.000000000000000000, -0.000000000000000000, -0.000000000000000000 ) ) ;
#43970=CIRCLE ( 'NONE', #5682, 77.49899999999999523 ) ;
#43972=EDGE_LOOP ( 'NONE', ( #29412, #19089, #7947, #22434 ) ) ;
#43973=CARTESIAN_POINT ( 'NONE',  ( 5.999999999999999112, 74.74816331893430288, 33.71516098798768724 ) ) ;
#43975=CARTESIAN_POINT ( 'NONE',  ( 15.00000000000000000, -4.261787119645322974, -26.19803753235774835 ) ) ;
#43979=ORIENTED_EDGE ( 'NONE', *, *, #19768, .F. ) ;
#43985=DIRECTION ( 'NONE',  ( 0.000000000000000000, 0.000000000000000000, -1.000000000000000000 ) ) ;
#43986=CARTESIAN_POINT ( 'NONE',  ( 15.00000000000000000, 16.61724383029361718, -20.69703378468926402 ) ) ;
#43987=EDGE_LOOP ( 'NONE', ( #6928, #22898, #2244, #23996 ) ) ;
#43989=CYLINDRICAL_SURFACE ( 'NONE', #13197, 31.99999999999998579 ) ;
#43990=VERTEX_POINT ( 'NONE', #17009 ) ;
#43991=CARTESIAN_POINT ( 'NONE',  ( 11.99999999999999822, 62.50329211542494789, -41.76937507738723099 ) ) ;
#44002=CIRCLE ( 'NONE', #33827, 31.99999999999998579 ) ;
#44006=ORIENTED_EDGE ( 'NONE', *, *, #39186, .T. ) ;
#44007=VERTEX_POINT ( 'NONE', #43202 ) ;
#44009=AXIS2_PLACEMENT_3D ( 'NONE', #11847, #19903, #8173 ) ;
#44023=VERTEX_POINT ( 'NONE', #42969 ) ;
#44027=AXIS2_PLACEMENT_3D ( 'NONE', #38883, #28325, #46460 ) ;
#44029=CYLINDRICAL_SURFACE ( 'NONE', #28421, 31.99999999999998579 ) ;
#44031=CIRCLE ( 'NONE', #33104, 31.99999999999998579 ) ;
#44033=EDGE_CURVE ( 'NONE', #36090, #20737, #48045, .T. ) ;
#44036=DIRECTION ( 'NONE',  ( 0.000000000000000000, 0.000000000000000000, 1.000000000000000000 ) ) ;
#44038=CIRCLE ( 'NONE', #33110, 82.00000000000000000 ) ;
#44040=ORIENTED_EDGE ( 'NONE', *, *, #11954, .F. ) ;
#44042=AXIS2_PLACEMENT_3D ( 'NONE', #20564, #35017, #27944 ) ;
#44043=CARTESIAN_POINT ( 'NONE',  ( 0.000000000000000000, -56.15606465354916566, -59.75363087400133111 ) ) ;
#44047=AXIS2_PLACEMENT_3D ( 'NONE', #24757, #16444, #2463 ) ;
#44048=DIRECTION ( 'NONE',  ( 0.000000000000000000, -0.9781476007338043566, 0.2079116908177651712 ) ) ;
#44052=AXIS2_PLACEMENT_3D ( 'NONE', #35345, #16512, #32176 ) ;
#44058=DIRECTION ( 'NONE',  ( 0.000000000000000000, -0.9135454576426015327, 0.4067366430757989315 ) ) ;
#44059=VERTEX_POINT ( 'NONE', #43682 ) ;
#44062=VERTEX_POINT ( 'NONE', #38825 ) ;
#44064=DIRECTION ( 'NONE',  ( 0.000000000000000000, 0.1045284632676459491, -0.9945218953682741780 ) ) ;
#44067=AXIS2_PLACEMENT_3D ( 'NONE', #32912, #40039, #43940 ) ;
#44069=VERTEX_POINT ( 'NONE', #20199 ) ;
#44071=CIRCLE ( 'NONE', #3388, 31.99999999999998934 ) ;
#44072=AXIS2_PLACEMENT_3D ( 'NONE', #5978, #31690, #46841 ) ;
#44075=CIRCLE ( 'NONE', #16620, 82.00000000000000000 ) ;
#44077=DIRECTION ( 'NONE',  ( -1.000000000000000000, -0.000000000000000000, -0.000000000000000000 ) ) ;
#44082=CARTESIAN_POINT ( 'NONE',  ( 11.99999999999999822, 65.59268652807263322, -36.72794159290169347 ) ) ;
#44083=ORIENTED_EDGE ( 'NONE', *, *, #12546, .F. ) ;
#44084=EDGE_CURVE ( 'NONE', #2861, #11520, #12156, .T. ) ;
#44089=CARTESIAN_POINT ( 'NONE',  ( 0.000000000000000000, 51.03279382321166224, -55.19960302592011914 ) ) ;
#44090=ORIENTED_EDGE ( 'NONE', *, *, #33230, .F. ) ;
#44099=EDGE_LOOP ( 'NONE', ( #42955, #33612, #3132, #6767 ) ) ;
#44100=EDGE_CURVE ( 'NONE', #31098, #32136, #41047, .T. ) ;
#44102=AXIS2_PLACEMENT_3D ( 'NONE', #30447, #11846, #41703 ) ;
#44103=CYLINDRICAL_SURFACE ( 'NONE', #33975, 31.99999999999998579 ) ;
#44105=AXIS2_PLACEMENT_3D ( 'NONE', #2338, #31988, #46899 ) ;
#44107=ADVANCED_FACE ( 'NONE', ( #29709 ), #3525, .T. ) ;
#44110=ORIENTED_EDGE ( 'NONE', *, *, #22478, .T. ) ;
#44113=DIRECTION ( 'NONE',  ( 0.000000000000000000, -1.000000000000000000, -1.301042606982602560E-15 ) ) ;
#44116=VECTOR ( 'NONE', #22300, 1000.000000000000000 ) ;
#44120=CARTESIAN_POINT ( 'NONE',  ( 11.99999999999999822, -2.946379043146863719, 75.11764819372146462 ) ) ;
#44121=AXIS2_PLACEMENT_3D ( 'NONE', #18279, #18032, #41066 ) ;
#44122=VECTOR ( 'NONE', #21737, 1000.000000000000000 ) ;
#44127=CARTESIAN_POINT ( 'NONE',  ( 0.000000000000000000, -73.72996012237429397, -14.67089635893794508 ) ) ;
#44130=ORIENTED_EDGE ( 'NONE', *, *, #34367, .F. ) ;
#44138=CIRCLE ( 'NONE', #23036, 31.99999999999998934 ) ;
#44140=ADVANCED_FACE ( 'NONE', ( #7195 ), #43919, .T. ) ;
#44149=DIRECTION ( 'NONE',  ( 0.000000000000000000, 0.8660254037844363761, -0.5000000000000039968 ) ) ;
#44163=ORIENTED_EDGE ( 'NONE', *, *, #47137, .F. ) ;
#44164=ORIENTED_EDGE ( 'NONE', *, *, #4685, .F. ) ;
#44169=FACE_OUTER_BOUND ( 'NONE', #47464, .T. ) ;
#44170=VERTEX_POINT ( 'NONE', #6480 ) ;
#44174=CARTESIAN_POINT ( 'NONE',  ( 0.000000000000000000, -55.20638768913797634, 51.02545421589302777 ) ) ;
#44176=CARTESIAN_POINT ( 'NONE',  ( 15.00000000000000000, 20.85821328998756385, 10.92862929874494249 ) ) ;
#44185=CARTESIAN_POINT ( 'NONE',  ( 12.00000000000000000, 9.615535125378766423, -24.73947219025917121 ) ) ;
#44189=AXIS2_PLACEMENT_3D ( 'NONE', #46280, #35741, #43089 ) ;
#44193=ORIENTED_EDGE ( 'NONE', *, *, #25890, .T. ) ;
#44196=AXIS2_PLACEMENT_3D ( 'NONE', #16142, #14748, #45998 ) ;
#44201=CARTESIAN_POINT ( 'NONE',  ( 0.000000000000000000, 41.76106447765489094, 62.50884508063442269 ) ) ;
#44203=EDGE_CURVE ( 'NONE', #15440, #7146, #36808, .T. ) ;
#44205=VECTOR ( 'NONE', #34585, 1000.000000000000000 ) ;
#44210=EDGE_LOOP ( 'NONE', ( #12721, #38371, #30639, #18545 ) ) ;
#44218=CARTESIAN_POINT ( 'NONE',  ( 11.99999999999999822, -55.38113227695820484, 54.21277698773656084 ) ) ;
#44219=DIRECTION ( 'NONE',  ( -1.000000000000000000, -0.000000000000000000, -0.000000000000000000 ) ) ;
#44222=VERTEX_POINT ( 'NONE', #37056 ) ;
#44223=CARTESIAN_POINT ( 'NONE',  ( 15.00000000000000000, -20.55727247249748402, -16.78983467731284307 ) ) ;
#44232=CIRCLE ( 'NONE', #37199, 82.00000000000000000 ) ;
#44233=CARTESIAN_POINT ( 'NONE',  ( 11.99999999999999822, 41.19522573413826194, -65.64334221924865176 ) ) ;
#44234=DIRECTION ( 'NONE',  ( 1.000000000000000000, 0.000000000000000000, 0.000000000000000000 ) ) ;
#44235=EDGE_CURVE ( 'NONE', #37423, #36132, #48312, .T. ) ;
#44250=DIRECTION ( 'NONE',  ( -1.000000000000000000, 0.000000000000000000, -0.000000000000000000 ) ) ;
#44259=DIRECTION ( 'NONE',  ( 1.000000000000000000, 0.000000000000000000, 0.000000000000000000 ) ) ;
#44263=EDGE_CURVE ( 'NONE', #2304, #8879, #34571, .T. ) ;
#44264=DIRECTION ( 'NONE',  ( -1.000000000000000000, -0.000000000000000000, -0.000000000000000000 ) ) ;
#44266=VECTOR ( 'NONE', #33579, 1000.000000000000000 ) ;
#44272=DIRECTION ( 'NONE',  ( 0.000000000000000000, 0.000000000000000000, 1.000000000000000000 ) ) ;
#44275=DIRECTION ( 'NONE',  ( 0.000000000000000000, -0.2334453638559128297, 0.9723699203976748917 ) ) ;
#44276=CARTESIAN_POINT ( 'NONE',  ( 11.99999999999999822, -73.72996012237449293, 14.67089635893687571 ) ) ;
#44277=DIRECTION ( 'NONE',  ( -1.000000000000000000, -0.000000000000000000, -0.000000000000000000 ) ) ;
#44278=ORIENTED_EDGE ( 'NONE', *, *, #28410, .F. ) ;
#44284=ORIENTED_EDGE ( 'NONE', *, *, #38190, .F. ) ;
#44287=DIRECTION ( 'NONE',  ( 0.000000000000000000, 0.07845909572784512398, -0.9969173337331279638 ) ) ;
#44311=FACE_OUTER_BOUND ( 'NONE', #6014, .T. ) ;
#44313=DIRECTION ( 'NONE',  ( 0.000000000000000000, 0.000000000000000000, 1.000000000000000000 ) ) ;
#44317=ORIENTED_EDGE ( 'NONE', *, *, #35238, .T. ) ;
#44318=CIRCLE ( 'NONE', #27146, 31.99999999999998579 ) ;
#44325=ORIENTED_EDGE ( 'NONE', *, *, #31749, .T. ) ;
#44328=AXIS2_PLACEMENT_3D ( 'NONE', #34845, #35085, #5472 ) ;
#44329=ORIENTED_EDGE ( 'NONE', *, *, #21984, .F. ) ;
#44332=LINE ( 'NONE', #3447, #18365 ) ;
#44335=DIRECTION ( 'NONE',  ( -1.000000000000000000, 0.000000000000000000, -0.000000000000000000 ) ) ;
#44336=LINE ( 'NONE', #41396, #2828 ) ;
#44338=CARTESIAN_POINT ( 'NONE',  ( 11.99999999999999822, 0.000000000000000000, 0.000000000000000000 ) ) ;
#44341=DIRECTION ( 'NONE',  ( -1.000000000000000000, 0.000000000000000000, 0.000000000000000000 ) ) ;
#44345=ORIENTED_EDGE ( 'NONE', *, *, #35353, .T. ) ;
#44348=ORIENTED_EDGE ( 'NONE', *, *, #22147, .T. ) ;
#44364=VECTOR ( 'NONE', #10223, 1000.000000000000114 ) ;
#44365=ORIENTED_EDGE ( 'NONE', *, *, #22872, .F. ) ;
#44368=CARTESIAN_POINT ( 'NONE',  ( 11.99999999999999822, -77.19088730480528682, 6.903761155837505825 ) ) ;
#44374=ORIENTED_EDGE ( 'NONE', *, *, #800, .T. ) ;
#44378=EDGE_CURVE ( 'NONE', #25935, #27340, #48090, .T. ) ;
#44384=ORIENTED_EDGE ( 'NONE', *, *, #19755, .F. ) ;
#44387=CARTESIAN_POINT ( 'NONE',  ( 11.99999999999999822, 50.23322058963442061, -64.81221759200288091 ) ) ;
#44390=ORIENTED_EDGE ( 'NONE', *, *, #15375, .T. ) ;
#44392=CARTESIAN_POINT ( 'NONE',  ( 0.000000000000000000, 55.20638768913760686, 51.02545421589343988 ) ) ;
#44401=ORIENTED_EDGE ( 'NONE', *, *, #22937, .F. ) ;
#44409=ORIENTED_EDGE ( 'NONE', *, *, #44033, .F. ) ;
#44414=CIRCLE ( 'NONE', #29563, 31.99999999999998934 ) ;
#44430=EDGE_CURVE ( 'NONE', #24067, #44556, #36349, .T. ) ;
#44431=CARTESIAN_POINT ( 'NONE',  ( 11.99999999999999822, 0.000000000000000000, 0.000000000000000000 ) ) ;
#44434=ORIENTED_EDGE ( 'NONE', *, *, #46739, .T. ) ;
#44436=EDGE_CURVE ( 'NONE', #43138, #19294, #19077, .T. ) ;
#44437=EDGE_CURVE ( 'NONE', #30049, #39130, #25323, .T. ) ;
#44445=VERTEX_POINT ( 'NONE', #17181 ) ;
#44446=DIRECTION ( 'NONE',  ( 0.000000000000000000, 0.000000000000000000, 1.000000000000000000 ) ) ;
#44450=DIRECTION ( 'NONE',  ( -1.000000000000000000, -0.000000000000000000, -0.000000000000000000 ) ) ;
#44451=DIRECTION ( 'NONE',  ( 1.000000000000000000, 0.000000000000000000, 0.000000000000000000 ) ) ;
#44455=DIRECTION ( 'NONE',  ( 0.000000000000000000, 0.000000000000000000, 1.000000000000000000 ) ) ;
#44464=AXIS2_PLACEMENT_3D ( 'NONE', #4490, #22840, #29943 ) ;
#44468=CARTESIAN_POINT ( 'NONE',  ( 11.99999999999999822, 80.28980883073758434, 16.65972982744962749 ) ) ;
#44470=EDGE_CURVE ( 'NONE', #25450, #41683, #33122, .T. ) ;
#44472=DIRECTION ( 'NONE',  ( 1.000000000000000000, -0.000000000000000000, 0.000000000000000000 ) ) ;
#44477=CARTESIAN_POINT ( 'NONE',  ( 6.000000000000000000, 10.30890764327501152, -81.34940948281325745 ) ) ;
#44480=( GEOMETRIC_REPRESENTATION_CONTEXT ( 3 ) GLOBAL_UNCERTAINTY_ASSIGNED_CONTEXT ( ( #45766 ) ) GLOBAL_UNIT_ASSIGNED_CONTEXT ( ( #41851, #30107, #37680 ) ) REPRESENTATION_CONTEXT ( 'NONE', 'WORKASPACE' ) );
#44481=CARTESIAN_POINT ( 'NONE',  ( 0.000000000000000000, 66.50666863322055633, -39.78640506895536078 ) ) ;
#44484=CARTESIAN_POINT ( 'NONE',  ( -10.00000000000000000, 0.000000000000000000, 0.000000000000000000 ) ) ;
#44485=DIRECTION ( 'NONE',  ( -1.000000000000000000, 0.000000000000000000, 0.000000000000000000 ) ) ;
#44490=ORIENTED_EDGE ( 'NONE', *, *, #322, .T. ) ;
#44491=EDGE_LOOP ( 'NONE', ( #8756, #8632, #22237, #1457 ) ) ;
#44495=LINE ( 'NONE', #2891, #32713 ) ;
#44498=EDGE_LOOP ( 'NONE', ( #13115, #32707, #33712, #20710 ) ) ;
#44501=DIRECTION ( 'NONE',  ( 0.000000000000000000, 0.6494480483301848794, -0.7604059656000299317 ) ) ;
#44503=ORIENTED_EDGE ( 'NONE', *, *, #38127, .T. ) ;
#44508=VERTEX_POINT ( 'NONE', #36990 ) ;
#44510=DIRECTION ( 'NONE',  ( 0.000000000000000000, -0.9510565162951500895, -0.3090169943749582204 ) ) ;
#44517=ADVANCED_FACE ( 'NONE', ( #10586 ), #28706, .T. ) ;
#44520=VERTEX_POINT ( 'NONE', #25729 ) ;
#44521=DIRECTION ( 'NONE',  ( -1.000000000000000000, 0.000000000000000000, 0.000000000000000000 ) ) ;
#44532=EDGE_CURVE ( 'NONE', #17161, #36444, #8914, .T. ) ;
#44535=DIRECTION ( 'NONE',  ( -1.000000000000000000, 0.000000000000000000, -0.000000000000000000 ) ) ;
#44536=DIRECTION ( 'NONE',  ( 0.000000000000000000, 0.000000000000000000, 1.000000000000000000 ) ) ;
#44538=CARTESIAN_POINT ( 'NONE',  ( 0.000000000000000000, 64.81221759200417409, -50.23322058963276504 ) ) ;
#44539=DIRECTION ( 'NONE',  ( 0.000000000000000000, -0.4067366430757989315, -0.9135454576426015327 ) ) ;
#44543=ORIENTED_EDGE ( 'NONE', *, *, #33177, .F. ) ;
#44546=CARTESIAN_POINT ( 'NONE',  ( 11.99999999999999822, 63.97538442413500093, -51.29473840253155714 ) ) ;
#44550=VECTOR ( 'NONE', #27688, 1000.000000000000227 ) ;
#44553=ORIENTED_EDGE ( 'NONE', *, *, #25343, .T. ) ;
#44556=VERTEX_POINT ( 'NONE', #3466 ) ;
#44559=CARTESIAN_POINT ( 'NONE',  ( 0.000000000000000000, -8.966570791701281351, 81.50828551894223040 ) ) ;
#44564=ORIENTED_EDGE ( 'NONE', *, *, #37125, .T. ) ;
#44565=ORIENTED_EDGE ( 'NONE', *, *, #11066, .F. ) ;
#44568=DIRECTION ( 'NONE',  ( 0.000000000000000000, 0.000000000000000000, 1.000000000000000000 ) ) ;
#44569=LINE ( 'NONE', #25713, #32951 ) ;
#44580=FACE_OUTER_BOUND ( 'NONE', #37657, .T. ) ;
#44581=DIRECTION ( 'NONE',  ( 0.000000000000000000, 0.5877852522924685852, 0.8090169943749506709 ) ) ;
#44587=EDGE_CURVE ( 'NONE', #10741, #41791, #7340, .T. ) ;
#44595=FACE_OUTER_BOUND ( 'NONE', #4969, .T. ) ;
#44598=DIRECTION ( 'NONE',  ( 0.000000000000000000, 0.7071067811865436870, 0.7071067811865513475 ) ) ;
#44603=DIRECTION ( 'NONE',  ( -1.000000000000000000, 0.000000000000000000, -0.000000000000000000 ) ) ;
#44608=VECTOR ( 'NONE', #9854, 1000.000000000000000 ) ;
#44609=ORIENTED_EDGE ( 'NONE', *, *, #13483, .T. ) ;
#44612=VERTEX_POINT ( 'NONE', #47758 ) ;
#44614=LINE ( 'NONE', #41202, #23654 ) ;
#44616=DIRECTION ( 'NONE',  ( 0.000000000000000000, 0.000000000000000000, 1.000000000000000000 ) ) ;
#44618=EDGE_CURVE ( 'NONE', #3340, #19509, #32369, .T. ) ;
#44619=PLANE ( 'NONE',  #10424 ) ;
#44620=VERTEX_POINT ( 'NONE', #48008 ) ;
#44621=VECTOR ( 'NONE', #41236, 1000.000000000000000 ) ;
#44639=DIRECTION ( 'NONE',  ( 0.000000000000000000, 0.3826834323650841752, 0.9238795325112891810 ) ) ;
#44643=DIRECTION ( 'NONE',  ( 0.000000000000000000, -0.9723699203976741146, -0.2334453638559160493 ) ) ;
#44652=DIRECTION ( 'NONE',  ( 0.000000000000000000, 0.3090169943749410675, 0.9510565162951556406 ) ) ;
#44654=DIRECTION ( 'NONE',  ( 1.000000000000000000, -0.000000000000000000, -0.000000000000000000 ) ) ;
#44656=FACE_OUTER_BOUND ( 'NONE', #43242, .T. ) ;
#44658=DIRECTION ( 'NONE',  ( 0.000000000000000000, 0.000000000000000000, 1.000000000000000000 ) ) ;
#44659=LINE ( 'NONE', #18474, #28306 ) ;
#44662=AXIS2_PLACEMENT_3D ( 'NONE', #5180, #8109, #46287 ) ;
#44669=CARTESIAN_POINT ( 'NONE',  ( 11.99999999999999822, -46.21855187248673502, 62.20884554314003623 ) ) ;
#44670=VECTOR ( 'NONE', #10940, 1000.000000000000227 ) ;
#44672=CIRCLE ( 'NONE', #8606, 31.99999999999999289 ) ;
#44678=CARTESIAN_POINT ( 'NONE',  ( 11.99999999999999822, 0.000000000000000000, 0.000000000000000000 ) ) ;
#44680=ORIENTED_EDGE ( 'NONE', *, *, #34579, .T. ) ;
#44690=CIRCLE ( 'NONE', #14195, 31.99999999999998579 ) ;
#44691=ORIENTED_EDGE ( 'NONE', *, *, #25062, .T. ) ;
#44693=DIRECTION ( 'NONE',  ( 1.000000000000000000, -0.000000000000000000, -0.000000000000000000 ) ) ;
#44696=AXIS2_PLACEMENT_3D ( 'NONE', #253, #8336, #41160 ) ;
#44701=CARTESIAN_POINT ( 'NONE',  ( 0.000000000000000000, 36.72794159290241822, 65.59268652807223532 ) ) ;
#44702=EDGE_CURVE ( 'NONE', #43790, #42577, #34519, .T. ) ;
#44704=CIRCLE ( 'NONE', #19671, 77.49900000000000944 ) ;
#44709=LINE ( 'NONE', #6793, #25131 ) ;
#44711=CARTESIAN_POINT ( 'NONE',  ( 11.99999999999999822, -20.40083707022829174, -72.35432306680507963 ) ) ;
#44714=DIRECTION ( 'NONE',  ( -1.000000000000000000, 0.000000000000000000, 0.000000000000000000 ) ) ;
#44723=EDGE_CURVE ( 'NONE', #7347, #39648, #21418, .T. ) ;
#44728=AXIS2_PLACEMENT_3D ( 'NONE', #22139, #41243, #11856 ) ;
#44733=AXIS2_PLACEMENT_3D ( 'NONE', #9142, #39005, #1798 ) ;
#44740=CARTESIAN_POINT ( 'NONE',  ( 11.99999999999999822, 74.18225833017889670, 34.94270380257665209 ) ) ;
#44743=VERTEX_POINT ( 'NONE', #41898 ) ;
#44745=ORIENTED_EDGE ( 'NONE', *, *, #2817, .F. ) ;
#44746=ORIENTED_EDGE ( 'NONE', *, *, #5715, .F. ) ;
#44748=AXIS2_PLACEMENT_3D ( 'NONE', #29592, #44521, #26172 ) ;
#44755=EDGE_CURVE ( 'NONE', #3949, #45561, #11316, .T. ) ;
#44757=CIRCLE ( 'NONE', #20514, 82.00000000000000000 ) ;
#44758=SURFACE_STYLE_USAGE ( .BOTH. , #15401 ) ;
#44760=ORIENTED_EDGE ( 'NONE', *, *, #1873, .T. ) ;
#44768=DIRECTION ( 'NONE',  ( 0.000000000000000000, -0.4539904997395542430, 0.8910065241883641241 ) ) ;
#44772=AXIS2_PLACEMENT_3D ( 'NONE', #2167, #9741, #17804 ) ;
#44777=DIRECTION ( 'NONE',  ( -1.000000000000000000, 0.000000000000000000, -0.000000000000000000 ) ) ;
#44783=EDGE_LOOP ( 'NONE', ( #39423, #43602, #37398, #1837 ) ) ;
#44785=DIRECTION ( 'NONE',  ( 0.000000000000000000, 0.000000000000000000, 1.000000000000000000 ) ) ;
#44791=EDGE_CURVE ( 'NONE', #23027, #25415, #8105, .T. ) ;
#44796=ORIENTED_EDGE ( 'NONE', *, *, #24289, .T. ) ;
#44798=VERTEX_POINT ( 'NONE', #530 ) ;
#44803=CARTESIAN_POINT ( 'NONE',  ( 11.99999999999999822, -71.87247863392384772, -39.47590169984923136 ) ) ;
#44813=VECTOR ( 'NONE', #47347, 1000.000000000000000 ) ;
#44814=EDGE_LOOP ( 'NONE', ( #11756, #8329, #46474, #23397 ) ) ;
#44815=EDGE_CURVE ( 'NONE', #43484, #1236, #16419, .T. ) ;
#44819=ORIENTED_EDGE ( 'NONE', *, *, #5429, .T. ) ;
#44820=CARTESIAN_POINT ( 'NONE',  ( 11.99999999999999822, 0.000000000000000000, 0.000000000000000000 ) ) ;
#44826=DIRECTION ( 'NONE',  ( 0.000000000000000000, 0.000000000000000000, 1.000000000000000000 ) ) ;
#44827=FACE_OUTER_BOUND ( 'NONE', #10733, .T. ) ;
#44831=DIRECTION ( 'NONE',  ( 1.000000000000000000, 0.000000000000000000, 0.000000000000000000 ) ) ;
#44833=AXIS2_PLACEMENT_3D ( 'NONE', #30349, #45497, #45269 ) ;
#44835=CYLINDRICAL_SURFACE ( 'NONE', #43470, 82.00000000000000000 ) ;
#44839=CARTESIAN_POINT ( 'NONE',  ( 11.99999999999999822, -65.64334221924937651, 41.19522573413711797 ) ) ;
#44850=CARTESIAN_POINT ( 'NONE',  ( 11.99999999999999822, 55.19960302592141232, -51.03279382321027668 ) ) ;
#44861=ADVANCED_FACE ( 'NONE', ( #24241 ), #5647, .T. ) ;
#44863=VERTEX_POINT ( 'NONE', #23757 ) ;
#44868=ADVANCED_FACE ( 'NONE', ( #16905 ), #19833, .F. ) ;
#44870=VECTOR ( 'NONE', #38039, 1000.000000000000000 ) ;
#44874=VERTEX_POINT ( 'NONE', #39175 ) ;
#44877=ADVANCED_FACE ( 'NONE', ( #31609 ), #27684, .T. ) ;
#44882=CARTESIAN_POINT ( 'NONE',  ( 0.000000000000000000, 11.30684508768339569, 76.66974797899841576 ) ) ;
#44884=ORIENTED_EDGE ( 'NONE', *, *, #39186, .F. ) ;
#44891=CARTESIAN_POINT ( 'NONE',  ( 0.000000000000000000, 0.000000000000000000, 0.000000000000000000 ) ) ;
#44895=DIRECTION ( 'NONE',  ( 0.000000000000000000, 0.000000000000000000, 1.000000000000000000 ) ) ;
#44899=DIRECTION ( 'NONE',  ( -1.000000000000000000, -0.000000000000000000, 0.000000000000000000 ) ) ;
#44909=DIRECTION ( 'NONE',  ( 0.000000000000000000, 0.000000000000000000, 1.000000000000000000 ) ) ;
#44916=ORIENTED_EDGE ( 'NONE', *, *, #23105, .T. ) ;
#44919=AXIS2_PLACEMENT_3D ( 'NONE', #5188, #20103, #43103 ) ;
#44920=CIRCLE ( 'NONE', #366, 31.99999999999998224 ) ;
#44923=VECTOR ( 'NONE', #22356, 1000.000000000000000 ) ;
#44929=ADVANCED_FACE ( 'NONE', ( #16661 ), #46532, .T. ) ;
#44930=DIRECTION ( 'NONE',  ( -1.000000000000000000, 0.000000000000000000, 0.000000000000000000 ) ) ;
#44931=ADVANCED_FACE ( 'NONE', ( #33273 ), #17851, .T. ) ;
#44940=LINE ( 'NONE', #11423, #10275 ) ;
#44942=CYLINDRICAL_SURFACE ( 'NONE', #2450, 82.00000000000000000 ) ;
#44945=CARTESIAN_POINT ( 'NONE',  ( 0.000000000000000000, -73.95703589263990807, 23.16143007188399139 ) ) ;
#44946=VERTEX_POINT ( 'NONE', #29108 ) ;
#44952=CARTESIAN_POINT ( 'NONE',  ( 15.00000000000000000, -3.948201729842032215, 23.21447184625297666 ) ) ;
#44953=PLANE ( 'NONE',  #12773 ) ;
#44956=LINE ( 'NONE', #33681, #16408 ) ;
#44960=EDGE_CURVE ( 'NONE', #47874, #41381, #25433, .T. ) ;
#44974=DIRECTION ( 'NONE',  ( 0.000000000000000000, 0.000000000000000000, 1.000000000000000000 ) ) ;
#44975=DIRECTION ( 'NONE',  ( 0.000000000000000000, 0.9945218953682732899, -0.1045284632676548031 ) ) ;
#44978=CARTESIAN_POINT ( 'NONE',  ( 11.99999999999999822, -51.02545421589285723, -55.20638768913812555 ) ) ;
#44980=ORIENTED_EDGE ( 'NONE', *, *, #3962, .T. ) ;
#44989=VECTOR ( 'NONE', #31897, 1000.000000000000227 ) ;
#44993=ORIENTED_EDGE ( 'NONE', *, *, #32758, .T. ) ;
#44995=EDGE_CURVE ( 'NONE', #14629, #5793, #23797, .T. ) ;
#44998=AXIS2_PLACEMENT_3D ( 'NONE', #252, #30140, #45064 ) ;
#45001=ORIENTED_EDGE ( 'NONE', *, *, #16214, .T. ) ;
#45003=ORIENTED_EDGE ( 'NONE', *, *, #9276, .T. ) ;
#45008=VECTOR ( 'NONE', #34879, 1000.000000000000000 ) ;
#45010=CARTESIAN_POINT ( 'NONE',  ( 0.000000000000000000, -46.54456581323762521, -59.03342792756313884 ) ) ;
#45011=AXIS2_PLACEMENT_3D ( 'NONE', #22625, #12116, #37803 ) ;
#45013=ORIENTED_EDGE ( 'NONE', *, *, #45215, .T. ) ;
#45017=ORIENTED_EDGE ( 'NONE', *, *, #14405, .F. ) ;
#45023=DIRECTION ( 'NONE',  ( 0.000000000000000000, 0.000000000000000000, 1.000000000000000000 ) ) ;
#45030=CARTESIAN_POINT ( 'NONE',  ( 0.000000000000000000, 51.02545421589324803, 55.20638768913779870 ) ) ;
#45033=DIRECTION ( 'NONE',  ( -1.000000000000000000, 0.000000000000000000, 0.000000000000000000 ) ) ;
#45039=AXIS2_PLACEMENT_3D ( 'NONE', #41007, #33882, #47739 ) ;
#45043=EDGE_CURVE ( 'NONE', #32940, #6721, #40147, .T. ) ;
#45045=DIRECTION ( 'NONE',  ( 0.000000000000000000, 0.3090169943749572767, 0.9510565162951503115 ) ) ;
#45049=AXIS2_PLACEMENT_3D ( 'NONE', #26430, #19309, #45494 ) ;
#45050=ORIENTED_EDGE ( 'NONE', *, *, #30472, .T. ) ;
#45051=LINE ( 'NONE', #7599, #17098 ) ;
#45056=EDGE_CURVE ( 'NONE', #17996, #37652, #14406, .T. ) ;
#45057=DIRECTION ( 'NONE',  ( -1.000000000000000000, -0.000000000000000000, -0.000000000000000000 ) ) ;
#45058=VECTOR ( 'NONE', #30319, 1000.000000000000114 ) ;
#45060=VERTEX_POINT ( 'NONE', #32317 ) ;
#45063=VECTOR ( 'NONE', #14192, 1000.000000000000000 ) ;
#45064=DIRECTION ( 'NONE',  ( 0.000000000000000000, 0.8090169943749433434, -0.5877852522924786882 ) ) ;
#45068=DIRECTION ( 'NONE',  ( 0.000000000000000000, -0.3090169943749560555, -0.9510565162951506446 ) ) ;
#45069=ORIENTED_EDGE ( 'NONE', *, *, #3075, .F. ) ;
#45072=ORIENTED_EDGE ( 'NONE', *, *, #35819, .F. ) ;
#45079=DIRECTION ( 'NONE',  ( -1.000000000000000000, 0.000000000000000000, 0.000000000000000000 ) ) ;
#45081=DIRECTION ( 'NONE',  ( -1.000000000000000000, -0.000000000000000000, 0.000000000000000000 ) ) ;
#45085=AXIS2_PLACEMENT_3D ( 'NONE', #26610, #37140, #41073 ) ;
#45111=CYLINDRICAL_SURFACE ( 'NONE', #21392, 31.99999999999998579 ) ;
#45112=ORIENTED_EDGE ( 'NONE', *, *, #17880, .T. ) ;
#45117=DIRECTION ( 'NONE',  ( -1.000000000000000000, -0.000000000000000000, 0.000000000000000000 ) ) ;
#45120=EDGE_LOOP ( 'NONE', ( #5799, #560, #17129, #4396 ) ) ;
#45122=DIRECTION ( 'NONE',  ( -1.000000000000000000, -0.000000000000000000, -0.000000000000000000 ) ) ;
#45124=CARTESIAN_POINT ( 'NONE',  ( 11.99999999999999822, -62.50884508063395373, -41.76106447765554464 ) ) ;
#45134=AXIS2_PLACEMENT_3D ( 'NONE', #23647, #33698, #42253 ) ;
#45138=ORIENTED_EDGE ( 'NONE', *, *, #27140, .F. ) ;
#45140=FACE_OUTER_BOUND ( 'NONE', #19767, .T. ) ;
#45142=DIRECTION ( 'NONE',  ( -1.000000000000000000, -0.000000000000000000, 0.000000000000000000 ) ) ;
#45147=EDGE_LOOP ( 'NONE', ( #26558, #43797, #28908, #34135 ) ) ;
#45155=AXIS2_PLACEMENT_3D ( 'NONE', #33286, #44058, #44539 ) ;
#45157=CARTESIAN_POINT ( 'NONE',  ( 5.999999999999999112, -64.81221759200306565, -50.23322058963418613 ) ) ;
#45163=ORIENTED_EDGE ( 'NONE', *, *, #12599, .F. ) ;
#45168=ORIENTED_EDGE ( 'NONE', *, *, #26483, .T. ) ;
#45174=EDGE_LOOP ( 'NONE', ( #2176, #33192, #22660, #20740 ) ) ;
#45177=ORIENTED_EDGE ( 'NONE', *, *, #17633, .F. ) ;
#45182=DIRECTION ( 'NONE',  ( -1.000000000000000000, 0.000000000000000000, 0.000000000000000000 ) ) ;
#45184=LINE ( 'NONE', #4064, #36106 ) ;
#45190=DIRECTION ( 'NONE',  ( 0.000000000000000000, 0.9510565162951544194, -0.3090169943749446757 ) ) ;
#45193=DIRECTION ( 'NONE',  ( 0.000000000000000000, 0.000000000000000000, 1.000000000000000000 ) ) ;
#45194=FACE_OUTER_BOUND ( 'NONE', #34298, .T. ) ;
#45196=DIRECTION ( 'NONE',  ( 0.000000000000000000, -0.9876883405951394357, 0.1564344650402205716 ) ) ;
#45197=DIRECTION ( 'NONE',  ( -1.000000000000000000, 0.000000000000000000, 0.000000000000000000 ) ) ;
#45215=EDGE_CURVE ( 'NONE', #34943, #25765, #388, .T. ) ;
#45216=CYLINDRICAL_SURFACE ( 'NONE', #45085, 82.00000000000000000 ) ;
#45219=EDGE_CURVE ( 'NONE', #43548, #18388, #29288, .T. ) ;
#45222=DIRECTION ( 'NONE',  ( -1.000000000000000000, 0.000000000000000000, 0.000000000000000000 ) ) ;
#45225=EDGE_CURVE ( 'NONE', #37785, #12329, #42074, .T. ) ;
#45227=DIRECTION ( 'NONE',  ( -1.000000000000000000, -0.000000000000000000, -0.000000000000000000 ) ) ;
#45228=DIRECTION ( 'NONE',  ( 0.000000000000000000, 0.000000000000000000, 1.000000000000000000 ) ) ;
#45234=CARTESIAN_POINT ( 'NONE',  ( 0.000000000000000000, 26.02418014898407961, -70.52718814184231633 ) ) ;
#45239=CARTESIAN_POINT ( 'NONE',  ( 0.000000000000000000, 81.50828551894240093, -8.966570791699810528 ) ) ;
#45245=ORIENTED_EDGE ( 'NONE', *, *, #44263, .T. ) ;
#45246=CIRCLE ( 'NONE', #19439, 31.99999999999998934 ) ;
#45247=LINE ( 'NONE', #23447, #15717 ) ;
#45249=CYLINDRICAL_SURFACE ( 'NONE', #46980, 77.49899999999999523 ) ;
#45254=EDGE_LOOP ( 'NONE', ( #18668, #40902, #14001, #34743 ) ) ;
#45257=CARTESIAN_POINT ( 'NONE',  ( 15.00000000000000000, 0.000000000000000000, 0.000000000000000000 ) ) ;
#45258=DIRECTION ( 'NONE',  ( 1.000000000000000000, -0.000000000000000000, 0.000000000000000000 ) ) ;
#45265=CIRCLE ( 'NONE', #42931, 82.00000000000000000 ) ;
#45269=DIRECTION ( 'NONE',  ( 0.000000000000000000, -0.7604059656000369261, 0.6494480483301767748 ) ) ;
#45270=AXIS2_PLACEMENT_3D ( 'NONE', #4088, #3841, #45434 ) ;
#45271=CARTESIAN_POINT ( 'NONE',  ( 0.000000000000000000, -77.16300072079681627, 27.74655509720641433 ) ) ;
#45277=FACE_OUTER_BOUND ( 'NONE', #5044, .T. ) ;
#45293=CYLINDRICAL_SURFACE ( 'NONE', #30931, 82.00000000000000000 ) ;
#45300=DIRECTION ( 'NONE',  ( -1.000000000000000000, 0.000000000000000000, 0.000000000000000000 ) ) ;
#45301=VERTEX_POINT ( 'NONE', #27891 ) ;
#45304=CARTESIAN_POINT ( 'NONE',  ( 15.00000000000000000, 22.07842321921492612, 8.187992925817123790 ) ) ;
#45311=FACE_OUTER_BOUND ( 'NONE', #4728, .T. ) ;
#45313=CYLINDRICAL_SURFACE ( 'NONE', #19265, 77.49899999999999523 ) ;
#45316=DIRECTION ( 'NONE',  ( 0.000000000000000000, -0.5000000000000038858, -0.8660254037844363761 ) ) ;
#45318=ADVANCED_FACE ( 'NONE', ( #12695 ), #12226, .T. ) ;
#45331=VERTEX_POINT ( 'NONE', #17079 ) ;
#45332=AXIS2_PLACEMENT_3D ( 'NONE', #36738, #17898, #33557 ) ;
#45335=EDGE_CURVE ( 'NONE', #6202, #30049, #8523, .T. ) ;
#45337=DIRECTION ( 'NONE',  ( 0.000000000000000000, 0.7071067811865439090, 0.7071067811865512365 ) ) ;
#45343=ORIENTED_EDGE ( 'NONE', *, *, #10454, .T. ) ;
#45344=EDGE_CURVE ( 'NONE', #6863, #1013, #39621, .T. ) ;
#45350=ORIENTED_EDGE ( 'NONE', *, *, #14765, .T. ) ;
#45351=CIRCLE ( 'NONE', #5496, 82.00000000000000000 ) ;
#45356=VECTOR ( 'NONE', #27320, 1000.000000000000114 ) ;
#45361=ORIENTED_EDGE ( 'NONE', *, *, #782, .F. ) ;
#45370=FACE_OUTER_BOUND ( 'NONE', #4495, .T. ) ;
#45374=CARTESIAN_POINT ( 'NONE',  ( 0.000000000000000000, 0.000000000000000000, 0.000000000000000000 ) ) ;
#45377=DIRECTION ( 'NONE',  ( 0.000000000000000000, 0.000000000000000000, 1.000000000000000000 ) ) ;
#45380=FACE_OUTER_BOUND ( 'NONE', #3076, .T. ) ;
#45382=CYLINDRICAL_SURFACE ( 'NONE', #47387, 77.49899999999999523 ) ;
#45383=ORIENTED_EDGE ( 'NONE', *, *, #21155, .T. ) ;
#45386=AXIS2_PLACEMENT_3D ( 'NONE', #21348, #36522, #17428 ) ;
#45388=ORIENTED_EDGE ( 'NONE', *, *, #861, .T. ) ;
#45394=AXIS2_PLACEMENT_3D ( 'NONE', #746, #38705, #5167 ) ;
#45402=EDGE_CURVE ( 'NONE', #39044, #6346, #35543, .T. ) ;
#45404=DIRECTION ( 'NONE',  ( -1.000000000000000000, -0.000000000000000000, 0.000000000000000000 ) ) ;
#45406=EDGE_CURVE ( 'NONE', #4856, #15331, #22269, .T. ) ;
#45410=ORIENTED_EDGE ( 'NONE', *, *, #6188, .T. ) ;
#45414=DIRECTION ( 'NONE',  ( -1.000000000000000000, 0.000000000000000000, -0.000000000000000000 ) ) ;
#45416=CYLINDRICAL_SURFACE ( 'NONE', #16080, 31.99999999999998579 ) ;
#45427=ORIENTED_EDGE ( 'NONE', *, *, #12912, .F. ) ;
#45429=CARTESIAN_POINT ( 'NONE',  ( 0.000000000000000000, -64.81221759200306565, -50.23322058963418613 ) ) ;
#45434=DIRECTION ( 'NONE',  ( 0.000000000000000000, 0.000000000000000000, 1.000000000000000000 ) ) ;
#45442=CARTESIAN_POINT ( 'NONE',  ( 0.000000000000000000, 0.000000000000000000, 0.000000000000000000 ) ) ;
#45443=ADVANCED_FACE ( 'NONE', ( #36157 ), #22135, .T. ) ;
#45444=CYLINDRICAL_SURFACE ( 'NONE', #16161, 77.49899999999999523 ) ;
#45448=ORIENTED_EDGE ( 'NONE', *, *, #44960, .T. ) ;
#45453=DIRECTION ( 'NONE',  ( -1.000000000000000000, 0.000000000000000000, 0.000000000000000000 ) ) ;
#45460=EDGE_CURVE ( 'NONE', #21369, #13195, #43521, .T. ) ;
#45461=ORIENTED_EDGE ( 'NONE', *, *, #8008, .T. ) ;
#45468=VERTEX_POINT ( 'NONE', #2614 ) ;
#45470=ADVANCED_FACE ( 'NONE', ( #32501 ), #47427, .T. ) ;
#45471=ORIENTED_EDGE ( 'NONE', *, *, #32332, .T. ) ;
#45474=AXIS2_PLACEMENT_3D ( 'NONE', #5573, #9241, #20489 ) ;
#45475=DIRECTION ( 'NONE',  ( 0.000000000000000000, 0.9969173337331276308, 0.07845909572784864894 ) ) ;
#45476=FACE_OUTER_BOUND ( 'NONE', #4381, .T. ) ;
#45478=EDGE_LOOP ( 'NONE', ( #22043, #10680, #42474, #6067 ) ) ;
#45480=CARTESIAN_POINT ( 'NONE',  ( 0.000000000000000000, -10.30890764327441289, 81.34940948281332851 ) ) ;
#45494=DIRECTION ( 'NONE',  ( 0.000000000000000000, 0.1564344650402311743, -0.9876883405951376593 ) ) ;
#45497=DIRECTION ( 'NONE',  ( -1.000000000000000000, 0.000000000000000000, 0.000000000000000000 ) ) ;
#45502=EDGE_CURVE ( 'NONE', #19364, #32361, #16259, .T. ) ;
#45512=ORIENTED_EDGE ( 'NONE', *, *, #44587, .T. ) ;
#45514=ORIENTED_EDGE ( 'NONE', *, *, #26197, .F. ) ;
#45527=AXIS2_PLACEMENT_3D ( 'NONE', #11234, #41104, #7561 ) ;
#45528=DIRECTION ( 'NONE',  ( -1.000000000000000000, -0.000000000000000000, -0.000000000000000000 ) ) ;
#45531=ORIENTED_EDGE ( 'NONE', *, *, #10454, .F. ) ;
#45539=ORIENTED_EDGE ( 'NONE', *, *, #23713, .F. ) ;
#45540=CARTESIAN_POINT ( 'NONE',  ( 12.00000000000000000, -22.32062822937488988, -14.36278369418800160 ) ) ;
#45541=CARTESIAN_POINT ( 'NONE',  ( 11.99999999999999822, 0.000000000000000000, 0.000000000000000000 ) ) ;
#45546=DIRECTION ( 'NONE',  ( -1.000000000000000000, 0.000000000000000000, 0.000000000000000000 ) ) ;
#45559=ORIENTED_EDGE ( 'NONE', *, *, #6749, .T. ) ;
#45560=VECTOR ( 'NONE', #47013, 1000.000000000000000 ) ;
#45561=VERTEX_POINT ( 'NONE', #34344 ) ;
#45563=FACE_BOUND ( 'NONE', #44498, .T. ) ;
#45574=ADVANCED_FACE ( 'NONE', ( #23110 ), #30954, .F. ) ;
#45575=AXIS2_PLACEMENT_3D ( 'NONE', #15971, #30911, #22581 ) ;
#45577=ORIENTED_EDGE ( 'NONE', *, *, #22147, .F. ) ;
#45578=EDGE_CURVE ( 'NONE', #38615, #4357, #16052, .T. ) ;
#45580=EDGE_LOOP ( 'NONE', ( #10287, #46659, #1413, #32936 ) ) ;
#45582=DIRECTION ( 'NONE',  ( -1.000000000000000000, 0.000000000000000000, 0.000000000000000000 ) ) ;
#45586=EDGE_CURVE ( 'NONE', #35673, #21593, #820, .T. ) ;
#45587=VECTOR ( 'NONE', #17869, 1000.000000000000000 ) ;
#45594=EDGE_LOOP ( 'NONE', ( #19513, #37407, #13283, #23697 ) ) ;
#45600=CIRCLE ( 'NONE', #22930, 82.00000000000000000 ) ;
#45602=EDGE_CURVE ( 'NONE', #3020, #46849, #11614, .T. ) ;
#45604=CIRCLE ( 'NONE', #3380, 31.99999999999998579 ) ;
#45606=LINE ( 'NONE', #29711, #28210 ) ;
#45607=ORIENTED_EDGE ( 'NONE', *, *, #38021, .T. ) ;
#45608=CARTESIAN_POINT ( 'NONE',  ( 11.99999999999999822, 0.000000000000000000, 77.49899999999999523 ) ) ;
#45613=CARTESIAN_POINT ( 'NONE',  ( 0.000000000000000000, 33.71516098798849015, -74.74816331893393340 ) ) ;
#45615=VECTOR ( 'NONE', #18936, 1000.000000000000000 ) ;
#45616=CARTESIAN_POINT ( 'NONE',  ( 15.00000000000000000, 23.49999999999999645, -1.500000000000003997 ) ) ;
#45617=CARTESIAN_POINT ( 'NONE',  ( 11.99999999999999822, -75.54627589209931671, -17.28742895386162814 ) ) ;
#45622=AXIS2_PLACEMENT_3D ( 'NONE', #8922, #20914, #20412 ) ;
#45628=VERTEX_POINT ( 'NONE', #593 ) ;
#45631=EDGE_CURVE ( 'NONE', #36257, #27089, #6692, .T. ) ;
#45636=CIRCLE ( 'NONE', #14380, 77.49899999999999523 ) ;
#45638=VERTEX_POINT ( 'NONE', #27033 ) ;
#45639=ORIENTED_EDGE ( 'NONE', *, *, #32874, .F. ) ;
#45641=EDGE_LOOP ( 'NONE', ( #6648, #23940, #28387, #23935 ) ) ;
#45642=EDGE_CURVE ( 'NONE', #526, #31086, #41967, .T. ) ;
#45644=EDGE_CURVE ( 'NONE', #31959, #39227, #12957, .T. ) ;
#45646=AXIS2_PLACEMENT_3D ( 'NONE', #8734, #25949, #16570 ) ;
#45647=LINE ( 'NONE', #12369, #13641 ) ;
#45650=AXIS2_PLACEMENT_3D ( 'NONE', #25613, #21710, #40557 ) ;
#45652=ORIENTED_EDGE ( 'NONE', *, *, #4809, .T. ) ;
#45656=VERTEX_POINT ( 'NONE', #9609 ) ;
#45657=ORIENTED_EDGE ( 'NONE', *, *, #46084, .F. ) ;
#45660=FACE_OUTER_BOUND ( 'NONE', #20696, .T. ) ;
#45661=ORIENTED_EDGE ( 'NONE', *, *, #37459, .T. ) ;
#45667=DIRECTION ( 'NONE',  ( 0.000000000000000000, 0.000000000000000000, 1.000000000000000000 ) ) ;
#45668=DIRECTION ( 'NONE',  ( -1.000000000000000000, 0.000000000000000000, 0.000000000000000000 ) ) ;
#45673=CARTESIAN_POINT ( 'NONE',  ( 11.99999999999999822, -51.03279382321048985, -55.19960302592120627 ) ) ;
#45676=AXIS2_PLACEMENT_3D ( 'NONE', #5175, #42620, #35745 ) ;
#45677=FACE_OUTER_BOUND ( 'NONE', #41922, .T. ) ;
#45678=VERTEX_POINT ( 'NONE', #24312 ) ;
#45682=AXIS2_PLACEMENT_3D ( 'NONE', #14027, #28950, #43887 ) ;
#45685=DIRECTION ( 'NONE',  ( 1.000000000000000000, -0.000000000000000000, -0.000000000000000000 ) ) ;
#45686=DIRECTION ( 'NONE',  ( -1.000000000000000000, -0.000000000000000000, 0.000000000000000000 ) ) ;
#45687=EDGE_CURVE ( 'NONE', #25899, #16268, #1202, .T. ) ;
#45695=DIRECTION ( 'NONE',  ( -1.000000000000000000, -0.000000000000000000, -0.000000000000000000 ) ) ;
#45697=EDGE_CURVE ( 'NONE', #12035, #43548, #10608, .T. ) ;
#45698=ORIENTED_EDGE ( 'NONE', *, *, #9005, .F. ) ;
#45700=EDGE_CURVE ( 'NONE', #14857, #1751, #37950, .T. ) ;
#45701=DIRECTION ( 'NONE',  ( 0.000000000000000000, 0.000000000000000000, 1.000000000000000000 ) ) ;
#45702=AXIS2_PLACEMENT_3D ( 'NONE', #18525, #33922, #41525 ) ;
#45703=ORIENTED_EDGE ( 'NONE', *, *, #23190, .T. ) ;
#45705=EDGE_LOOP ( 'NONE', ( #38361, #4253, #31568, #6216 ) ) ;
#45708=EDGE_LOOP ( 'NONE', ( #16391, #7953, #11705, #31337 ) ) ;
#45710=EDGE_LOOP ( 'NONE', ( #14478, #2428, #25954, #5375 ) ) ;
#45712=EDGE_CURVE ( 'NONE', #14617, #925, #28557, .T. ) ;
#45713=ORIENTED_EDGE ( 'NONE', *, *, #2288, .T. ) ;
#45717=VERTEX_POINT ( 'NONE', #20636 ) ;
#45722=DIRECTION ( 'NONE',  ( 0.000000000000000000, 0.8910065241883691201, -0.4539904997395446951 ) ) ;
#45726=AXIS2_PLACEMENT_3D ( 'NONE', #21424, #13606, #17755 ) ;
#45730=ORIENTED_EDGE ( 'NONE', *, *, #29086, .F. ) ;
#45736=CARTESIAN_POINT ( 'NONE',  ( 15.00000000000000000, 18.84667830672579569, -18.68964196561269375 ) ) ;
#45738=VERTEX_POINT ( 'NONE', #32389 ) ;
#45741=LINE ( 'NONE', #19766, #4811 ) ;
#45743=APPLICATION_CONTEXT ( 'automotive_design' ) ;
#45747=PLANE ( 'NONE',  #23975 ) ;
#45749=CIRCLE ( 'NONE', #12146, 31.99999999999998934 ) ;
#45750=CARTESIAN_POINT ( 'NONE',  ( 0.000000000000000000, 0.000000000000000000, 0.000000000000000000 ) ) ;
#45753=VECTOR ( 'NONE', #26776, 1000.000000000000000 ) ;
#45758=EDGE_CURVE ( 'NONE', #15795, #8980, #39499, .T. ) ;
#45760=CARTESIAN_POINT ( 'NONE',  ( 12.00000000000000000, -22.32062822937469093, 14.36278369418830181 ) ) ;
#45766=UNCERTAINTY_MEASURE_WITH_UNIT (LENGTH_MEASURE( 1.000000000000000082E-05 ), #41851, 'distance_accuracy_value', 'NONE');
#45767=DIRECTION ( 'NONE',  ( 0.000000000000000000, 0.000000000000000000, 1.000000000000000000 ) ) ;
#45777=VECTOR ( 'NONE', #28717, 1000.000000000000000 ) ;
#45778=EDGE_CURVE ( 'NONE', #10773, #5492, #20155, .T. ) ;
#45779=DIRECTION ( 'NONE',  ( 0.000000000000000000, 0.9510565162951543083, 0.3090169943749448977 ) ) ;
#45785=ORIENTED_EDGE ( 'NONE', *, *, #40843, .T. ) ;
#45786=EDGE_CURVE ( 'NONE', #27256, #18839, #17433, .T. ) ;
#45791=ORIENTED_EDGE ( 'NONE', *, *, #31637, .F. ) ;
#45792=CARTESIAN_POINT ( 'NONE',  ( 0.000000000000000000, -44.88180994100419952, 63.18004540533013369 ) ) ;
#45801=CIRCLE ( 'NONE', #40321, 77.49900000000000944 ) ;
#45802=ORIENTED_EDGE ( 'NONE', *, *, #14609, .F. ) ;
#45805=VERTEX_POINT ( 'NONE', #16491 ) ;
#45808=ORIENTED_EDGE ( 'NONE', *, *, #27479, .F. ) ;
#45812=LINE ( 'NONE', #12283, #27665 ) ;
#45821=ORIENTED_EDGE ( 'NONE', *, *, #39302, .T. ) ;
#45826=DIRECTION ( 'NONE',  ( 0.000000000000000000, 0.000000000000000000, 1.000000000000000000 ) ) ;
#45827=VECTOR ( 'NONE', #16237, 1000.000000000000000 ) ;
#45828=DIRECTION ( 'NONE',  ( 0.000000000000000000, 0.000000000000000000, 1.000000000000000000 ) ) ;
#45829=EDGE_CURVE ( 'NONE', #1236, #12511, #32842, .T. ) ;
#45830=VERTEX_POINT ( 'NONE', #25253 ) ;
#45832=AXIS2_PLACEMENT_3D ( 'NONE', #12234, #41124, #37926 ) ;
#45833=DIRECTION ( 'NONE',  ( -1.000000000000000000, 0.000000000000000000, -0.000000000000000000 ) ) ;
#45835=ORIENTED_EDGE ( 'NONE', *, *, #28276, .F. ) ;
#45836=ADVANCED_FACE ( 'NONE', ( #44595 ), #29435, .T. ) ;
#45842=AXIS2_PLACEMENT_3D ( 'NONE', #13397, #10200, #43020 ) ;
#45844=CYLINDRICAL_SURFACE ( 'NONE', #19050, 31.99999999999998579 ) ;
#45857=DIRECTION ( 'NONE',  ( -1.000000000000000000, -0.000000000000000000, -0.000000000000000000 ) ) ;
#45863=ORIENTED_EDGE ( 'NONE', *, *, #28580, .F. ) ;
#45864=ORIENTED_EDGE ( 'NONE', *, *, #7480, .T. ) ;
#45865=CARTESIAN_POINT ( 'NONE',  ( 11.99999999999999822, 0.000000000000000000, 0.000000000000000000 ) ) ;
#45870=VERTEX_POINT ( 'NONE', #6914 ) ;
#45872=CARTESIAN_POINT ( 'NONE',  ( 15.00000000000000000, 23.59884966291538078, 12.14883922797231008 ) ) ;
#45874=DIRECTION ( 'NONE',  ( 0.000000000000000000, -0.6494480483301739993, -0.7604059656000390355 ) ) ;
#45882=AXIS2_PLACEMENT_3D ( 'NONE', #13724, #6376, #2443 ) ;
#45889=FACE_OUTER_BOUND ( 'NONE', #3555, .T. ) ;
#45891=VERTEX_POINT ( 'NONE', #29176 ) ;
#45896=ORIENTED_EDGE ( 'NONE', *, *, #28580, .T. ) ;
#45901=LINE ( 'NONE', #22642, #14447 ) ;
#45904=VERTEX_POINT ( 'NONE', #36292 ) ;
#45914=AXIS2_PLACEMENT_3D ( 'NONE', #15239, #33345, #19132 ) ;
#45923=LINE ( 'NONE', #12390, #45356 ) ;
#45925=CARTESIAN_POINT ( 'NONE',  ( 0.000000000000000000, 0.000000000000000000, 0.000000000000000000 ) ) ;
#45930=LINE ( 'NONE', #42244, #2001 ) ;
#45935=LINE ( 'NONE', #23401, #25115 ) ;
#45939=EDGE_CURVE ( 'NONE', #43802, #4790, #25508, .T. ) ;
#45940=CARTESIAN_POINT ( 'NONE',  ( 11.99999999999999822, -67.80270845531855173, -46.11716303203260736 ) ) ;
#45943=DIRECTION ( 'NONE',  ( -1.000000000000000000, 0.000000000000000000, 0.000000000000000000 ) ) ;
#45951=EDGE_LOOP ( 'NONE', ( #8077, #40264, #41785, #47179 ) ) ;
#45952=VERTEX_POINT ( 'NONE', #15470 ) ;
#45954=ORIENTED_EDGE ( 'NONE', *, *, #1215, .F. ) ;
#45955=DIRECTION ( 'NONE',  ( 0.000000000000000000, 0.4067366430757889950, -0.9135454576426058626 ) ) ;
#45969=ORIENTED_EDGE ( 'NONE', *, *, #20953, .F. ) ;
#45972=ORIENTED_EDGE ( 'NONE', *, *, #40092, .T. ) ;
#45977=ORIENTED_EDGE ( 'NONE', *, *, #32822, .T. ) ;
#45978=FACE_OUTER_BOUND ( 'NONE', #13252, .T. ) ;
#45979=CARTESIAN_POINT ( 'NONE',  ( 6.000000000000000000, -22.90783923731685334, 78.73519480814945837 ) ) ;
#45984=ORIENTED_EDGE ( 'NONE', *, *, #32110, .T. ) ;
#45990=CARTESIAN_POINT ( 'NONE',  ( 11.99999999999999822, 0.000000000000000000, 0.000000000000000000 ) ) ;
#45991=CARTESIAN_POINT ( 'NONE',  ( 0.000000000000000000, -54.21277698773713638, 55.38113227695764351 ) ) ;
#45993=ORIENTED_EDGE ( 'NONE', *, *, #16976, .F. ) ;
#45995=CARTESIAN_POINT ( 'NONE',  ( 11.99999999999999822, 54.21277698773675979, 55.38113227695801299 ) ) ;
#45996=EDGE_CURVE ( 'NONE', #37697, #10193, #7488, .T. ) ;
#45998=DIRECTION ( 'NONE',  ( 0.000000000000000000, -0.5877852522924801315, 0.8090169943749423442 ) ) ;
#46011=VECTOR ( 'NONE', #46787, 1000.000000000000000 ) ;
#46014=ORIENTED_EDGE ( 'NONE', *, *, #48016, .T. ) ;
#46020=ORIENTED_EDGE ( 'NONE', *, *, #47467, .F. ) ;
#46021=DIRECTION ( 'NONE',  ( -1.000000000000000000, -0.000000000000000000, -0.000000000000000000 ) ) ;
#46025=CARTESIAN_POINT ( 'NONE',  ( 11.99999999999999822, 12.93880638057426502, -76.41127070299258150 ) ) ;
#46026=ORIENTED_EDGE ( 'NONE', *, *, #35261, .F. ) ;
#46039=DIRECTION ( 'NONE',  ( 0.000000000000000000, 0.9723699203976756689, 0.2334453638559093602 ) ) ;
#46040=ORIENTED_EDGE ( 'NONE', *, *, #39654, .F. ) ;
#46048=CARTESIAN_POINT ( 'NONE',  ( 0.000000000000000000, -44.99326035066007279, -68.55367621811190304 ) ) ;
#46055=DIRECTION ( 'NONE',  ( 0.000000000000000000, 0.000000000000000000, 1.000000000000000000 ) ) ;
#46059=DIRECTION ( 'NONE',  ( -1.000000000000000000, -0.000000000000000000, 0.000000000000000000 ) ) ;
#46061=DIRECTION ( 'NONE',  ( 1.000000000000000000, 0.000000000000000000, 0.000000000000000000 ) ) ;
#46064=EDGE_LOOP ( 'NONE', ( #44564, #39507, #45461, #40765 ) ) ;
#46065=EDGE_CURVE ( 'NONE', #7777, #29618, #11413, .T. ) ;
#46067=EDGE_LOOP ( 'NONE', ( #8374, #47687, #19732, #22426 ) ) ;
#46068=CARTESIAN_POINT ( 'NONE',  ( 0.000000000000000000, -50.23322058963299241, -64.81221759200397514 ) ) ;
#46070=CARTESIAN_POINT ( 'NONE',  ( 11.99999999999999822, 75.11764819372149304, -2.946379043146603482 ) ) ;
#46071=EDGE_LOOP ( 'NONE', ( #33553, #40529, #26583, #45713 ) ) ;
#46073=AXIS2_PLACEMENT_3D ( 'NONE', #16106, #31774, #46688 ) ;
#46074=DIRECTION ( 'NONE',  ( 0.000000000000000000, -0.7604059656000369261, 0.6494480483301766638 ) ) ;
#46078=CIRCLE ( 'NONE', #24964, 31.99999999999998579 ) ;
#46081=DIRECTION ( 'NONE',  ( -1.000000000000000000, -0.000000000000000000, -0.000000000000000000 ) ) ;
#46084=EDGE_CURVE ( 'NONE', #46329, #32083, #34069, .T. ) ;
#46091=FACE_OUTER_BOUND ( 'NONE', #17357, .T. ) ;
#46098=PLANE ( 'NONE',  #20000 ) ;
#46105=DIRECTION ( 'NONE',  ( 0.000000000000000000, 0.000000000000000000, 1.000000000000000000 ) ) ;
#46108=CARTESIAN_POINT ( 'NONE',  ( 11.99999999999999822, -75.11764819372145041, 29.05362095685286050 ) ) ;
#46109=VECTOR ( 'NONE', #4150, 1000.000000000000114 ) ;
#46111=DIRECTION ( 'NONE',  ( -0.000000000000000000, 0.8090169943749426773, -0.5877852522924796874 ) ) ;
#46114=FACE_OUTER_BOUND ( 'NONE', #19149, .T. ) ;
#46115=VECTOR ( 'NONE', #13032, 1000.000000000000114 ) ;
#46116=CARTESIAN_POINT ( 'NONE',  ( 6.000000000000000000, -81.96053171279903893, 2.543863470248107994 ) ) ;
#46118=CIRCLE ( 'NONE', #17966, 31.99999999999998579 ) ;
#46123=EDGE_LOOP ( 'NONE', ( #31938, #1127, #45703, #40423 ) ) ;
#46130=ORIENTED_EDGE ( 'NONE', *, *, #11929, .F. ) ;
#46133=DIRECTION ( 'NONE',  ( -1.000000000000000000, 0.000000000000000000, 0.000000000000000000 ) ) ;
#46136=DIRECTION ( 'NONE',  ( 1.000000000000000000, 0.000000000000000000, -0.000000000000000000 ) ) ;
#46137=CYLINDRICAL_SURFACE ( 'NONE', #13652, 77.49899999999999523 ) ;
#46156=FACE_OUTER_BOUND ( 'NONE', #39075, .T. ) ;
#46163=ORIENTED_EDGE ( 'NONE', *, *, #33575, .F. ) ;
#46169=FACE_OUTER_BOUND ( 'NONE', #8748, .T. ) ;
#46171=DIRECTION ( 'NONE',  ( 0.000000000000000000, -0.9969173337331270757, -0.07845909572785580988 ) ) ;
#46174=AXIS2_PLACEMENT_3D ( 'NONE', #16485, #30949, #46341 ) ;
#46180=AXIS2_PLACEMENT_3D ( 'NONE', #32583, #6401, #21318 ) ;
#46181=CARTESIAN_POINT ( 'NONE',  ( 11.99999999999999822, 51.02545421589402252, -55.20638768913705263 ) ) ;
#46187=ORIENTED_EDGE ( 'NONE', *, *, #43057, .F. ) ;
#46191=CARTESIAN_POINT ( 'NONE',  ( 0.000000000000000000, -59.03961581697367933, -46.53671651294010303 ) ) ;
#46194=ADVANCED_FACE ( 'NONE', ( #40621 ), #33027, .T. ) ;
#46195=CARTESIAN_POINT ( 'NONE',  ( 11.99999999999999822, 0.000000000000000000, 0.000000000000000000 ) ) ;
#46196=CARTESIAN_POINT ( 'NONE',  ( -10.00000000000000000, 0.000000000000000000, 0.000000000000000000 ) ) ;
#46200=ORIENTED_EDGE ( 'NONE', *, *, #47052, .F. ) ;
#46201=AXIS2_PLACEMENT_3D ( 'NONE', #46196, #23676, #39598 ) ;
#46204=ORIENTED_EDGE ( 'NONE', *, *, #45406, .T. ) ;
#46209=CIRCLE ( 'NONE', #39963, 31.99999999999999289 ) ;
#46211=VERTEX_POINT ( 'NONE', #22010 ) ;
#46213=DIRECTION ( 'NONE',  ( 0.000000000000000000, 0.000000000000000000, 1.000000000000000000 ) ) ;
#46218=ORIENTED_EDGE ( 'NONE', *, *, #4958, .T. ) ;
#46224=CYLINDRICAL_SURFACE ( 'NONE', #38476, 31.99999999999998579 ) ;
#46227=DIRECTION ( 'NONE',  ( -1.000000000000000000, 0.000000000000000000, 0.000000000000000000 ) ) ;
#46229=DIRECTION ( 'NONE',  ( 0.000000000000000000, 0.9723699203976773342, -0.2334453638559024491 ) ) ;
#46230=CARTESIAN_POINT ( 'NONE',  ( 11.99999999999999822, 0.000000000000000000, 0.000000000000000000 ) ) ;
#46243=AXIS2_PLACEMENT_3D ( 'NONE', #30498, #4328, #26589 ) ;
#46246=DIRECTION ( 'NONE',  ( -1.000000000000000000, 0.000000000000000000, -0.000000000000000000 ) ) ;
#46247=DIRECTION ( 'NONE',  ( -1.000000000000000000, 0.000000000000000000, 0.000000000000000000 ) ) ;
#46254=ORIENTED_EDGE ( 'NONE', *, *, #30777, .F. ) ;
#46263=DIRECTION ( 'NONE',  ( -1.000000000000000000, 0.000000000000000000, -0.000000000000000000 ) ) ;
#46264=ORIENTED_EDGE ( 'NONE', *, *, #4585, .T. ) ;
#46265=CARTESIAN_POINT ( 'NONE',  ( 11.99999999999999822, 36.72794159290334903, -65.59268652807170952 ) ) ;
#46269=CARTESIAN_POINT ( 'NONE',  ( 11.99999999999999822, 20.40083707022987625, -72.35432306680462489 ) ) ;
#46271=CIRCLE ( 'NONE', #44728, 77.49900000000002365 ) ;
#46275=AXIS2_PLACEMENT_3D ( 'NONE', #6472, #35843, #43675 ) ;
#46277=ORIENTED_EDGE ( 'NONE', *, *, #11402, .T. ) ;
#46279=CARTESIAN_POINT ( 'NONE',  ( 15.00000000000000000, 14.60985201121729737, 18.46759930825687235 ) ) ;
#46280=CARTESIAN_POINT ( 'NONE',  ( 11.99999999999999822, 41.76937507738875155, -62.50329211542393892 ) ) ;
#46281=CIRCLE ( 'NONE', #40788, 31.99999999999998579 ) ;
#46284=CARTESIAN_POINT ( 'NONE',  ( 0.000000000000000000, 0.000000000000000000, 0.000000000000000000 ) ) ;
#46286=CIRCLE ( 'NONE', #25160, 31.99999999999998224 ) ;
#46287=DIRECTION ( 'NONE',  ( 0.000000000000000000, -0.9238795325112906243, 0.3826834323650805114 ) ) ;
#46288=CARTESIAN_POINT ( 'NONE',  ( 11.99999999999999822, 0.000000000000000000, 0.000000000000000000 ) ) ;
#46290=DIRECTION ( 'NONE',  ( 0.000000000000000000, 0.5224985647159441360, 0.8526401643540951758 ) ) ;
#46293=DIRECTION ( 'NONE',  ( -1.000000000000000000, 0.000000000000000000, 0.000000000000000000 ) ) ;
#46296=PLANE ( 'NONE',  #31151 ) ;
#46297=VERTEX_POINT ( 'NONE', #22270 ) ;
#46299=EDGE_CURVE ( 'NONE', #4301, #13754, #9863, .T. ) ;
#46302=ADVANCED_FACE ( 'NONE', ( #2684 ), #3663, .T. ) ;
#46305=DIRECTION ( 'NONE',  ( 0.000000000000000000, -0.9723699203976789995, 0.2334453638558956767 ) ) ;
#46307=ORIENTED_EDGE ( 'NONE', *, *, #9217, .T. ) ;
#46309=AXIS2_PLACEMENT_3D ( 'NONE', #20200, #39051, #24123 ) ;
#46316=EDGE_CURVE ( 'NONE', #9506, #11531, #42709, .T. ) ;
#46319=ORIENTED_EDGE ( 'NONE', *, *, #20530, .F. ) ;
#46320=DIRECTION ( 'NONE',  ( 0.000000000000000000, 0.000000000000000000, 1.000000000000000000 ) ) ;
#46321=AXIS2_PLACEMENT_3D ( 'NONE', #4356, #42263, #42511 ) ;
#46324=DIRECTION ( 'NONE',  ( 0.000000000000000000, 0.07845909572783793529, 0.9969173337331285190 ) ) ;
#46326=FACE_OUTER_BOUND ( 'NONE', #20122, .T. ) ;
#46329=VERTEX_POINT ( 'NONE', #22511 ) ;
#46330=DIRECTION ( 'NONE',  ( 0.000000000000000000, 0.9781476007338043566, -0.2079116908177651712 ) ) ;
#46336=CARTESIAN_POINT ( 'NONE',  ( 11.99999999999999822, 0.000000000000000000, 0.000000000000000000 ) ) ;
#46341=DIRECTION ( 'NONE',  ( 0.000000000000000000, 0.000000000000000000, 1.000000000000000000 ) ) ;
#46343=DIRECTION ( 'NONE',  ( -1.000000000000000000, -0.000000000000000000, -0.000000000000000000 ) ) ;
#46351=AXIS2_PLACEMENT_3D ( 'NONE', #43040, #25386, #46724 ) ;
#46364=VECTOR ( 'NONE', #24975, 1000.000000000000000 ) ;
#46365=ORIENTED_EDGE ( 'NONE', *, *, #48191, .F. ) ;
#46367=CIRCLE ( 'NONE', #35396, 31.99999999999998934 ) ;
#46375=ORIENTED_EDGE ( 'NONE', *, *, #33825, .T. ) ;
#46376=DIRECTION ( 'NONE',  ( 0.000000000000000000, 0.000000000000000000, 1.000000000000000000 ) ) ;
#46378=ORIENTED_EDGE ( 'NONE', *, *, #16202, .F. ) ;
#46380=ORIENTED_EDGE ( 'NONE', *, *, #19045, .F. ) ;
#46382=DIRECTION ( 'NONE',  ( 0.000000000000000000, -0.9876883405951394357, 0.1564344650402205716 ) ) ;
#46386=AXIS2_PLACEMENT_3D ( 'NONE', #5991, #2292, #36778 ) ;
#46387=AXIS2_PLACEMENT_3D ( 'NONE', #3051, #22396, #11134 ) ;
#46388=ORIENTED_EDGE ( 'NONE', *, *, #34084, .T. ) ;
#46396=CARTESIAN_POINT ( 'NONE',  ( 11.99999999999999822, 0.000000000000000000, 0.000000000000000000 ) ) ;
#46398=LINE ( 'NONE', #16784, #41561 ) ;
#46401=CARTESIAN_POINT ( 'NONE',  ( 6.000000000000000000, 34.94270380257741238, -74.18225833017852722 ) ) ;
#46408=VERTEX_POINT ( 'NONE', #41845 ) ;
#46411=CARTESIAN_POINT ( 'NONE',  ( 11.99999999999999822, 0.000000000000000000, 0.000000000000000000 ) ) ;
#46415=CARTESIAN_POINT ( 'NONE',  ( 11.99999999999999822, -73.73191006444561424, -14.66109333815538918 ) ) ;
#46418=EDGE_CURVE ( 'NONE', #27749, #38028, #8530, .T. ) ;
#46421=CIRCLE ( 'NONE', #4220, 77.49899999999999523 ) ;
#46423=EDGE_CURVE ( 'NONE', #33736, #5920, #8305, .T. ) ;
#46424=VERTEX_POINT ( 'NONE', #11737 ) ;
#46425=DIRECTION ( 'NONE',  ( 0.000000000000000000, 0.000000000000000000, 1.000000000000000000 ) ) ;
#46427=ADVANCED_FACE ( 'NONE', ( #30572 ), #22988, .T. ) ;
#46431=EDGE_CURVE ( 'NONE', #45656, #41935, #13789, .T. ) ;
#46432=VERTEX_POINT ( 'NONE', #26911 ) ;
#46434=LINE ( 'NONE', #38857, #42153 ) ;
#46436=AXIS2_PLACEMENT_3D ( 'NONE', #19621, #564, #15495 ) ;
#46439=CARTESIAN_POINT ( 'NONE',  ( 0.000000000000000000, 0.000000000000000000, 0.000000000000000000 ) ) ;
#46445=DIRECTION ( 'NONE',  ( 0.000000000000000000, 0.1564344650402244852, 0.9876883405951387696 ) ) ;
#46446=VERTEX_POINT ( 'NONE', #705 ) ;
#46456=CARTESIAN_POINT ( 'NONE',  ( 0.000000000000000000, 71.21200624218852226, -40.65526001592539984 ) ) ;
#46457=AXIS2_PLACEMENT_3D ( 'NONE', #17257, #47386, #13364 ) ;
#46458=VERTEX_POINT ( 'NONE', #23233 ) ;
#46460=DIRECTION ( 'NONE',  ( 0.000000000000000000, 0.000000000000000000, 1.000000000000000000 ) ) ;
#46462=DIRECTION ( 'NONE',  ( 0.000000000000000000, 0.000000000000000000, 1.000000000000000000 ) ) ;
#46465=EDGE_LOOP ( 'NONE', ( #13300, #8504, #33501, #25986 ) ) ;
#46469=AXIS2_PLACEMENT_3D ( 'NONE', #15201, #45057, #4833 ) ;
#46472=AXIS2_PLACEMENT_3D ( 'NONE', #26177, #14439, #44768 ) ;
#46474=ORIENTED_EDGE ( 'NONE', *, *, #36564, .F. ) ;
#46477=DIRECTION ( 'NONE',  ( 0.000000000000000000, 0.000000000000000000, -1.000000000000000000 ) ) ;
#46478=CARTESIAN_POINT ( 'NONE',  ( 6.000000000000000000, 15.33399622253482697, 80.55351364060595643 ) ) ;
#46483=CARTESIAN_POINT ( 'NONE',  ( 11.99999999999999822, 75.16055320797057959, -18.89407956138179046 ) ) ;
#46488=CARTESIAN_POINT ( 'NONE',  ( 0.000000000000000000, 49.70050353004975818, -59.46389618801909904 ) ) ;
#46489=ADVANCED_FACE ( 'NONE', ( #7582 ), #32040, .F. ) ;
#46502=CIRCLE ( 'NONE', #31669, 82.00000000000000000 ) ;
#46508=EDGE_LOOP ( 'NONE', ( #29239, #19172, #10209, #15595 ) ) ;
#46509=AXIS2_PLACEMENT_3D ( 'NONE', #15342, #4324, #22435 ) ;
#46512=ORIENTED_EDGE ( 'NONE', *, *, #11632, .T. ) ;
#46513=CARTESIAN_POINT ( 'NONE',  ( 5.999999999999999112, 46.11716303203283474, -67.80270845531839541 ) ) ;
#46516=DIRECTION ( 'NONE',  ( 0.000000000000000000, 0.000000000000000000, 1.000000000000000000 ) ) ;
#46517=CARTESIAN_POINT ( 'NONE',  ( 11.99999999999999822, 0.000000000000000000, 0.000000000000000000 ) ) ;
#46519=DIRECTION ( 'NONE',  ( 0.000000000000000000, -0.9876883405951394357, 0.1564344650402203496 ) ) ;
#46522=VECTOR ( 'NONE', #24188, 1000.000000000000000 ) ;
#46527=DIRECTION ( 'NONE',  ( -1.000000000000000000, 0.000000000000000000, 0.000000000000000000 ) ) ;
#46532=CYLINDRICAL_SURFACE ( 'NONE', #15977, 31.99999999999998579 ) ;
#46533=DIRECTION ( 'NONE',  ( -1.000000000000000000, 0.000000000000000000, 0.000000000000000000 ) ) ;
#46538=AXIS2_PLACEMENT_3D ( 'NONE', #14776, #25287, #6461 ) ;
#46545=DIRECTION ( 'NONE',  ( 0.000000000000000000, 0.000000000000000000, 1.000000000000000000 ) ) ;
#46551=EDGE_CURVE ( 'NONE', #26074, #22545, #14590, .T. ) ;
#46561=AXIS2_PLACEMENT_3D ( 'NONE', #20890, #31684, #28224 ) ;
#46565=DIRECTION ( 'NONE',  ( 0.000000000000000000, 0.000000000000000000, 1.000000000000000000 ) ) ;
#46567=AXIS2_PLACEMENT_3D ( 'NONE', #33253, #40374, #44272 ) ;
#46571=EDGE_LOOP ( 'NONE', ( #41731, #44390, #45896, #40518 ) ) ;
#46574=CIRCLE ( 'NONE', #19971, 31.99999999999998579 ) ;
#46577=AXIS2_PLACEMENT_3D ( 'NONE', #34105, #38034, #20143 ) ;
#46578=LINE ( 'NONE', #42412, #37080 ) ;
#46587=DIRECTION ( 'NONE',  ( 1.000000000000000000, -0.000000000000000000, 0.000000000000000000 ) ) ;
#46598=DIRECTION ( 'NONE',  ( -1.000000000000000000, -0.000000000000000000, 0.000000000000000000 ) ) ;
#46602=DIRECTION ( 'NONE',  ( -1.000000000000000000, 0.000000000000000000, -0.000000000000000000 ) ) ;
#46615=AXIS2_PLACEMENT_3D ( 'NONE', #31436, #46343, #12818 ) ;
#46617=VERTEX_POINT ( 'NONE', #16609 ) ;
#46618=EDGE_CURVE ( 'NONE', #23653, #16881, #1940, .T. ) ;
#46621=VERTEX_POINT ( 'NONE', #24196 ) ;
#46623=ORIENTED_EDGE ( 'NONE', *, *, #33477, .T. ) ;
#46624=AXIS2_PLACEMENT_3D ( 'NONE', #6613, #21545, #36469 ) ;
#46625=CARTESIAN_POINT ( 'NONE',  ( 15.00000000000000000, 14.60985201121703980, -18.46759930825707841 ) ) ;
#46628=VERTEX_POINT ( 'NONE', #5604 ) ;
#46630=CARTESIAN_POINT ( 'NONE',  ( 15.00000000000000000, -13.04903810567646971, 19.60159698893442481 ) ) ;
#46633=FACE_OUTER_BOUND ( 'NONE', #35280, .T. ) ;
#46641=ORIENTED_EDGE ( 'NONE', *, *, #39400, .F. ) ;
#46642=LINE ( 'NONE', #6479, #40293 ) ;
#46643=EDGE_CURVE ( 'NONE', #41886, #19983, #13672, .T. ) ;
#46644=CIRCLE ( 'NONE', #18501, 31.99999999999998934 ) ;
#46649=DIRECTION ( 'NONE',  ( -1.000000000000000000, -0.000000000000000000, 0.000000000000000000 ) ) ;
#46654=DIRECTION ( 'NONE',  ( -1.000000000000000000, 0.000000000000000000, 0.000000000000000000 ) ) ;
#46656=DIRECTION ( 'NONE',  ( -1.000000000000000000, -0.000000000000000000, 0.000000000000000000 ) ) ;
#46657=EDGE_LOOP ( 'NONE', ( #31776, #45072, #30965, #7980 ) ) ;
#46658=VECTOR ( 'NONE', #4621, 1000.000000000000000 ) ;
#46659=ORIENTED_EDGE ( 'NONE', *, *, #30713, .T. ) ;
#46660=CYLINDRICAL_SURFACE ( 'NONE', #41929, 31.99999999999998579 ) ;
#46664=EDGE_CURVE ( 'NONE', #30440, #23468, #21727, .T. ) ;
#46667=DIRECTION ( 'NONE',  ( 0.000000000000000000, -0.5877852522924801315, 0.8090169943749423442 ) ) ;
#46668=AXIS2_PLACEMENT_3D ( 'NONE', #22214, #48390, #14871 ) ;
#46669=DIRECTION ( 'NONE',  ( -1.000000000000000000, 0.000000000000000000, 0.000000000000000000 ) ) ;
#46674=VERTEX_POINT ( 'NONE', #28827 ) ;
#46675=DIRECTION ( 'NONE',  ( 0.000000000000000000, 0.000000000000000000, -1.000000000000000000 ) ) ;
#46676=ORIENTED_EDGE ( 'NONE', *, *, #17686, .F. ) ;
#46679=ORIENTED_EDGE ( 'NONE', *, *, #28149, .T. ) ;
#46687=VECTOR ( 'NONE', #33092, 1000.000000000000000 ) ;
#46688=DIRECTION ( 'NONE',  ( 0.000000000000000000, 0.000000000000000000, 1.000000000000000000 ) ) ;
#46689=DIRECTION ( 'NONE',  ( 0.000000000000000000, 0.7071067811865487940, -0.7071067811865462405 ) ) ;
#46693=ORIENTED_EDGE ( 'NONE', *, *, #23601, .T. ) ;
#46695=CARTESIAN_POINT ( 'NONE',  ( 11.99999999999999822, 0.000000000000000000, 0.000000000000000000 ) ) ;
#46704=EDGE_CURVE ( 'NONE', #37684, #22174, #14390, .T. ) ;
#46705=CYLINDRICAL_SURFACE ( 'NONE', #10388, 77.49899999999999523 ) ;
#46707=LINE ( 'NONE', #27875, #41666 ) ;
#46709=ORIENTED_EDGE ( 'NONE', *, *, #10342, .F. ) ;
#46724=DIRECTION ( 'NONE',  ( 0.000000000000000000, -0.4539904997395350916, -0.8910065241883738940 ) ) ;
#46726=CARTESIAN_POINT ( 'NONE',  ( 0.000000000000000000, 0.000000000000000000, 0.000000000000000000 ) ) ;
#46731=CARTESIAN_POINT ( 'NONE',  ( 0.000000000000000000, 0.000000000000000000, 0.000000000000000000 ) ) ;
#46735=ORIENTED_EDGE ( 'NONE', *, *, #33039, .T. ) ;
#46739=EDGE_CURVE ( 'NONE', #39596, #30049, #20868, .T. ) ;
#46740=CARTESIAN_POINT ( 'NONE',  ( 11.99999999999999822, 0.000000000000000000, 0.000000000000000000 ) ) ;
#46742=ORIENTED_EDGE ( 'NONE', *, *, #42948, .F. ) ;
#46747=AXIS2_PLACEMENT_3D ( 'NONE', #40465, #34909, #1390 ) ;
#46750=ORIENTED_EDGE ( 'NONE', *, *, #26851, .F. ) ;
#46751=VECTOR ( 'NONE', #34681, 999.9999999999998863 ) ;
#46752=EDGE_CURVE ( 'NONE', #12206, #30376, #2882, .T. ) ;
#46753=DIRECTION ( 'NONE',  ( -1.000000000000000000, 0.000000000000000000, 0.000000000000000000 ) ) ;
#46759=DIRECTION ( 'NONE',  ( 0.000000000000000000, 0.000000000000000000, 1.000000000000000000 ) ) ;
#46761=CARTESIAN_POINT ( 'NONE',  ( 11.99999999999999822, 59.03342792756263435, 46.54456581323825048 ) ) ;
#46762=ORIENTED_EDGE ( 'NONE', *, *, #6457, .F. ) ;
#46763=ADVANCED_FACE ( 'NONE', ( #11682 ), #45216, .T. ) ;
#46764=LINE ( 'NONE', #33448, #9474 ) ;
#46766=ORIENTED_EDGE ( 'NONE', *, *, #1644, .T. ) ;
#46768=CARTESIAN_POINT ( 'NONE',  ( 6.000000000000000000, -81.90746397400386059, -3.894527615418766242 ) ) ;
#46773=ADVANCED_FACE ( 'NONE', ( #15113 ), #3607, .T. ) ;
#46774=LINE ( 'NONE', #21275, #16629 ) ;
#46776=ORIENTED_EDGE ( 'NONE', *, *, #32793, .F. ) ;
#46780=DIRECTION ( 'NONE',  ( 0.000000000000000000, 0.9876883405951383255, -0.1564344650402277048 ) ) ;
#46781=DIRECTION ( 'NONE',  ( 0.000000000000000000, -0.8090169943749530024, 0.5877852522924653655 ) ) ;
#46785=DIRECTION ( 'NONE',  ( -1.000000000000000000, -0.000000000000000000, -0.000000000000000000 ) ) ;
#46787=DIRECTION ( 'NONE',  ( -1.000000000000000000, 0.000000000000000000, -0.000000000000000000 ) ) ;
#46794=CARTESIAN_POINT ( 'NONE',  ( 15.00000000000000000, 14.60985201121703980, -18.46759930825707841 ) ) ;
#46798=AXIS2_PLACEMENT_3D ( 'NONE', #4467, #4225, #30900 ) ;
#46804=DIRECTION ( 'NONE',  ( 0.000000000000000000, -0.8660254037844421493, -0.4999999999999939493 ) ) ;
#46811=ADVANCED_FACE ( 'NONE', ( #19005 ), #45444, .T. ) ;
#46812=VECTOR ( 'NONE', #8501, 1000.000000000000000 ) ;
#46819=CARTESIAN_POINT ( 'NONE',  ( 11.99999999999999822, 0.000000000000000000, 0.000000000000000000 ) ) ;
#46825=CARTESIAN_POINT ( 'NONE',  ( 11.99999999999999822, -70.52718814184277107, 26.02418014898285037 ) ) ;
#46831=PRODUCT ( 'slow gear_ISO - Spur gear 2M 80T 20PA 12FW ---S80A75H50L38.0N', 'slow gear_ISO - Spur gear 2M 80T 20PA 12FW ---S80A75H50L38.0N', '', ( #4474 ) ) ;
#46832=CARTESIAN_POINT ( 'NONE',  ( 15.00000000000000000, -0.9646360437375368635, -23.52805723605589705 ) ) ;
#46834=MECHANICAL_DESIGN_GEOMETRIC_PRESENTATION_REPRESENTATION('',(#39811),#44480);
#46839=CARTESIAN_POINT ( 'NONE',  ( 11.99999999999999822, 0.000000000000000000, 0.000000000000000000 ) ) ;
#46841=DIRECTION ( 'NONE',  ( 0.000000000000000000, -0.8910065241883626808, -0.4539904997395568520 ) ) ;
#46847=CIRCLE ( 'NONE', #8533, 31.99999999999998579 ) ;
#46849=VERTEX_POINT ( 'NONE', #37623 ) ;
#46850=CARTESIAN_POINT ( 'NONE',  ( -10.00000000000000000, 0.000000000000000000, 0.000000000000000000 ) ) ;
#46855=ORIENTED_EDGE ( 'NONE', *, *, #45712, .F. ) ;
#46860=ORIENTED_EDGE ( 'NONE', *, *, #29459, .T. ) ;
#46861=DIRECTION ( 'NONE',  ( 0.000000000000000000, -0.2334453638558922350, -0.9723699203976797767 ) ) ;
#46866=ADVANCED_FACE ( 'NONE', ( #26846 ), #7271, .T. ) ;
#46871=DIRECTION ( 'NONE',  ( -0.000000000000000000, 0.5877852522924796874, 0.8090169943749426773 ) ) ;
#46872=DIRECTION ( 'NONE',  ( 0.000000000000000000, 0.3090169943749411785, 0.9510565162951556406 ) ) ;
#46873=DIRECTION ( 'NONE',  ( -1.000000000000000000, -0.000000000000000000, -0.000000000000000000 ) ) ;
#46885=DIRECTION ( 'NONE',  ( -1.000000000000000000, 0.000000000000000000, -0.000000000000000000 ) ) ;
#46887=CARTESIAN_POINT ( 'NONE',  ( 0.000000000000000000, 59.46389618801964616, 49.70050353004909738 ) ) ;
#46892=VERTEX_POINT ( 'NONE', #31024 ) ;
#46896=CARTESIAN_POINT ( 'NONE',  ( 11.99999999999999822, 75.16055320797030959, 18.89407956138283851 ) ) ;
#46899=DIRECTION ( 'NONE',  ( 0.000000000000000000, -0.8660254037844432595, -0.4999999999999920064 ) ) ;
#46906=EDGE_CURVE ( 'NONE', #18388, #18579, #38845, .T. ) ;
#46907=VECTOR ( 'NONE', #13090, 1000.000000000000000 ) ;
#46919=ORIENTED_EDGE ( 'NONE', *, *, #37907, .F. ) ;
#46923=ADVANCED_FACE ( 'NONE', ( #35385 ), #8712, .T. ) ;
#46926=FACE_OUTER_BOUND ( 'NONE', #41530, .T. ) ;
#46931=ORIENTED_EDGE ( 'NONE', *, *, #33029, .F. ) ;
#46932=CYLINDRICAL_SURFACE ( 'NONE', #16897, 31.99999999999998579 ) ;
#46935=CARTESIAN_POINT ( 'NONE',  ( 12.00000000000000000, 8.688484142254226938, 21.88630264137359305 ) ) ;
#46937=FACE_OUTER_BOUND ( 'NONE', #39298, .T. ) ;
#46941=CIRCLE ( 'NONE', #32100, 77.49899999999999523 ) ;
#46942=DIRECTION ( 'NONE',  ( 0.000000000000000000, -0.2334453638558922350, -0.9723699203976797767 ) ) ;
#46944=CIRCLE ( 'NONE', #25814, 77.49899999999998101 ) ;
#46946=EDGE_LOOP ( 'NONE', ( #31280, #35774, #16572, #9813 ) ) ;
#46948=VECTOR ( 'NONE', #46753, 1000.000000000000000 ) ;
#46954=AXIS2_PLACEMENT_3D ( 'NONE', #9598, #47060, #6428 ) ;
#46955=FACE_OUTER_BOUND ( 'NONE', #19760, .T. ) ;
#46956=ORIENTED_EDGE ( 'NONE', *, *, #33477, .F. ) ;
#46957=DIRECTION ( 'NONE',  ( 0.000000000000000000, -0.7431448254773871387, 0.6691306063588661202 ) ) ;
#46963=ORIENTED_EDGE ( 'NONE', *, *, #35594, .F. ) ;
#46967=DIRECTION ( 'NONE',  ( 0.000000000000000000, 0.000000000000000000, 1.000000000000000000 ) ) ;
#46969=ORIENTED_EDGE ( 'NONE', *, *, #35588, .F. ) ;
#46971=VECTOR ( 'NONE', #39772, 1000.000000000000000 ) ;
#46980=AXIS2_PLACEMENT_3D ( 'NONE', #29828, #7311, #22497 ) ;
#46986=ADVANCED_FACE ( 'NONE', ( #8482 ), #31498, .T. ) ;
#46987=ORIENTED_EDGE ( 'NONE', *, *, #40092, .F. ) ;
#47000=LINE ( 'NONE', #47240, #23081 ) ;
#47005=DIRECTION ( 'NONE',  ( 0.000000000000000000, 0.000000000000000000, 1.000000000000000000 ) ) ;
#47007=CARTESIAN_POINT ( 'NONE',  ( 11.99999999999999822, -17.28742895386031719, -75.54627589209962935 ) ) ;
#47008=AXIS2_PLACEMENT_3D ( 'NONE', #16965, #9860, #2986 ) ;
#47009=EDGE_CURVE ( 'NONE', #17273, #39718, #5260, .T. ) ;
#47013=DIRECTION ( 'NONE',  ( -1.000000000000000000, -0.000000000000000000, -0.000000000000000000 ) ) ;
#47023=DIRECTION ( 'NONE',  ( -1.000000000000000000, 0.000000000000000000, 0.000000000000000000 ) ) ;
#47024=CIRCLE ( 'NONE', #6390, 77.49899999999999523 ) ;
#47026=DIRECTION ( 'NONE',  ( -1.000000000000000000, 0.000000000000000000, 0.000000000000000000 ) ) ;
#47027=ORIENTED_EDGE ( 'NONE', *, *, #39897, .F. ) ;
#47032=ORIENTED_EDGE ( 'NONE', *, *, #35768, .F. ) ;
#47049=DIRECTION ( 'NONE',  ( -1.000000000000000000, 0.000000000000000000, 0.000000000000000000 ) ) ;
#47052=EDGE_CURVE ( 'NONE', #35187, #31605, #36825, .T. ) ;
#47055=DIRECTION ( 'NONE',  ( 0.000000000000000000, 0.000000000000000000, 1.000000000000000000 ) ) ;
#47057=CARTESIAN_POINT ( 'NONE',  ( 0.000000000000000000, 0.000000000000000000, 0.000000000000000000 ) ) ;
#47060=DIRECTION ( 'NONE',  ( -1.000000000000000000, 0.000000000000000000, 0.000000000000000000 ) ) ;
#47061=CARTESIAN_POINT ( 'NONE',  ( 12.00000000000000000, 16.61724383029390140, 20.69703378468902955 ) ) ;
#47063=LINE ( 'NONE', #27995, #15185 ) ;
#47067=DIRECTION ( 'NONE',  ( 0.000000000000000000, -0.4999999999999921174, 0.8660254037844431485 ) ) ;
#47069=DIRECTION ( 'NONE',  ( 0.000000000000000000, 0.000000000000000000, 1.000000000000000000 ) ) ;
#47079=ADVANCED_FACE ( 'NONE', ( #10408 ), #9680, .T. ) ;
#47087=EDGE_CURVE ( 'NONE', #2398, #27438, #10739, .T. ) ;
#47089=CARTESIAN_POINT ( 'NONE',  ( 0.000000000000000000, -69.42325613327466272, 34.44570377933573724 ) ) ;
#47093=FACE_OUTER_BOUND ( 'NONE', #15545, .T. ) ;
#47094=ORIENTED_EDGE ( 'NONE', *, *, #9010, .T. ) ;
#47095=PLANE ( 'NONE',  #10954 ) ;
#47103=VECTOR ( 'NONE', #2280, 1000.000000000000227 ) ;
#47105=VERTEX_POINT ( 'NONE', #13601 ) ;
#47109=DIRECTION ( 'NONE',  ( -1.000000000000000000, 0.000000000000000000, 0.000000000000000000 ) ) ;
#47112=DIRECTION ( 'NONE',  ( 1.000000000000000000, 0.000000000000000000, 0.000000000000000000 ) ) ;
#47113=DIRECTION ( 'NONE',  ( -1.000000000000000000, 0.000000000000000000, -0.000000000000000000 ) ) ;
#47123=AXIS2_PLACEMENT_3D ( 'NONE', #23848, #31206, #19206 ) ;
#47127=EDGE_CURVE ( 'NONE', #11149, #5341, #21896, .T. ) ;
#47128=DIRECTION ( 'NONE',  ( 0.000000000000000000, 0.000000000000000000, 1.000000000000000000 ) ) ;
#47130=FACE_OUTER_BOUND ( 'NONE', #46946, .T. ) ;
#47131=ORIENTED_EDGE ( 'NONE', *, *, #22210, .F. ) ;
#47132=CARTESIAN_POINT ( 'NONE',  ( 12.00000000000000000, 16.83928648764922542, -16.46020748918050458 ) ) ;
#47133=ORIENTED_EDGE ( 'NONE', *, *, #43406, .T. ) ;
#47137=EDGE_CURVE ( 'NONE', #33199, #13081, #13857, .T. ) ;
#47138=EDGE_CURVE ( 'NONE', #35412, #42832, #31049, .T. ) ;
#47139=ORIENTED_EDGE ( 'NONE', *, *, #28175, .F. ) ;
#47142=AXIS2_PLACEMENT_3D ( 'NONE', #10205, #21708, #43743 ) ;
#47147=EDGE_LOOP ( 'NONE', ( #36215, #4689, #6937, #3878 ) ) ;
#47148=VECTOR ( 'NONE', #12953, 1000.000000000000000 ) ;
#47151=CYLINDRICAL_SURFACE ( 'NONE', #43721, 31.99999999999998579 ) ;
#47155=EDGE_CURVE ( 'NONE', #45830, #42640, #21420, .T. ) ;
#47161=FACE_OUTER_BOUND ( 'NONE', #20888, .T. ) ;
#47163=LINE ( 'NONE', #13634, #22795 ) ;
#47164=ORIENTED_EDGE ( 'NONE', *, *, #23607, .F. ) ;
#47165=ORIENTED_EDGE ( 'NONE', *, *, #47087, .T. ) ;
#47167=ORIENTED_EDGE ( 'NONE', *, *, #24201, .F. ) ;
#47173=CIRCLE ( 'NONE', #19030, 31.99999999999998579 ) ;
#47174=CARTESIAN_POINT ( 'NONE',  ( 0.000000000000000000, 73.73191006444572793, -14.66109333815486515 ) ) ;
#47177=ORIENTED_EDGE ( 'NONE', *, *, #17886, .T. ) ;
#47178=CARTESIAN_POINT ( 'NONE',  ( 11.99999999999999822, -28.89263327155693517, -71.91182617369219088 ) ) ;
#47179=ORIENTED_EDGE ( 'NONE', *, *, #41408, .T. ) ;
#47180=AXIS2_PLACEMENT_3D ( 'NONE', #47821, #42973, #9421 ) ;
#47181=CIRCLE ( 'NONE', #21382, 82.00000000000000000 ) ;
#47183=EDGE_CURVE ( 'NONE', #1839, #35935, #2820, .T. ) ;
#47185=CARTESIAN_POINT ( 'NONE',  ( 11.99999999999999822, 51.02545421589324803, 55.20638768913779870 ) ) ;
#47190=ORIENTED_EDGE ( 'NONE', *, *, #29058, .F. ) ;
#47191=CIRCLE ( 'NONE', #22939, 77.49899999999999523 ) ;
#47195=DIRECTION ( 'NONE',  ( 0.000000000000000000, 0.2334453638559058908, -0.9723699203976764460 ) ) ;
#47197=VECTOR ( 'NONE', #31611, 1000.000000000000000 ) ;
#47209=AXIS2_PLACEMENT_3D ( 'NONE', #18042, #44250, #10725 ) ;
#47212=CARTESIAN_POINT ( 'NONE',  ( 0.000000000000000000, 0.000000000000000000, 0.000000000000000000 ) ) ;
#47216=ORIENTED_EDGE ( 'NONE', *, *, #4763, .F. ) ;
#47223=VERTEX_POINT ( 'NONE', #4290 ) ;
#47227=CARTESIAN_POINT ( 'NONE',  ( 11.99999999999999822, 40.65526001592611749, 71.21200624218811015 ) ) ;
#47228=AXIS2_PLACEMENT_3D ( 'NONE', #177, #26621, #41552 ) ;
#47230=CARTESIAN_POINT ( 'NONE',  ( 5.999999999999999112, -55.16347631943085617, 60.67117009219117563 ) ) ;
#47233=CARTESIAN_POINT ( 'NONE',  ( 11.99999999999999822, -6.903761155838323837, 77.19088730480521576 ) ) ;
#47236=DIRECTION ( 'NONE',  ( -1.000000000000000000, 0.000000000000000000, 0.000000000000000000 ) ) ;
#47240=CARTESIAN_POINT ( 'NONE',  ( 11.99999999999999822, 76.41127070299273782, 12.93880638057342836 ) ) ;
#47242=ADVANCED_FACE ( 'NONE', ( #45380 ), #41720, .T. ) ;
#47253=DIRECTION ( 'NONE',  ( 0.000000000000000000, 0.000000000000000000, 1.000000000000000000 ) ) ;
#47256=CARTESIAN_POINT ( 'NONE',  ( 11.99999999999999822, -14.66109333815513160, 73.73191006444567108 ) ) ;
#47258=CIRCLE ( 'NONE', #22123, 82.00000000000000000 ) ;
#47260=CYLINDRICAL_SURFACE ( 'NONE', #32731, 82.00000000000000000 ) ;
#47261=DIRECTION ( 'NONE',  ( 0.000000000000000000, -0.2079116908177554846, 0.9781476007338064660 ) ) ;
#47273=CARTESIAN_POINT ( 'NONE',  ( 11.99999999999999822, 0.000000000000000000, 0.000000000000000000 ) ) ;
#47277=LINE ( 'NONE', #30715, #5474 ) ;
#47280=DIRECTION ( 'NONE',  ( -1.000000000000000000, -0.000000000000000000, 0.000000000000000000 ) ) ;
#47286=CARTESIAN_POINT ( 'NONE',  ( 11.99999999999999822, 75.54627589209944460, 17.28742895386110945 ) ) ;
#47287=ORIENTED_EDGE ( 'NONE', *, *, #47482, .T. ) ;
#47292=CARTESIAN_POINT ( 'NONE',  ( 11.99999999999999822, -30.41916302227062019, -71.27951684758059514 ) ) ;
#47304=EDGE_CURVE ( 'NONE', #19294, #15803, #27194, .T. ) ;
#47307=CARTESIAN_POINT ( 'NONE',  ( 15.00000000000000000, 23.49999999999999645, -1.500000000000003997 ) ) ;
#47309=ORIENTED_EDGE ( 'NONE', *, *, #37685, .F. ) ;
#47313=FACE_OUTER_BOUND ( 'NONE', #45478, .T. ) ;
#47327=FACE_OUTER_BOUND ( 'NONE', #36708, .T. ) ;
#47330=CYLINDRICAL_SURFACE ( 'NONE', #5706, 31.99999999999998579 ) ;
#47335=CIRCLE ( 'NONE', #20742, 31.99999999999998579 ) ;
#47340=ORIENTED_EDGE ( 'NONE', *, *, #2640, .T. ) ;
#47343=AXIS2_PLACEMENT_3D ( 'NONE', #47057, #32376, #13522 ) ;
#47345=EDGE_CURVE ( 'NONE', #28702, #27047, #6101, .T. ) ;
#47347=DIRECTION ( 'NONE',  ( -1.000000000000000000, 0.000000000000000000, 0.000000000000000000 ) ) ;
#47352=CARTESIAN_POINT ( 'NONE',  ( 5.999999999999999112, -77.16300072079641836, -27.74655509720751922 ) ) ;
#47355=EDGE_LOOP ( 'NONE', ( #17773, #6776, #19090, #17578 ) ) ;
#47359=ADVANCED_FACE ( 'NONE', ( #32331 ), #41976, .F. ) ;
#47363=EDGE_LOOP ( 'NONE', ( #41043, #30439, #47654, #10358 ) ) ;
#47371=CARTESIAN_POINT ( 'NONE',  ( 11.99999999999999822, -41.19522573413780009, 65.64334221924896440 ) ) ;
#47373=DIRECTION ( 'NONE',  ( -1.000000000000000000, 0.000000000000000000, 0.000000000000000000 ) ) ;
#47374=DIRECTION ( 'NONE',  ( -1.000000000000000000, -0.000000000000000000, -0.000000000000000000 ) ) ;
#47377=VECTOR ( 'NONE', #20799, 1000.000000000000000 ) ;
#47378=ORIENTED_EDGE ( 'NONE', *, *, #924, .F. ) ;
#47379=CARTESIAN_POINT ( 'NONE',  ( 11.99999999999999822, -74.65491531819124305, 8.830959090342128448 ) ) ;
#47385=DIRECTION ( 'NONE',  ( -1.000000000000000000, 0.000000000000000000, 0.000000000000000000 ) ) ;
#47386=DIRECTION ( 'NONE',  ( -1.000000000000000000, -0.000000000000000000, -0.000000000000000000 ) ) ;
#47387=AXIS2_PLACEMENT_3D ( 'NONE', #3787, #8187, #37806 ) ;
#47390=AXIS2_PLACEMENT_3D ( 'NONE', #518, #259, #11301 ) ;
#47396=DIRECTION ( 'NONE',  ( -1.000000000000000000, -0.000000000000000000, -0.000000000000000000 ) ) ;
#47401=CARTESIAN_POINT ( 'NONE',  ( -10.00000000000000000, 0.000000000000000000, 0.000000000000000000 ) ) ;
#47402=ORIENTED_EDGE ( 'NONE', *, *, #18272, .F. ) ;
#47413=CARTESIAN_POINT ( 'NONE',  ( 11.99999999999999822, -44.99326035066103202, 68.55367621811127776 ) ) ;
#47415=CARTESIAN_POINT ( 'NONE',  ( 0.000000000000000000, -31.46837873495025306, 68.27212725128265447 ) ) ;
#47425=EDGE_CURVE ( 'NONE', #2149, #9566, #27969, .T. ) ;
#47426=VERTEX_POINT ( 'NONE', #35519 ) ;
#47427=CYLINDRICAL_SURFACE ( 'NONE', #37149, 82.00000000000000000 ) ;
#47431=CARTESIAN_POINT ( 'NONE',  ( 11.99999999999999822, 73.95703589263975175, 23.16143007188452785 ) ) ;
#47441=AXIS2_PLACEMENT_3D ( 'NONE', #20390, #35578, #16494 ) ;
#47451=ORIENTED_EDGE ( 'NONE', *, *, #38441, .T. ) ;
#47458=CARTESIAN_POINT ( 'NONE',  ( 12.00000000000000000, -25.60904388321925040, -6.976881207771165272 ) ) ;
#47460=LINE ( 'NONE', #17595, #1746 ) ;
#47461=AXIS2_PLACEMENT_3D ( 'NONE', #45442, #34183, #41540 ) ;
#47462=DIRECTION ( 'NONE',  ( -1.000000000000000000, 0.000000000000000000, 0.000000000000000000 ) ) ;
#47464=EDGE_LOOP ( 'NONE', ( #12133, #16587, #36388, #18629 ) ) ;
#47467=EDGE_CURVE ( 'NONE', #13807, #20955, #34975, .T. ) ;
#47473=EDGE_LOOP ( 'NONE', ( #23586, #24581, #45138, #3928 ) ) ;
#47482=EDGE_CURVE ( 'NONE', #1013, #40177, #17776, .T. ) ;
#47488=CARTESIAN_POINT ( 'NONE',  ( 12.00000000000000000, 22.07842321921480888, -8.187992925817425771 ) ) ;
#47494=AXIS2_PLACEMENT_3D ( 'NONE', #47751, #14240, #29158 ) ;
#47509=DIRECTION ( 'NONE',  ( -1.000000000000000000, 0.000000000000000000, 0.000000000000000000 ) ) ;
#47510=DIRECTION ( 'NONE',  ( -1.000000000000000000, 0.000000000000000000, -0.000000000000000000 ) ) ;
#47511=ORIENTED_EDGE ( 'NONE', *, *, #18333, .F. ) ;
#47514=FACE_OUTER_BOUND ( 'NONE', #36442, .T. ) ;
#47519=CARTESIAN_POINT ( 'NONE',  ( 0.000000000000000000, -22.90783923731685334, 78.73519480814945837 ) ) ;
#47520=ADVANCED_FACE ( 'NONE', ( #29379 ), #6620, .F. ) ;
#47521=CIRCLE ( 'NONE', #36590, 31.99999999999998579 ) ;
#47522=DIRECTION ( 'NONE',  ( -1.000000000000000000, -0.000000000000000000, -0.000000000000000000 ) ) ;
#47523=DIRECTION ( 'NONE',  ( -1.000000000000000000, 0.000000000000000000, -0.000000000000000000 ) ) ;
#47524=ORIENTED_EDGE ( 'NONE', *, *, #26550, .T. ) ;
#47527=EDGE_LOOP ( 'NONE', ( #2494, #37168, #10590, #38996 ) ) ;
#47529=LINE ( 'NONE', #43859, #2706 ) ;
#47535=VERTEX_POINT ( 'NONE', #28884 ) ;
#47537=DIRECTION ( 'NONE',  ( -0.000000000000000000, 0.1045284632676437703, -0.9945218953682742891 ) ) ;
#47540=DIRECTION ( 'NONE',  ( 0.000000000000000000, 0.000000000000000000, 1.000000000000000000 ) ) ;
#47545=CARTESIAN_POINT ( 'NONE',  ( 11.99999999999999822, -14.67089635893658794, -73.72996012237454977 ) ) ;
#47546=DIRECTION ( 'NONE',  ( 0.000000000000000000, 0.000000000000000000, 1.000000000000000000 ) ) ;
#47555=DIRECTION ( 'NONE',  ( 0.000000000000000000, 0.000000000000000000, 1.000000000000000000 ) ) ;
#47556=AXIS2_PLACEMENT_3D ( 'NONE', #33240, #40108, #25157 ) ;
#47566=CARTESIAN_POINT ( 'NONE',  ( 11.99999999999999822, 36.73666225445988687, -65.58780272294035285 ) ) ;
#47567=ORIENTED_EDGE ( 'NONE', *, *, #5690, .T. ) ;
#47569=ORIENTED_EDGE ( 'NONE', *, *, #29459, .F. ) ;
#47576=CARTESIAN_POINT ( 'NONE',  ( 11.99999999999999822, -59.03961581697432592, 46.53671651293927880 ) ) ;
#47585=EDGE_LOOP ( 'NONE', ( #15788, #28555, #47167, #33297 ) ) ;
#47586=DIRECTION ( 'NONE',  ( 0.000000000000000000, 0.000000000000000000, 1.000000000000000000 ) ) ;
#47588=FACE_OUTER_BOUND ( 'NONE', #32685, .T. ) ;
#47593=ORIENTED_EDGE ( 'NONE', *, *, #32542, .T. ) ;
#47595=DIRECTION ( 'NONE',  ( 1.000000000000000000, 0.000000000000000000, 0.000000000000000000 ) ) ;
#47603=CARTESIAN_POINT ( 'NONE',  ( 11.99999999999999822, -39.78640506895559525, -66.50666863322042843 ) ) ;
#47606=CARTESIAN_POINT ( 'NONE',  ( 11.99999999999999822, 73.44644590900094272, -24.73286445877629802 ) ) ;
#47607=VERTEX_POINT ( 'NONE', #21781 ) ;
#47612=ORIENTED_EDGE ( 'NONE', *, *, #36125, .T. ) ;
#47617=ORIENTED_EDGE ( 'NONE', *, *, #11250, .T. ) ;
#47618=CIRCLE ( 'NONE', #22619, 82.00000000000000000 ) ;
#47623=ORIENTED_EDGE ( 'NONE', *, *, #42506, .F. ) ;
#47628=EDGE_LOOP ( 'NONE', ( #39083, #28366, #46026, #9278 ) ) ;
#47634=AXIS2_PLACEMENT_3D ( 'NONE', #38633, #1424, #5099 ) ;
#47635=CARTESIAN_POINT ( 'NONE',  ( 15.00000000000000000, -10.45096189432314127, 21.10159698893440350 ) ) ;
#47640=LINE ( 'NONE', #3093, #17465 ) ;
#47645=EDGE_LOOP ( 'NONE', ( #17412, #32458, #15115, #3243 ) ) ;
#47651=DIRECTION ( 'NONE',  ( -1.000000000000000000, -0.000000000000000000, 0.000000000000000000 ) ) ;
#47654=ORIENTED_EDGE ( 'NONE', *, *, #35855, .T. ) ;
#47655=DIRECTION ( 'NONE',  ( -1.000000000000000000, 0.000000000000000000, -0.000000000000000000 ) ) ;
#47660=CARTESIAN_POINT ( 'NONE',  ( 11.99999999999999822, 0.000000000000000000, 0.000000000000000000 ) ) ;
#47666=ORIENTED_EDGE ( 'NONE', *, *, #18505, .F. ) ;
#47667=FACE_OUTER_BOUND ( 'NONE', #22775, .T. ) ;
#47673=EDGE_LOOP ( 'NONE', ( #40818, #20587, #25832, #30665 ) ) ;
#47674=ORIENTED_EDGE ( 'NONE', *, *, #12478, .F. ) ;
#47675=EDGE_CURVE ( 'NONE', #17321, #31583, #44414, .T. ) ;
#47676=ORIENTED_EDGE ( 'NONE', *, *, #41931, .T. ) ;
#47679=ORIENTED_EDGE ( 'NONE', *, *, #322, .F. ) ;
#47681=ORIENTED_EDGE ( 'NONE', *, *, #16163, .T. ) ;
#47685=DIRECTION ( 'NONE',  ( -1.000000000000000000, 0.000000000000000000, -0.000000000000000000 ) ) ;
#47687=ORIENTED_EDGE ( 'NONE', *, *, #15431, .F. ) ;
#47689=ORIENTED_EDGE ( 'NONE', *, *, #13086, .T. ) ;
#47693=EDGE_LOOP ( 'NONE', ( #31587, #40310, #11759, #15007 ) ) ;
#47698=ORIENTED_EDGE ( 'NONE', *, *, #6422, .F. ) ;
#47707=CARTESIAN_POINT ( 'NONE',  ( 0.000000000000000000, 0.8261519478431255115, 77.49459641780886443 ) ) ;
#47708=EDGE_CURVE ( 'NONE', #35935, #36518, #5323, .T. ) ;
#47709=FACE_OUTER_BOUND ( 'NONE', #35163, .T. ) ;
#47715=ORIENTED_EDGE ( 'NONE', *, *, #9629, .T. ) ;
#47716=ORIENTED_EDGE ( 'NONE', *, *, #5096, .F. ) ;
#47718=AXIS2_PLACEMENT_3D ( 'NONE', #1649, #16577, #46445 ) ;
#47722=EDGE_CURVE ( 'NONE', #4001, #3020, #487, .T. ) ;
#47723=DIRECTION ( 'NONE',  ( 0.000000000000000000, 0.9723699203976773342, -0.2334453638559024213 ) ) ;
#47725=CIRCLE ( 'NONE', #17226, 31.99999999999999645 ) ;
#47730=DIRECTION ( 'NONE',  ( 0.000000000000000000, 0.000000000000000000, 1.000000000000000000 ) ) ;
#47734=DIRECTION ( 'NONE',  ( 0.000000000000000000, 0.000000000000000000, 1.000000000000000000 ) ) ;
#47735=DIRECTION ( 'NONE',  ( -1.000000000000000000, -0.000000000000000000, -0.000000000000000000 ) ) ;
#47739=DIRECTION ( 'NONE',  ( 0.000000000000000000, 0.000000000000000000, 1.000000000000000000 ) ) ;
#47741=CARTESIAN_POINT ( 'NONE',  ( 0.000000000000000000, 15.33399622253601713, -80.55351364060572905 ) ) ;
#47745=AXIS2_PLACEMENT_3D ( 'NONE', #40676, #7149, #22801 ) ;
#47747=ORIENTED_EDGE ( 'NONE', *, *, #8126, .F. ) ;
#47751=CARTESIAN_POINT ( 'NONE',  ( 11.99999999999999822, -75.11725578898466438, -2.956366410621452001 ) ) ;
#47753=ORIENTED_EDGE ( 'NONE', *, *, #33044, .F. ) ;
#47755=CARTESIAN_POINT ( 'NONE',  ( 11.99999999999999822, -77.19088730480518734, -6.903761155838607166 ) ) ;
#47758=CARTESIAN_POINT ( 'NONE',  ( 0.000000000000000000, -41.19522573413780009, 65.64334221924896440 ) ) ;
#47759=DIRECTION ( 'NONE',  ( -1.000000000000000000, 0.000000000000000000, -0.000000000000000000 ) ) ;
#47760=DIRECTION ( 'NONE',  ( 0.000000000000000000, 0.9876883405951383255, -0.1564344650402276216 ) ) ;
#47765=EDGE_CURVE ( 'NONE', #22825, #9001, #30343, .T. ) ;
#47770=CARTESIAN_POINT ( 'NONE',  ( -10.00000000000000000, 0.000000000000000000, 0.000000000000000000 ) ) ;
#47773=AXIS2_PLACEMENT_3D ( 'NONE', #13220, #43322, #17118 ) ;
#47775=ORIENTED_EDGE ( 'NONE', *, *, #30713, .F. ) ;
#47776=ORIENTED_EDGE ( 'NONE', *, *, #11873, .T. ) ;
#47780=CARTESIAN_POINT ( 'NONE',  ( 6.000000000000000000, -81.50828551894234408, 8.966570791700414489 ) ) ;
#47782=ORIENTED_EDGE ( 'NONE', *, *, #4103, .F. ) ;
#47784=DIRECTION ( 'NONE',  ( 0.000000000000000000, 0.000000000000000000, 1.000000000000000000 ) ) ;
#47795=ORIENTED_EDGE ( 'NONE', *, *, #1402, .F. ) ;
#47796=CIRCLE ( 'NONE', #11866, 31.99999999999998934 ) ;
#47800=DIRECTION ( 'NONE',  ( 0.000000000000000000, 0.3090169943749480064, -0.9510565162951534202 ) ) ;
#47801=DIRECTION ( 'NONE',  ( 0.000000000000000000, 0.000000000000000000, 1.000000000000000000 ) ) ;
#47804=ORIENTED_EDGE ( 'NONE', *, *, #11632, .F. ) ;
#47807=VERTEX_POINT ( 'NONE', #21937 ) ;
#47810=DIRECTION ( 'NONE',  ( -1.000000000000000000, -0.000000000000000000, -0.000000000000000000 ) ) ;
#47811=VERTEX_POINT ( 'NONE', #40329 ) ;
#47813=CARTESIAN_POINT ( 'NONE',  ( 6.000000000000000000, 39.47590169984945163, -71.87247863392373404 ) ) ;
#47815=EDGE_LOOP ( 'NONE', ( #26363, #22502, #40758, #19998 ) ) ;
#47821=CARTESIAN_POINT ( 'NONE',  ( 15.00000000000000000, 0.000000000000000000, 0.000000000000000000 ) ) ;
#47823=CARTESIAN_POINT ( 'NONE',  ( 0.000000000000000000, 0.000000000000000000, 0.000000000000000000 ) ) ;
#47824=CIRCLE ( 'NONE', #20471, 31.99999999999999289 ) ;
#47825=CARTESIAN_POINT ( 'NONE',  ( 5.999999999999999112, -33.71516098798793593, 74.74816331893417498 ) ) ;
#47826=CARTESIAN_POINT ( 'NONE',  ( 0.000000000000000000, -14.67089635893764665, 73.72996012237435082 ) ) ;
#47832=CARTESIAN_POINT ( 'NONE',  ( 11.99999999999999822, -73.95703589263990807, 23.16143007188399139 ) ) ;
#47833=CARTESIAN_POINT ( 'NONE',  ( 11.99999999999999822, 0.8261519478431255115, 77.49459641780886443 ) ) ;
#47837=DIRECTION ( 'NONE',  ( -1.000000000000000000, -0.000000000000000000, -0.000000000000000000 ) ) ;
#47843=FACE_OUTER_BOUND ( 'NONE', #45147, .T. ) ;
#47844=VERTEX_POINT ( 'NONE', #33206 ) ;
#47850=CIRCLE ( 'NONE', #43950, 31.99999999999998579 ) ;
#47852=ORIENTED_EDGE ( 'NONE', *, *, #12430, .F. ) ;
#47853=EDGE_LOOP ( 'NONE', ( #40502, #37989, #14004, #40800 ) ) ;
#47854=EDGE_CURVE ( 'NONE', #43377, #26074, #6881, .T. ) ;
#47855=AXIS2_PLACEMENT_3D ( 'NONE', #40921, #37241, #44826 ) ;
#47857=CARTESIAN_POINT ( 'NONE',  ( 11.99999999999999822, 77.19088730480524418, 6.903761155838049390 ) ) ;
#47863=ORIENTED_EDGE ( 'NONE', *, *, #18890, .F. ) ;
#47864=CIRCLE ( 'NONE', #36134, 31.99999999999998579 ) ;
#47866=DIRECTION ( 'NONE',  ( -1.000000000000000000, 0.000000000000000000, -0.000000000000000000 ) ) ;
#47868=ORIENTED_EDGE ( 'NONE', *, *, #19034, .T. ) ;
#47874=VERTEX_POINT ( 'NONE', #14122 ) ;
#47885=DIRECTION ( 'NONE',  ( -1.000000000000000000, 0.000000000000000000, -0.000000000000000000 ) ) ;
#47896=CARTESIAN_POINT ( 'NONE',  ( 11.99999999999999822, 77.16300072079661732, 27.74655509720698277 ) ) ;
#47901=FACE_OUTER_BOUND ( 'NONE', #43987, .T. ) ;
#47904=LINE ( 'NONE', #7034, #42531 ) ;
#47906=CIRCLE ( 'NONE', #30733, 31.99999999999998224 ) ;
#47913=CARTESIAN_POINT ( 'NONE',  ( 0.000000000000000000, -74.65491531819111515, -8.830959090343204920 ) ) ;
#47915=ORIENTED_EDGE ( 'NONE', *, *, #40316, .T. ) ;
#47920=ADVANCED_FACE ( 'NONE', ( #16060 ), #8460, .T. ) ;
#47921=AXIS2_PLACEMENT_3D ( 'NONE', #29119, #25680, #44536 ) ;
#47922=EDGE_CURVE ( 'NONE', #22545, #20106, #38324, .T. ) ;
#47926=ORIENTED_EDGE ( 'NONE', *, *, #193, .T. ) ;
#47931=FACE_OUTER_BOUND ( 'NONE', #29585, .T. ) ;
#47933=VECTOR ( 'NONE', #15583, 1000.000000000000000 ) ;
#47936=LINE ( 'NONE', #28638, #4 ) ;
#47947=ORIENTED_EDGE ( 'NONE', *, *, #30116, .T. ) ;
#47950=FACE_OUTER_BOUND ( 'NONE', #37998, .T. ) ;
#47951=DIRECTION ( 'NONE',  ( 0.000000000000000000, 0.000000000000000000, -1.000000000000000000 ) ) ;
#47952=ADVANCED_FACE ( 'NONE', ( #37598 ), #4554, .T. ) ;
#47966=CIRCLE ( 'NONE', #22952, 31.99999999999999289 ) ;
#47969=AXIS2_PLACEMENT_3D ( 'NONE', #7388, #17421, #43864 ) ;
#47972=VECTOR ( 'NONE', #19664, 1000.000000000000000 ) ;
#47983=CARTESIAN_POINT ( 'NONE',  ( 11.99999999999999822, 77.49459641780886443, 0.8261519478433866359 ) ) ;
#47994=DIRECTION ( 'NONE',  ( 0.000000000000000000, -0.3826834323650772363, -0.9238795325112919565 ) ) ;
#47996=LINE ( 'NONE', #45979, #1833 ) ;
#47999=CYLINDRICAL_SURFACE ( 'NONE', #5547, 31.99999999999998579 ) ;
#48003=ORIENTED_EDGE ( 'NONE', *, *, #18505, .T. ) ;
#48004=DIRECTION ( 'NONE',  ( 0.000000000000000000, -1.000000000000000000, -2.312964634635746211E-15 ) ) ;
#48005=CIRCLE ( 'NONE', #8915, 31.99999999999998579 ) ;
#48008=CARTESIAN_POINT ( 'NONE',  ( 0.000000000000000000, -55.16347631943085617, 60.67117009219117563 ) ) ;
#48010=DIRECTION ( 'NONE',  ( 0.000000000000000000, -0.9238795325112821866, -0.3826834323651006065 ) ) ;
#48012=EDGE_LOOP ( 'NONE', ( #36742, #1177, #41016, #46679 ) ) ;
#48013=AXIS2_PLACEMENT_3D ( 'NONE', #34561, #42903, #19630 ) ;
#48016=EDGE_CURVE ( 'NONE', #11149, #15029, #37350, .T. ) ;
#48021=AXIS2_PLACEMENT_3D ( 'NONE', #31217, #34149, #23371 ) ;
#48027=AXIS2_PLACEMENT_3D ( 'NONE', #43991, #17560, #6318 ) ;
#48028=EDGE_CURVE ( 'NONE', #35932, #16941, #28790, .T. ) ;
#48029=AXIS2_PLACEMENT_3D ( 'NONE', #18051, #40360, #14402 ) ;
#48030=ADVANCED_FACE ( 'NONE', ( #34888 ), #27317, .T. ) ;
#48032=CYLINDRICAL_SURFACE ( 'NONE', #22971, 77.49899999999999523 ) ;
#48033=DIRECTION ( 'NONE',  ( -1.000000000000000000, -0.000000000000000000, 0.000000000000000000 ) ) ;
#48035=VECTOR ( 'NONE', #30026, 1000.000000000000000 ) ;
#48036=ORIENTED_EDGE ( 'NONE', *, *, #38190, .T. ) ;
#48042=ORIENTED_EDGE ( 'NONE', *, *, #6046, .F. ) ;
#48045=CIRCLE ( 'NONE', #43349, 82.00000000000000000 ) ;
#48046=VECTOR ( 'NONE', #50, 1000.000000000000114 ) ;
#48047=DIRECTION ( 'NONE',  ( -1.000000000000000000, -0.000000000000000000, 0.000000000000000000 ) ) ;
#48051=CIRCLE ( 'NONE', #46538, 77.49899999999999523 ) ;
#48054=ORIENTED_EDGE ( 'NONE', *, *, #26483, .F. ) ;
#48057=FACE_OUTER_BOUND ( 'NONE', #6832, .T. ) ;
#48059=VERTEX_POINT ( 'NONE', #21618 ) ;
#48079=DIRECTION ( 'NONE',  ( -1.000000000000000000, 0.000000000000000000, -0.000000000000000000 ) ) ;
#48083=LINE ( 'NONE', #40993, #44621 ) ;
#48084=CARTESIAN_POINT ( 'NONE',  ( 15.00000000000000000, -19.89357724624986545, 12.59942793731086219 ) ) ;
#48086=FACE_OUTER_BOUND ( 'NONE', #26959, .T. ) ;
#48089=DIRECTION ( 'NONE',  ( -1.000000000000000000, 0.000000000000000000, 0.000000000000000000 ) ) ;
#48090=CIRCLE ( 'NONE', #37111, 31.99999999999998579 ) ;
#48099=ORIENTED_EDGE ( 'NONE', *, *, #47087, .F. ) ;
#48104=AXIS2_PLACEMENT_3D ( 'NONE', #25173, #47462, #40844 ) ;
#48106=ORIENTED_EDGE ( 'NONE', *, *, #32452, .F. ) ;
#48113=LINE ( 'NONE', #14599, #25366 ) ;
#48115=CARTESIAN_POINT ( 'NONE',  ( 11.99999999999999822, 0.000000000000000000, 0.000000000000000000 ) ) ;
#48118=CARTESIAN_POINT ( 'NONE',  ( 0.000000000000000000, 0.000000000000000000, 0.000000000000000000 ) ) ;
#48127=VERTEX_POINT ( 'NONE', #25515 ) ;
#48128=VERTEX_POINT ( 'NONE', #37502 ) ;
#48137=DIRECTION ( 'NONE',  ( -0.000000000000000000, 0.5000000000000019984, 0.8660254037844374864 ) ) ;
#48139=EDGE_CURVE ( 'NONE', #36422, #7117, #18884, .T. ) ;
#48140=CARTESIAN_POINT ( 'NONE',  ( 11.99999999999999822, -59.75363087400035056, -56.15606465355020305 ) ) ;
#48145=EDGE_CURVE ( 'NONE', #41319, #18807, #3233, .T. ) ;
#48146=DIRECTION ( 'NONE',  ( 0.000000000000000000, 0.1564344650402244019, 0.9876883405951387696 ) ) ;
#48149=CARTESIAN_POINT ( 'NONE',  ( 0.000000000000000000, -79.10210256391353312, -21.60688246758670061 ) ) ;
#48151=CIRCLE ( 'NONE', #5151, 31.99999999999998579 ) ;
#48163=CIRCLE ( 'NONE', #1288, 77.49899999999999523 ) ;
#48165=AXIS2_PLACEMENT_3D ( 'NONE', #2752, #36042, #47067 ) ;
#48168=ORIENTED_EDGE ( 'NONE', *, *, #37134, .F. ) ;
#48174=ORIENTED_EDGE ( 'NONE', *, *, #10966, .F. ) ;
#48179=VECTOR ( 'NONE', #40095, 1000.000000000000000 ) ;
#48181=CARTESIAN_POINT ( 'NONE',  ( 0.000000000000000000, -27.74655509720617985, -77.16300072079690153 ) ) ;
#48183=DIRECTION ( 'NONE',  ( 0.000000000000000000, -0.5224985647159561264, 0.8526401643540878483 ) ) ;
#48184=EDGE_CURVE ( 'NONE', #29406, #26733, #33583, .T. ) ;
#48188=DIRECTION ( 'NONE',  ( 0.000000000000000000, 0.9723699203976756689, 0.2334453638559095823 ) ) ;
#48191=EDGE_CURVE ( 'NONE', #11246, #40230, #3001, .T. ) ;
#48197=CARTESIAN_POINT ( 'NONE',  ( 11.99999999999999822, 0.000000000000000000, 0.000000000000000000 ) ) ;
#48200=DIRECTION ( 'NONE',  ( 1.000000000000000000, 0.000000000000000000, 0.000000000000000000 ) ) ;
#48203=DIRECTION ( 'NONE',  ( -1.000000000000000000, 0.000000000000000000, 0.000000000000000000 ) ) ;
#48205=DIRECTION ( 'NONE',  ( 0.000000000000000000, 0.000000000000000000, 1.000000000000000000 ) ) ;
#48206=DIRECTION ( 'NONE',  ( -1.000000000000000000, -0.000000000000000000, -0.000000000000000000 ) ) ;
#48210=CARTESIAN_POINT ( 'NONE',  ( 11.99999999999999822, 71.27951684758069462, -30.41916302227037150 ) ) ;
#48211=ORIENTED_EDGE ( 'NONE', *, *, #27581, .F. ) ;
#48212=DIRECTION ( 'NONE',  ( 0.000000000000000000, 0.000000000000000000, 1.000000000000000000 ) ) ;
#48213=CARTESIAN_POINT ( 'NONE',  ( 0.000000000000000000, -46.54456581323847786, 59.03342792756247093 ) ) ;
#48218=VERTEX_POINT ( 'NONE', #12056 ) ;
#48222=VERTEX_POINT ( 'NONE', #8123 ) ;
#48230=ORIENTED_EDGE ( 'NONE', *, *, #6041, .T. ) ;
#48232=EDGE_LOOP ( 'NONE', ( #37301, #41201, #45808, #7564 ) ) ;
#48233=ORIENTED_EDGE ( 'NONE', *, *, #34864, .F. ) ;
#48234=ORIENTED_EDGE ( 'NONE', *, *, #33489, .F. ) ;
#48236=EDGE_CURVE ( 'NONE', #29872, #15938, #36603, .T. ) ;
#48239=CIRCLE ( 'NONE', #44328, 82.00000000000000000 ) ;
#48251=VECTOR ( 'NONE', #47385, 1000.000000000000000 ) ;
#48256=ORIENTED_EDGE ( 'NONE', *, *, #16583, .T. ) ;
#48258=CARTESIAN_POINT ( 'NONE',  ( 11.99999999999999822, 5.256550761633951296, -77.32052557432835727 ) ) ;
#48260=ORIENTED_EDGE ( 'NONE', *, *, #33237, .F. ) ;
#48264=DIRECTION ( 'NONE',  ( 0.000000000000000000, 0.000000000000000000, 1.000000000000000000 ) ) ;
#48269=CARTESIAN_POINT ( 'NONE',  ( 11.99999999999999822, -41.76106447765443619, -62.50884508063471401 ) ) ;
#48274=DIRECTION ( 'NONE',  ( 0.000000000000000000, 0.000000000000000000, 1.000000000000000000 ) ) ;
#48279=DIRECTION ( 'NONE',  ( -1.000000000000000000, 0.000000000000000000, 0.000000000000000000 ) ) ;
#48284=DIRECTION ( 'NONE',  ( -1.000000000000000000, 0.000000000000000000, -0.000000000000000000 ) ) ;
#48296=EDGE_LOOP ( 'NONE', ( #5678, #24010, #29226, #43817 ) ) ;
#48301=CIRCLE ( 'NONE', #24863, 31.99999999999998579 ) ;
#48302=EDGE_LOOP ( 'NONE', ( #31463, #26087, #11470, #10674 ) ) ;
#48312=LINE ( 'NONE', #10147, #11347 ) ;
#48313=LINE ( 'NONE', #14792, #6388 ) ;
#48319=FACE_OUTER_BOUND ( 'NONE', #10905, .T. ) ;
#48326=DIRECTION ( 'NONE',  ( -1.000000000000000000, -0.000000000000000000, 0.000000000000000000 ) ) ;
#48327=CARTESIAN_POINT ( 'NONE',  ( -10.00000000000000000, 0.000000000000000000, 0.000000000000000000 ) ) ;
#48336=AXIS2_PLACEMENT_3D ( 'NONE', #20490, #34446, #38382 ) ;
#48347=ADVANCED_FACE ( 'NONE', ( #35273 ), #46296, .F. ) ;
#48350=VERTEX_POINT ( 'NONE', #1750 ) ;
#48351=LINE ( 'NONE', #15326, #28862 ) ;
#48354=VERTEX_POINT ( 'NONE', #42638 ) ;
#48359=FACE_OUTER_BOUND ( 'NONE', #28145, .T. ) ;
#48360=EDGE_CURVE ( 'NONE', #5353, #5571, #5914, .T. ) ;
#48361=DIRECTION ( 'NONE',  ( 0.000000000000000000, -0.9969173337331287410, 0.07845909572783489605 ) ) ;
#48362=DIRECTION ( 'NONE',  ( 0.000000000000000000, 0.8090169943749438985, -0.5877852522924780221 ) ) ;
#48363=ORIENTED_EDGE ( 'NONE', *, *, #24605, .T. ) ;
#48367=DIRECTION ( 'NONE',  ( -1.000000000000000000, 0.000000000000000000, 0.000000000000000000 ) ) ;
#48371=DIRECTION ( 'NONE',  ( -1.000000000000000000, -0.000000000000000000, -0.000000000000000000 ) ) ;
#48372=DIRECTION ( 'NONE',  ( 0.000000000000000000, 0.000000000000000000, 1.000000000000000000 ) ) ;
#48380=CARTESIAN_POINT ( 'NONE',  ( 15.00000000000000000, -18.13022148937263012, -15.02647892043543898 ) ) ;
#48384=DIRECTION ( 'NONE',  ( 0.000000000000000000, 0.3090169943749480064, -0.9510565162951534202 ) ) ;
#48390=DIRECTION ( 'NONE',  ( -1.000000000000000000, -0.000000000000000000, -0.000000000000000000 ) ) ;
#48393=CARTESIAN_POINT ( 'NONE',  ( 0.000000000000000000, 0.000000000000000000, 0.000000000000000000 ) ) ;
#48396=ORIENTED_EDGE ( 'NONE', *, *, #23157, .T. ) ;
#48397=AXIS2_PLACEMENT_3D ( 'NONE', #1261, #45546, #4456 ) ;
#48398=VECTOR ( 'NONE', #3867, 1000.000000000000000 ) ;
#48399=ORIENTED_EDGE ( 'NONE', *, *, #25086, .F. ) ;
#48402=DIRECTION ( 'NONE',  ( -1.000000000000000000, 0.000000000000000000, 0.000000000000000000 ) ) ;
#48411=ADVANCED_FACE ( 'NONE', ( #13248 ), #47260, .T. ) ;
#48414=DIRECTION ( 'NONE',  ( -1.000000000000000000, -0.000000000000000000, -0.000000000000000000 ) ) ;
#48415=ORIENTED_EDGE ( 'NONE', *, *, #33531, .F. ) ;
#48417=FACE_OUTER_BOUND ( 'NONE', #28356, .T. ) ;
#48418=DIRECTION ( 'NONE',  ( 0.000000000000000000, 0.000000000000000000, 1.000000000000000000 ) ) ;
#48421=VERTEX_POINT ( 'NONE', #9555 ) ;
#48422=FILL_AREA_STYLE ('',( #8032 ) ) ;
#48426=AXIS2_PLACEMENT_3D ( 'NONE', #22168, #41031, #14832 ) ;
#48428=CARTESIAN_POINT ( 'NONE',  ( 11.99999999999999822, 0.000000000000000000, 0.000000000000000000 ) ) ;
#48431=DIRECTION ( 'NONE',  ( 0.000000000000000000, 0.8090169943749486725, -0.5877852522924713607 ) ) ;
#48433=CARTESIAN_POINT ( 'NONE',  ( 11.99999999999999822, -41.76106447765533147, 62.50884508063410294 ) ) ;
#48434=CARTESIAN_POINT ( 'NONE',  ( 11.99999999999999822, -55.19960302592029677, -51.03279382321147750 ) ) ;
#48438=VECTOR ( 'NONE', #5523, 1000.000000000000000 ) ;
#48440=DIRECTION ( 'NONE',  ( 0.000000000000000000, -0.4067366430757908269, 0.9135454576426049744 ) ) ;
#48443=ORIENTED_EDGE ( 'NONE', *, *, #24470, .T. ) ;
#48451=EDGE_CURVE ( 'NONE', #35068, #31692, #45246, .T. ) ;
ENDSEC;
END-ISO-10303-21;
